ISO-10303-21;
HEADER;
FILE_DESCRIPTION (('STEP AP214'),
    '1' );
FILE_NAME ('Handle.step',
    '2026-10-07T06:38:26',
    ( '' ),
    ( '' ),
    'SwSTEP 2.0',
    'SolidWorks 2021',
    '' );
FILE_SCHEMA (( 'AUTOMOTIVE_DESIGN' ));
ENDSEC;

DATA;
#20=LINE ( 'NONE', #9560, #12153 ) ;
#22=CARTESIAN_POINT ( 'NONE',  ( 112.1249999999998437, 1.767766952966293159, 1.767766952966431937 ) ) ;
#32=CARTESIAN_POINT ( 'NONE',  ( 104.9374999999997726, 2.500000000000114575, -1.035533905932448873 ) ) ;
#35=MECHANICAL_DESIGN_GEOMETRIC_PRESENTATION_REPRESENTATION('',(#14770),#26040);
#39=CARTESIAN_POINT ( 'NONE',  ( 118.3749999999999147, -1.767766952966293159, 1.767766952966431937 ) ) ;
#41=VECTOR ( 'NONE', #11597, 1000.000000000000000 ) ;
#46=EDGE_CURVE ( 'NONE', #22177, #19788, #18313, .T. ) ;
#52=CARTESIAN_POINT ( 'NONE',  ( 106.7497167782375129, 1.308140751793612777, 1.308140751793529510 ) ) ;
#55=CARTESIAN_POINT ( 'NONE',  ( 119.3127832217621034, 1.849990392679501827, -0.7662911109077087390 ) ) ;
#73=DIRECTION ( 'NONE',  ( 5.551115123125785167E-17, -1.000000000000000000, -8.881784197001256268E-16 ) ) ;
#76=CARTESIAN_POINT ( 'NONE',  ( 116.5622167782374135, 1.849990392679562001, -0.7662911109077087390 ) ) ;
#81=CARTESIAN_POINT ( 'NONE',  ( 115.7502832217623308, -1.308140751793585022, 1.308140751793640533 ) ) ;
#104=CARTESIAN_POINT ( 'NONE',  ( 112.4374999999998010, -2.499999999999934719, 1.035533905932989551 ) ) ;
#116=CARTESIAN_POINT ( 'NONE',  ( 114.5624999999997442, -2.499999999999934719, -1.035533905932448873 ) ) ;
#118=CARTESIAN_POINT ( 'NONE',  ( 106.5627832217621602, 0.7662911109078588412, 1.849990392679712103 ) ) ;
#135=CARTESIAN_POINT ( 'NONE',  ( 107.1249999999998437, 1.767766952966265404, 1.767766952966320915 ) ) ;
#144=CARTESIAN_POINT ( 'NONE',  ( 108.6877832217621318, -0.7662911109077388261, 1.849990392679712103 ) ) ;
#148=UNCERTAINTY_MEASURE_WITH_UNIT (LENGTH_MEASURE( 1.000000000000000082E-05 ), #22122, 'distance_accuracy_value', 'NONE');
#160=CARTESIAN_POINT ( 'NONE',  ( 118.4613248654051034, 1.110223024625156540E-13, -2.000000000000001776 ) ) ;
#163=CARTESIAN_POINT ( 'NONE',  ( 113.2113248654051034, -1.999999999999918510, 1.110223024625156540E-13 ) ) ;
#165=ORIENTED_EDGE ( 'NONE', *, *, #8341, .F. ) ;
#174=CARTESIAN_POINT ( 'NONE',  ( 117.7261751345945413, -1.999999999999971800, 0.8284271247464157772 ) ) ;
#181=CARTESIAN_POINT ( 'NONE',  ( 114.2886751345947971, 2.000000000000029310, 1.110223024625156540E-13 ) ) ;
#182=CARTESIAN_POINT ( 'NONE',  ( 110.6249999999998437, -1.767766952966376426, -1.767766952966320915 ) ) ;
#188=CARTESIAN_POINT ( 'NONE',  ( 117.8122167782374135, 0.7662911109077388261, 1.849990392679832230 ) ) ;
#196=EDGE_LOOP ( 'NONE', ( #23554, #27384, #25817, #24929 ) ) ;
#204=CARTESIAN_POINT ( 'NONE',  ( 104.5622167782374703, 1.849990392679501827, -0.7662911109076485650 ) ) ;
#206=CARTESIAN_POINT ( 'NONE',  ( 119.3752832217622313, 1.849990392679523588, 0.000000000000000000 ) ) ;
#224=CARTESIAN_POINT ( 'NONE',  ( 116.4372167782373850, 0.7662911109078588412, -1.849990392679411677 ) ) ;
#228=CARTESIAN_POINT ( 'NONE',  ( 114.8752832217623165, -1.849990392679523588, 0.000000000000000000 ) ) ;
#248=CARTESIAN_POINT ( 'NONE',  ( 113.0624999999997726, 2.500000000000084821, 1.035533905932989551 ) ) ;
#261=CARTESIAN_POINT ( 'NONE',  ( 111.3124999999998295, -1.035533905932629173, 2.500000000000325517 ) ) ;
#263=CARTESIAN_POINT ( 'NONE',  ( 106.6877832217621602, -0.7662911109076785410, 1.849990392679712103 ) ) ;
#281=CARTESIAN_POINT ( 'NONE',  ( 106.5624999999998295, -2.499999999999874767, -1.035533905932629173 ) ) ;
#283=VERTEX_POINT ( 'NONE', #9216 ) ;
#287=CARTESIAN_POINT ( 'NONE',  ( 108.0002832217622597, -1.308140751793585022, -1.308140751793640533 ) ) ;
#292=CARTESIAN_POINT ( 'NONE',  ( 116.2113248654050750, -2.000000000000029310, 0.000000000000000000 ) ) ;
#324=CARTESIAN_POINT ( 'NONE',  ( 105.4374999999998153, -2.499999999999994671, 1.035533905932929599 ) ) ;
#334=CARTESIAN_POINT ( 'NONE',  ( 116.4372167782373850, 0.7662911109078588412, -1.849990392679411677 ) ) ;
#338=CARTESIAN_POINT ( 'NONE',  ( 116.6249999999999716, -1.767766952966459693, -1.767766952966209892 ) ) ;
#349=CARTESIAN_POINT ( 'NONE',  ( 106.5622167782373708, 1.849990392679501827, -0.7662911109076485650 ) ) ;
#352=CARTESIAN_POINT ( 'NONE',  ( 114.3127832217620465, 1.849990392679562001, -0.7662911109076485650 ) ) ;
#369=CARTESIAN_POINT ( 'NONE',  ( 115.6872167782374561, 1.849990392679532247, 0.7662911109080692285 ) ) ;
#373=CARTESIAN_POINT ( 'NONE',  ( 112.5627832217621886, 0.7662911109078588412, 1.849990392679712103 ) ) ;
#381=ORIENTED_EDGE ( 'NONE', *, *, #8508, .F. ) ;
#386=CYLINDRICAL_SURFACE ( 'NONE', #2332, 2.000000000000012879 ) ;
#394=CARTESIAN_POINT ( 'NONE',  ( 113.9999999999998153, 2.500000000000085265, 0.000000000000000000 ) ) ;
#401=CARTESIAN_POINT ( 'NONE',  ( 106.8511751345945981, -1.999999999999941602, -0.8284271247459350507 ) ) ;
#402=CARTESIAN_POINT ( 'NONE',  ( 111.3749999999999289, -1.767766952966320915, 1.767766952966431937 ) ) ;
#409=CARTESIAN_POINT ( 'NONE',  ( 107.5622167782374561, 1.849990392679472073, -0.7662911109077686911 ) ) ;
#422=CARTESIAN_POINT ( 'NONE',  ( 108.1874999999998579, 1.035533905932719101, 2.500000000000205169 ) ) ;
#430=CARTESIAN_POINT ( 'NONE',  ( 109.6252832217622739, -2.775557561562891351E-14, 1.849990392679523588 ) ) ;
#431=CARTESIAN_POINT ( 'NONE',  ( 1.110223024625164183E-16, -2.000000000000012879, -1.776356839400262692E-15 ) ) ;
#439=DIRECTION ( 'NONE',  ( -1.000000000000000000, -1.665334536937736783E-16, -2.220446049250315546E-16 ) ) ;
#440=ORIENTED_EDGE ( 'NONE', *, *, #16202, .T. ) ;
#444=CARTESIAN_POINT ( 'NONE',  ( 111.7886751345948255, -1.999999999999974021, 0.000000000000000000 ) ) ;
#460=ADVANCED_FACE ( 'NONE', ( #26093 ), #4748, .F. ) ;
#470=CARTESIAN_POINT ( 'NONE',  ( 104.8124999999998153, 1.035533905932779275, -2.499999999999904521 ) ) ;
#480=CARTESIAN_POINT ( 'NONE',  ( 115.9372167782375129, -0.7662911109076785410, 1.849990392679712103 ) ) ;
#486=CARTESIAN_POINT ( 'NONE',  ( 116.4999999999999574, -2.499999999999891198, 0.000000000000000000 ) ) ;
#498=UNCERTAINTY_MEASURE_WITH_UNIT (LENGTH_MEASURE( 1.000000000000000082E-05 ), #21304, 'distance_accuracy_value', 'NONE');
#500=CARTESIAN_POINT ( 'NONE',  ( 105.2886751345946550, 2.000000000000057288, 0.000000000000000000 ) ) ;
#501=CARTESIAN_POINT ( 'NONE',  ( 105.4997167782376550, 1.308140751793668288, -1.308140751793640533 ) ) ;
#503=CARTESIAN_POINT ( 'NONE',  ( 114.1877832217620892, 0.7662911109078588412, -1.849990392679291551 ) ) ;
#517=CARTESIAN_POINT ( 'NONE',  ( 115.1488248654049613, -1.999999999999941602, 0.8284271247464759513 ) ) ;
#522=CARTESIAN_POINT ( 'NONE',  ( 118.8511751345945413, -1.999999999999911626, -0.8284271247460553989 ) ) ;
#524=CARTESIAN_POINT ( 'NONE',  ( 104.7836787521071216, 1.152921169277180358, 1.489079044806365992 ) ) ;
#538=DIRECTION ( 'NONE',  ( 5.551115123125785167E-17, -1.000000000000000000, -8.881784197001256268E-16 ) ) ;
#539=CARTESIAN_POINT ( 'NONE',  ( 111.4613248654051176, 5.551115123125782702E-14, -2.000000000000001776 ) ) ;
#555=CARTESIAN_POINT ( 'NONE',  ( 114.0624999999997300, 2.500000000000114575, 1.035533905932989551 ) ) ;
#564=CARTESIAN_POINT ( 'NONE',  ( 104.6872167782374277, 1.849990392679532247, 0.7662911109080692285 ) ) ;
#575=CARTESIAN_POINT ( 'NONE',  ( 107.4374999999997868, -2.499999999999964473, 1.035533905932989551 ) ) ;
#584=CARTESIAN_POINT ( 'NONE',  ( 109.7502832217623734, -1.308140751793612777, 1.308140751793640533 ) ) ;
#628=CARTESIAN_POINT ( 'NONE',  ( 107.9999999999998863, 2.500000000000002220, 0.000000000000000000 ) ) ;
#638=EDGE_LOOP ( 'NONE', ( #15445, #9531, #17876, #24636 ) ) ;
#639=CARTESIAN_POINT ( 'NONE',  ( 116.9997167782375698, -1.308140751793557266, 1.308140751793862577 ) ) ;
#640=CARTESIAN_POINT ( 'NONE',  ( 118.3511751345946266, 2.000000000000091926, 0.8284271247463557142 ) ) ;
#642=EDGE_CURVE ( 'NONE', #1738, #14551, #13017, .T. ) ;
#645=CARTESIAN_POINT ( 'NONE',  ( 117.5624999999997584, -2.499999999999904521, -1.035533905932508825 ) ) ;
#647=EDGE_CURVE ( 'NONE', #14487, #18130, #29517, .T. ) ;
#654=LINE ( 'NONE', #11769, #4245 ) ;
#663=CARTESIAN_POINT ( 'NONE',  ( 117.1877832217620892, 0.7662911109078287542, -1.849990392679472073 ) ) ;
#679=EDGE_LOOP ( 'NONE', ( #963, #7486, #21683, #27878 ) ) ;
#684=CARTESIAN_POINT ( 'NONE',  ( 112.7886751345947403, -1.999999999999946265, 0.000000000000000000 ) ) ;
#694=DIRECTION ( 'NONE',  ( 5.551115123125785167E-17, -1.000000000000000000, -8.881784197001256268E-16 ) ) ;
#696=CARTESIAN_POINT ( 'NONE',  ( 111.2113248654051176, -1.999999999999946265, 0.000000000000000000 ) ) ;
#711=CARTESIAN_POINT ( 'NONE',  ( 110.8749999999998721, 1.767766952966431937, -1.767766952966209892 ) ) ;
#715=CARTESIAN_POINT ( 'NONE',  ( 112.9613248654051461, 5.551115123125782702E-14, 2.000000000000112799 ) ) ;
#720=CARTESIAN_POINT ( 'NONE',  ( 119.5002832217621886, 1.308140751793640533, 1.308140751793751555 ) ) ;
#730=CARTESIAN_POINT ( 'NONE',  ( 104.8124999999997868, 1.035533905932779275, -2.499999999999904521 ) ) ;
#741=CARTESIAN_POINT ( 'NONE',  ( 118.5624999999997016, -2.499999999999874767, -1.035533905932568777 ) ) ;
#752=CARTESIAN_POINT ( 'NONE',  ( 120.3124999999998579, -1.035533905932689347, 2.500000000000205169 ) ) ;
#767=VECTOR ( 'NONE', #17071, 1000.000000000000000 ) ;
#778=CARTESIAN_POINT ( 'NONE',  ( 0.000000000000000000, 0.000000000000000000, 0.000000000000000000 ) ) ;
#783=CARTESIAN_POINT ( 'NONE',  ( 104.5624999999997442, -2.499999999999934719, -1.035533905932689347 ) ) ;
#792=CARTESIAN_POINT ( 'NONE',  ( 118.7497167782375982, 1.308140751793696044, 1.308140751793640533 ) ) ;
#796=CARTESIAN_POINT ( 'NONE',  ( 114.2499999999999147, -1.110223024625156540E-13, 2.500000000000057732 ) ) ;
#821=DIRECTION ( 'NONE',  ( -1.000000000000000000, -1.665334536937736783E-16, -2.220446049250315546E-16 ) ) ;
#849=AXIS2_PLACEMENT_3D ( 'NONE', #28828, #17055, #25940 ) ;
#851=CARTESIAN_POINT ( 'NONE',  ( 113.0863248654050892, -1.414213562373173305, 1.414213562373145550 ) ) ;
#865=DIRECTION ( 'NONE',  ( -1.000000000000000000, -1.665334536937736783E-16, -2.220446049250315546E-16 ) ) ;
#877=CARTESIAN_POINT ( 'NONE',  ( 105.0627832217622455, -0.7662911109076785410, -1.849990392679411677 ) ) ;
#883=DIRECTION ( 'NONE',  ( -1.000000000000000000, -1.665334536937736783E-16, -2.220446049250315546E-16 ) ) ;
#888=CARTESIAN_POINT ( 'NONE',  ( 119.9999999999999289, 2.500000000000057732, 1.110223024625156540E-13 ) ) ;
#895=ORIENTED_EDGE ( 'NONE', *, *, #26464, .T. ) ;
#901=FILL_AREA_STYLE_COLOUR ( '', #10334 ) ;
#914=CARTESIAN_POINT ( 'NONE',  ( 107.8124999999997442, 1.035533905932809473, -2.499999999999784173 ) ) ;
#918=CARTESIAN_POINT ( 'NONE',  ( 104.7401757384975980, 1.479039993424821287, -1.137087370475787784 ) ) ;
#919=ORIENTED_EDGE ( 'NONE', *, *, #28096, .T. ) ;
#922=FACE_OUTER_BOUND ( 'NONE', #3937, .T. ) ;
#925=ORIENTED_EDGE ( 'NONE', *, *, #18609, .T. ) ;
#926=CARTESIAN_POINT ( 'NONE',  ( 112.8122167782374419, 0.7662911109079189043, 1.849990392679772278 ) ) ;
#931=CARTESIAN_POINT ( 'NONE',  ( 115.8749999999998579, 1.767766952966431937, -1.767766952966320915 ) ) ;
#944=CARTESIAN_POINT ( 'NONE',  ( 116.3363248654050608, -1.414213562373201061, -1.414213562373034527 ) ) ;
#962=CARTESIAN_POINT ( 'NONE',  ( 114.3122167782374419, -0.7662911109077388261, -1.849990392679231599 ) ) ;
#963=ORIENTED_EDGE ( 'NONE', *, *, #30074, .T. ) ;
#980=CARTESIAN_POINT ( 'NONE',  ( 120.0000000000000000, 1.338994316744045454, 1.808804601853416072 ) ) ;
#988=CARTESIAN_POINT ( 'NONE',  ( 117.0386751345946692, 5.551115123125782702E-14, -2.000000000000001776 ) ) ;
#998=CARTESIAN_POINT ( 'NONE',  ( -1.110223024625164676E-16, 2.000000000000012879, 2.021286199229734960E-15 ) ) ;
#1003=CARTESIAN_POINT ( 'NONE',  ( 120.3127832217622171, 1.849990392679591977, -0.7662911109075883909 ) ) ;
#1004=ADVANCED_FACE ( 'NONE', ( #16866, #5585 ), #5138, .F. ) ;
#1011=EDGE_CURVE ( 'NONE', #22693, #15450, #2747, .T. ) ;
#1017=CARTESIAN_POINT ( 'NONE',  ( 105.6874999999997442, -1.035533905932659149, -2.499999999999724221 ) ) ;
#1027=CARTESIAN_POINT ( 'NONE',  ( 118.4374999999998863, -2.499999999999964473, 1.035533905932929599 ) ) ;
#1048=CARTESIAN_POINT ( 'NONE',  ( 109.9997167782376835, -1.308140751793612777, 1.308140751793640533 ) ) ;
#1058=AXIS2_PLACEMENT_3D ( 'NONE', #778, #19533, #17385 ) ;
#1067=VERTEX_POINT ( 'NONE', #13320 ) ;
#1071=DIRECTION ( 'NONE',  ( -1.000000000000000000, -1.665334536937736783E-16, -2.220446049250315546E-16 ) ) ;
#1077=CARTESIAN_POINT ( 'NONE',  ( 119.9999999999996163, 1.621546429789529453, -1.617766924407829654 ) ) ;
#1083=CARTESIAN_POINT ( 'NONE',  ( 0.000000000000000000, 0.000000000000000000, 0.000000000000000000 ) ) ;
#1087=CARTESIAN_POINT ( 'NONE',  ( 112.2497167782374561, -1.308140751793585022, -1.308140751793640533 ) ) ;
#1094=CARTESIAN_POINT ( 'NONE',  ( 115.3749999999999574, -1.767766952966320915, 1.767766952966431937 ) ) ;
#1104=( GEOMETRIC_REPRESENTATION_CONTEXT ( 3 ) GLOBAL_UNCERTAINTY_ASSIGNED_CONTEXT ( ( #498 ) ) GLOBAL_UNIT_ASSIGNED_CONTEXT ( ( #21304, #26930, #28783 ) ) REPRESENTATION_CONTEXT ( 'NONE', 'WORKASPACE' ) );
#1115=CARTESIAN_POINT ( 'NONE',  ( 111.1872167782375698, -1.849990392679472073, -0.7662911109075283278 ) ) ;
#1116=( BOUNDED_CURVE ( )  B_SPLINE_CURVE ( 2, ( #10622, #3670, #22746, #13106, #10787, #29483, #3826, #13256, #22596 ),
 .UNSPECIFIED., .F., .T. ) 
 B_SPLINE_CURVE_WITH_KNOTS ( ( 3, 2, 2, 2, 3 ),
 ( 0.05882352941176470507, 0.06617647058823529493, 0.07352941176470588480, 0.08088235294117647467, 0.08823529411764706454 ),
 .UNSPECIFIED. ) 
 CURVE ( )  GEOMETRIC_REPRESENTATION_ITEM ( )  RATIONAL_B_SPLINE_CURVE ( ( 1.000000000000000000, 0.9238795325112867385, 1.000000000000000000, 0.9238795325112867385, 1.000000000000000000, 0.9238795325112867385, 1.000000000000000000, 0.9238795325112867385, 1.000000000000000000 ) ) 
 REPRESENTATION_ITEM ( '' )  );
#1153=CARTESIAN_POINT ( 'NONE',  ( 120.0002832217621886, -1.308140751793557266, -1.308140751793529510 ) ) ;
#1162=CARTESIAN_POINT ( 'NONE',  ( 105.6249999999999005, -1.767766952966376426, -1.767766952966320915 ) ) ;
#1168=CARTESIAN_POINT ( 'NONE',  ( 118.8988248654049187, 0.8284271247463855792, 2.000000000000151879 ) ) ;
#1170=CARTESIAN_POINT ( 'NONE',  ( 120.3124999999998579, -1.035533905932689347, 2.500000000000205169 ) ) ;
#1193=CARTESIAN_POINT ( 'NONE',  ( 107.2113248654050608, -1.999999999999946265, 0.000000000000000000 ) ) ;
#1210=CARTESIAN_POINT ( 'NONE',  ( 114.3752832217622597, 1.849990392679551343, 0.000000000000000000 ) ) ;
#1219=CARTESIAN_POINT ( 'NONE',  ( 104.7401757384974843, -1.849990392679535134, -0.2444181134155588853 ) ) ;
#1220=VERTEX_POINT ( 'NONE', #22811 ) ;
#1226=CARTESIAN_POINT ( 'NONE',  ( 117.7886751345947545, -1.999999999999946265, 1.110223024625156540E-13 ) ) ;
#1229=CARTESIAN_POINT ( 'NONE',  ( 112.3747167782374703, -5.551115123125782702E-14, -1.849990392679523588 ) ) ;
#1234=CARTESIAN_POINT ( 'NONE',  ( 115.4374999999997868, -2.499999999999934719, 1.035533905932929599 ) ) ;
#1236=CYLINDRICAL_SURFACE ( 'NONE', #12553, 2.000000000000012879 ) ;
#1264=CARTESIAN_POINT ( 'NONE',  ( 109.9999999999999432, 2.500000000000030198, 0.000000000000000000 ) ) ;
#1270=CARTESIAN_POINT ( 'NONE',  ( 110.7497167782376550, 1.308140751793640533, 1.308140751793640533 ) ) ;
#1271=ORIENTED_EDGE ( 'NONE', *, *, #12673, .F. ) ;
#1288=SURFACE_STYLE_FILL_AREA ( #19737 ) ;
#1291=CARTESIAN_POINT ( 'NONE',  ( 117.8363248654051176, 1.414213562373145550, 1.414213562373034527 ) ) ;
#1305=CARTESIAN_POINT ( 'NONE',  ( 111.9613248654051461, -2.775557561562891351E-14, 2.000000000000112799 ) ) ;
#1306=CARTESIAN_POINT ( 'NONE',  ( 120.2497167782375271, -1.308140751793529510, -1.308140751793640533 ) ) ;
#1312=CARTESIAN_POINT ( 'NONE',  ( 1101.535898384862321, 1.665334536937736830E-13, 2.220446049250315605E-13 ) ) ;
#1319=CARTESIAN_POINT ( 'NONE',  ( 0.000000000000000000, 0.000000000000000000, 0.000000000000000000 ) ) ;
#1325=ORIENTED_EDGE ( 'NONE', *, *, #19386, .F. ) ;
#1326=LINE ( 'NONE', #10740, #18160 ) ;
#1330=CARTESIAN_POINT ( 'NONE',  ( 118.7738248654049897, 2.000000000000122125, 0.8284271247462955401 ) ) ;
#1333=CARTESIAN_POINT ( 'NONE',  ( 114.9374999999997868, 2.500000000000055067, -1.035533905932629173 ) ) ;
#1347=CARTESIAN_POINT ( 'NONE',  ( 111.8752832217622881, -1.849990392679579099, 1.110223024625156540E-13 ) ) ;
#1351=( BOUNDED_CURVE ( )  B_SPLINE_CURVE ( 2, ( #11002, #18216, #11310, #17765, #20347, #30007, #29702 ),
 .UNSPECIFIED., .F., .F. ) 
 B_SPLINE_CURVE_WITH_KNOTS ( ( 3, 2, 2, 3 ),
 ( 0.01238478393654788429, 0.01470588235294112422, 0.02205882352941179736, 0.02941176470588236294 ),
 .UNSPECIFIED. ) 
 CURVE ( )  GEOMETRIC_REPRESENTATION_ITEM ( )  RATIONAL_B_SPLINE_CURVE ( ( 0.9671125746062365636, 0.9759710988701293388, 1.000000000000000000, 0.9238795325112867385, 1.000000000000000000, 0.9238795325112867385, 1.000000000000000000 ) ) 
 REPRESENTATION_ITEM ( '' )  );
#1362=ORIENTED_EDGE ( 'NONE', *, *, #29688, .F. ) ;
#1365=FACE_OUTER_BOUND ( 'NONE', #19338, .T. ) ;
#1368=CARTESIAN_POINT ( 'NONE',  ( 107.5386751345947403, 5.551115123125782702E-14, 2.000000000000001776 ) ) ;
#1375=CARTESIAN_POINT ( 'NONE',  ( 115.0002832217621886, -1.308140751793585022, -1.308140751793640533 ) ) ;
#1390=CARTESIAN_POINT ( 'NONE',  ( 112.4372167782373708, 0.7662911109079189043, -1.849990392679231599 ) ) ;
#1396=CARTESIAN_POINT ( 'NONE',  ( 113.1874999999998437, 1.035533905932779275, 2.500000000000205169 ) ) ;
#1401=( BOUNDED_CURVE ( )  B_SPLINE_CURVE ( 2, ( #21034, #18890, #18282, #25295, #23026, #21774, #7339, #12139, #16745 ),
 .UNSPECIFIED., .F., .F. ) 
 B_SPLINE_CURVE_WITH_KNOTS ( ( 3, 2, 2, 2, 3 ),
 ( 0.5588235294117647189, 0.5661764705882352811, 0.5735294117647058432, 0.5808823529411765163, 0.5882352941176470784 ),
 .UNSPECIFIED. ) 
 CURVE ( )  GEOMETRIC_REPRESENTATION_ITEM ( )  RATIONAL_B_SPLINE_CURVE ( ( 1.000000000000000000, 0.9238795325112867385, 1.000000000000000000, 0.9238795325112867385, 1.000000000000000000, 0.9238795325112867385, 1.000000000000000000, 0.9238795325112867385, 1.000000000000000000 ) ) 
 REPRESENTATION_ITEM ( '' )  );
#1415=CARTESIAN_POINT ( 'NONE',  ( 113.7886751345947687, -1.999999999999918510, 0.000000000000000000 ) ) ;
#1419=FACE_OUTER_BOUND ( 'NONE', #6136, .T. ) ;
#1424=CARTESIAN_POINT ( 'NONE',  ( 110.9374999999997442, 2.500000000000055067, -1.035533905932388699 ) ) ;
#1437=VERTEX_POINT ( 'NONE', #1415 ) ;
#1458=CARTESIAN_POINT ( 'NONE',  ( 114.6488248654050324, 2.000000000000122125, -0.8284271247459350507 ) ) ;
#1460=CARTESIAN_POINT ( 'NONE',  ( 111.7113248654050892, 2.000000000000057288, 0.000000000000000000 ) ) ;
#1461=CARTESIAN_POINT ( 'NONE',  ( 119.9372167782374277, -0.7662911109077388261, 1.849990392679652151 ) ) ;
#1466=CARTESIAN_POINT ( 'NONE',  ( 118.3752832217622029, 1.849990392679523588, 0.000000000000000000 ) ) ;
#1468=LINE ( 'NONE', #24665, #22836 ) ;
#1485=CARTESIAN_POINT ( 'NONE',  ( 119.0238248654050466, -0.8284271247461453269, 2.000000000000091926 ) ) ;
#1487=CARTESIAN_POINT ( 'NONE',  ( 114.4999999999998721, -2.499999999999891198, 0.000000000000000000 ) ) ;
#1489=CARTESIAN_POINT ( 'NONE',  ( 105.7738248654049897, 2.000000000000151879, 0.8284271247464157772 ) ) ;
#1495=CARTESIAN_POINT ( 'NONE',  ( 115.9374999999998010, 2.500000000000055067, -1.035533905932629173 ) ) ;
#1497=CARTESIAN_POINT ( 'NONE',  ( 111.8127832217621460, -1.849990392679441875, 0.7662911109079489913 ) ) ;
#1506=EDGE_CURVE ( 'NONE', #10100, #16147, #23761, .T. ) ;
#1526=CARTESIAN_POINT ( 'NONE',  ( 112.8127832217621886, -1.849990392679441875, 0.7662911109079489913 ) ) ;
#1544=CARTESIAN_POINT ( 'NONE',  ( 113.8122167782374987, 0.7662911109077987781, 1.849990392679652151 ) ) ;
#1546=CARTESIAN_POINT ( 'NONE',  ( 113.9761751345945839, -0.8284271247461453269, -1.999999999999791278 ) ) ;
#1550=EDGE_CURVE ( 'NONE', #22257, #29700, #23095, .T. ) ;
#1552=CARTESIAN_POINT ( 'NONE',  ( 110.5238248654050608, 0.8284271247463257382, -1.999999999999731104 ) ) ;
#1580=CARTESIAN_POINT ( 'NONE',  ( 108.5624999999997442, -2.499999999999934719, -1.035533905932568777 ) ) ;
#1584=CARTESIAN_POINT ( 'NONE',  ( 105.2113248654051745, -1.999999999999974021, 0.000000000000000000 ) ) ;
#1603=FACE_OUTER_BOUND ( 'NONE', #20031, .T. ) ;
#1642=CARTESIAN_POINT ( 'NONE',  ( 114.6874999999997300, -1.035533905932689347, -2.499999999999784173 ) ) ;
#1646=CARTESIAN_POINT ( 'NONE',  ( 106.2113248654051745, -1.999999999999946265, 0.000000000000000000 ) ) ;
#1655=CARTESIAN_POINT ( 'NONE',  ( 116.0624999999999005, 2.500000000000055067, 1.035533905932929599 ) ) ;
#1656=CARTESIAN_POINT ( 'NONE',  ( 108.8752832217621744, -1.849990392679468076, 1.110223024625156540E-13 ) ) ;
#1657=CARTESIAN_POINT ( 'NONE',  ( 107.7738248654050466, 2.000000000000061728, 0.8284271247463557142 ) ) ;
#1661=CARTESIAN_POINT ( 'NONE',  ( 108.3122167782374135, -0.7662911109077388261, -1.849990392679351725 ) ) ;
#1694=ORIENTED_EDGE ( 'NONE', *, *, #28303, .T. ) ;
#1700=CARTESIAN_POINT ( 'NONE',  ( 108.6247167782375271, 1.849990392679551343, 0.000000000000000000 ) ) ;
#1715=CARTESIAN_POINT ( 'NONE',  ( 117.5386751345946692, 5.551115123125782702E-14, 2.000000000000223821 ) ) ;
#1724=CARTESIAN_POINT ( 'NONE',  ( 106.5386751345947971, 1.110223024625156540E-13, 2.000000000000001776 ) ) ;
#1725=EDGE_CURVE ( 'NONE', #12068, #283, #5873, .T. ) ;
#1734=CARTESIAN_POINT ( 'NONE',  ( 107.3749999999999574, -1.767766952966293159, 1.767766952966431937 ) ) ;
#1738=VERTEX_POINT ( 'NONE', #23375 ) ;
#1751=CARTESIAN_POINT ( 'NONE',  ( 112.8511751345945981, -1.999999999999941602, -0.8284271247459952248 ) ) ;
#1764=CARTESIAN_POINT ( 'NONE',  ( 104.8415063509460055, -1.908493649053821795, 1.110223024625156540E-13 ) ) ;
#1774=CARTESIAN_POINT ( 'NONE',  ( 116.1252832217622881, -5.551115123125782702E-14, -1.849990392679412565 ) ) ;
#1776=ORIENTED_EDGE ( 'NONE', *, *, #20790, .T. ) ;
#1777=AXIS2_PLACEMENT_3D ( 'NONE', #6671, #27688, #16241 ) ;
#1791=CARTESIAN_POINT ( 'NONE',  ( 115.4999999999998153, -2.499999999999891198, 0.000000000000000000 ) ) ;
#1795=CARTESIAN_POINT ( 'NONE',  ( 106.0863248654050750, -1.414213562373090038, 1.414213562373145550 ) ) ;
#1803=CARTESIAN_POINT ( 'NONE',  ( 117.2499999999998721, 0.000000000000000000, 2.499999999999946709 ) ) ;
#1804=CARTESIAN_POINT ( 'NONE',  ( 111.5002832217621602, 1.308140751793723799, 1.308140751793640533 ) ) ;
#1805=CARTESIAN_POINT ( 'NONE',  ( 108.0863248654051603, -1.414213562373062283, 1.414213562373367594 ) ) ;
#1808=CARTESIAN_POINT ( 'NONE',  ( 108.8747167782374987, 0.000000000000000000, 1.849990392679523588 ) ) ;
#1834=CARTESIAN_POINT ( 'NONE',  ( 112.6877832217621034, -0.7662911109076184779, 1.849990392679652151 ) ) ;
#1835=AXIS2_PLACEMENT_3D ( 'NONE', #27414, #24668, #6086 ) ;
#1844=CARTESIAN_POINT ( 'NONE',  ( 104.7401757384972143, -1.604125865985250865, -0.9294237407942756990 ) ) ;
#1850=CARTESIAN_POINT ( 'NONE',  ( 109.5622167782374277, 1.849990392679501827, -0.7662911109077087390 ) ) ;
#1851=CARTESIAN_POINT ( 'NONE',  ( 112.1247167782376124, -1.849990392679579099, 1.110223024625156540E-13 ) ) ;
#1855=CARTESIAN_POINT ( 'NONE',  ( 110.3988248654048760, -0.8284271247461453269, -1.999999999999731104 ) ) ;
#1857=ORIENTED_EDGE ( 'NONE', *, *, #20790, .F. ) ;
#1865=CARTESIAN_POINT ( 'NONE',  ( 119.9999999999999289, 2.500000000000057732, 1.110223024625156540E-13 ) ) ;
#1875=CARTESIAN_POINT ( 'NONE',  ( 109.0624999999997584, 2.500000000000054623, 1.035533905932809473 ) ) ;
#1876=CARTESIAN_POINT ( 'NONE',  ( 106.7261751345945413, -1.999999999999941602, 0.8284271247462955401 ) ) ;
#1886=CARTESIAN_POINT ( 'NONE',  ( 106.4999999999999147, -2.499999999999946709, 1.110223024625156540E-13 ) ) ;
#1890=CARTESIAN_POINT ( 'NONE',  ( 108.2886751345946834, 2.000000000000057288, 2.220446049250313081E-13 ) ) ;
#1892=CARTESIAN_POINT ( 'NONE',  ( 119.6874999999998010, -1.035533905932809473, -2.499999999999784173 ) ) ;
#1903=CARTESIAN_POINT ( 'NONE',  ( 119.9999999999999574, -0.4876318259219858398, 1.939643060552387333 ) ) ;
#1905=CARTESIAN_POINT ( 'NONE',  ( 112.9761751345945981, -0.8284271247461153509, -1.999999999999610978 ) ) ;
#1907=CARTESIAN_POINT ( 'NONE',  ( 119.2502832217621886, 1.308140751793612777, -1.308140751793418488 ) ) ;
#1927=CARTESIAN_POINT ( 'NONE',  ( 116.4997167782376266, 1.308140751793640533, -1.308140751793640533 ) ) ;
#1934=ORIENTED_EDGE ( 'NONE', *, *, #2161, .T. ) ;
#1937=EDGE_CURVE ( 'NONE', #15812, #4583, #4725, .T. ) ;
#1943=CARTESIAN_POINT ( 'NONE',  ( 107.2886751345947118, 2.000000000000085265, 1.110223024625156540E-13 ) ) ;
#1955=CARTESIAN_POINT ( 'NONE',  ( 115.0624999999998153, 2.499999999999994671, 1.035533905932929599 ) ) ;
#1964=CARTESIAN_POINT ( 'NONE',  ( 116.7499999999997584, 1.665334536937734811E-13, -2.499999999999724665 ) ) ;
#1969=CARTESIAN_POINT ( 'NONE',  ( 110.0863248654050466, -1.414213562373090038, 1.414213562373256572 ) ) ;
#1973=ADVANCED_FACE ( 'NONE', ( #27029 ), #15723, .F. ) ;
#1985=CARTESIAN_POINT ( 'NONE',  ( 111.1011751345945413, 0.8284271247462654530, -1.999999999999851674 ) ) ;
#1986=CARTESIAN_POINT ( 'NONE',  ( 109.6011751345946266, -0.8284271247461453269, 2.000000000000212275 ) ) ;
#1989=CARTESIAN_POINT ( 'NONE',  ( 110.2502832217623165, 1.308140751793640533, -1.308140751793640533 ) ) ;
#1996=VECTOR ( 'NONE', #2689, 1000.000000000000000 ) ;
#2009=CARTESIAN_POINT ( 'NONE',  ( 110.4997167782375698, 1.308140751793668288, -1.308140751793640533 ) ) ;
#2011=CARTESIAN_POINT ( 'NONE',  ( 113.8122167782374987, 0.7662911109077987781, 1.849990392679652151 ) ) ;
#2021=AXIS2_PLACEMENT_3D ( 'NONE', #30364, #25131, #4096 ) ;
#2037=CARTESIAN_POINT ( 'NONE',  ( 111.3124999999998295, -1.035533905932629173, 2.500000000000325517 ) ) ;
#2041=CARTESIAN_POINT ( 'NONE',  ( 108.7113248654051176, 2.000000000000057288, 0.000000000000000000 ) ) ;
#2054=CARTESIAN_POINT ( 'NONE',  ( 105.6874999999997442, -1.035533905932659149, -2.499999999999724221 ) ) ;
#2060=CARTESIAN_POINT ( 'NONE',  ( 116.7886751345947687, -2.000000000000001776, 0.000000000000000000 ) ) ;
#2066=ORIENTED_EDGE ( 'NONE', *, *, #14089, .F. ) ;
#2073=CARTESIAN_POINT ( 'NONE',  ( 118.8127832217620465, -1.849990392679381701, 0.7662911109078287542 ) ) ;
#2089=CARTESIAN_POINT ( 'NONE',  ( 119.6247167782376124, 1.849990392679523588, 0.000000000000000000 ) ) ;
#2094=CARTESIAN_POINT ( 'NONE',  ( 114.4377832217621318, 1.849990392679562001, 0.7662911109079489913 ) ) ;
#2103=ADVANCED_FACE ( 'NONE', ( #18019 ), #13264, .F. ) ;
#2113=CARTESIAN_POINT ( 'NONE',  ( 111.6874999999997584, -1.035533905932719101, -2.499999999999844569 ) ) ;
#2118=EDGE_CURVE ( 'NONE', #4691, #13609, #19686, .T. ) ;
#2121=ORIENTED_EDGE ( 'NONE', *, *, #15780, .T. ) ;
#2123=CARTESIAN_POINT ( 'NONE',  ( 118.0624999999998010, 2.500000000000055067, 1.035533905932929599 ) ) ;
#2125=CARTESIAN_POINT ( 'NONE',  ( 106.5002832217622881, 1.308140751793696044, 1.308140751793640533 ) ) ;
#2129=CARTESIAN_POINT ( 'NONE',  ( 106.9372167782374703, -0.7662911109076785410, 1.849990392679772278 ) ) ;
#2130=EDGE_LOOP ( 'NONE', ( #2909, #12189, #895, #8535 ) ) ;
#2147=VERTEX_POINT ( 'NONE', #18317 ) ;
#2151=CARTESIAN_POINT ( 'NONE',  ( 112.3363248654049187, -1.414213562373173305, -1.414213562373034527 ) ) ;
#2152=CARTESIAN_POINT ( 'NONE',  ( 111.3127832217622171, 1.849990392679501827, -0.7662911109077087390 ) ) ;
#2161=EDGE_CURVE ( 'NONE', #1738, #24742, #13565, .T. ) ;
#2168=CARTESIAN_POINT ( 'NONE',  ( 108.8747167782374987, 0.000000000000000000, 1.849990392679523588 ) ) ;
#2170=CARTESIAN_POINT ( 'NONE',  ( 112.7497167782374845, 1.308140751793779311, 1.308140751793973600 ) ) ;
#2189=CARTESIAN_POINT ( 'NONE',  ( 109.3124999999999147, -1.035533905932598975, 2.500000000000265121 ) ) ;
#2190=CARTESIAN_POINT ( 'NONE',  ( 106.4136751345946692, 1.414213562373201061, 1.414213562373256572 ) ) ;
#2193=CARTESIAN_POINT ( 'NONE',  ( 114.9136751345945981, -1.414213562373201061, -1.414213562373034527 ) ) ;
#2203=CARTESIAN_POINT ( 'NONE',  ( 119.8122167782374277, 0.7662911109078588412, 1.849990392679712103 ) ) ;
#2219=( BOUNDED_CURVE ( )  B_SPLINE_CURVE ( 2, ( #12161, #21797, #23798, #5187, #28234, #7208, #7360, #21652, #16765 ),
 .UNSPECIFIED., .F., .T. ) 
 B_SPLINE_CURVE_WITH_KNOTS ( ( 3, 2, 2, 2, 3 ),
 ( 0.8529411764705882026, 0.8602941176470588758, 0.8676470588235294379, 0.8750000000000000000, 0.8823529411764705621 ),
 .UNSPECIFIED. ) 
 CURVE ( )  GEOMETRIC_REPRESENTATION_ITEM ( )  RATIONAL_B_SPLINE_CURVE ( ( 1.000000000000000000, 0.9238795325112867385, 1.000000000000000000, 0.9238795325112867385, 1.000000000000000000, 0.9238795325112867385, 1.000000000000000000, 0.9238795325112867385, 1.000000000000000000 ) ) 
 REPRESENTATION_ITEM ( '' )  );
#2221=CARTESIAN_POINT ( 'NONE',  ( 106.6872167782374277, 1.849990392679562001, 0.7662911109079489913 ) ) ;
#2222=CARTESIAN_POINT ( 'NONE',  ( 112.9136751345946976, -1.414213562373090038, -1.414213562373145550 ) ) ;
#2224=CARTESIAN_POINT ( 'NONE',  ( 121.0627832217620750, -0.7662911109076785410, -1.849990392679291551 ) ) ;
#2244=CYLINDRICAL_SURFACE ( 'NONE', #23221, 2.000000000000012879 ) ;
#2245=CARTESIAN_POINT ( 'NONE',  ( 117.7497167782374987, 1.308140751793723799, 1.308140751793640533 ) ) ;
#2249=CARTESIAN_POINT ( 'NONE',  ( 113.3752832217622881, 1.849990392679523588, 0.000000000000000000 ) ) ;
#2254=ORIENTED_EDGE ( 'NONE', *, *, #20352, .F. ) ;
#2266=( BOUNDED_CURVE ( )  B_SPLINE_CURVE ( 2, ( #9093, #18490, #27657, #18637, #20628, #9403, #14055, #27808, #11274 ),
 .UNSPECIFIED., .F., .F. ) 
 B_SPLINE_CURVE_WITH_KNOTS ( ( 3, 2, 2, 2, 3 ),
 ( 0.4117647058823529216, 0.4191176470588234837, 0.4264705882352941568, 0.4338235294117647189, 0.4411764705882352811 ),
 .UNSPECIFIED. ) 
 CURVE ( )  GEOMETRIC_REPRESENTATION_ITEM ( )  RATIONAL_B_SPLINE_CURVE ( ( 1.000000000000000000, 0.9238795325112867385, 1.000000000000000000, 0.9238795325112867385, 1.000000000000000000, 0.9238795325112867385, 1.000000000000000000, 0.9238795325112867385, 1.000000000000000000 ) ) 
 REPRESENTATION_ITEM ( '' )  );
#2267=CARTESIAN_POINT ( 'NONE',  ( 110.8749999999998721, 1.767766952966431937, -1.767766952966209892 ) ) ;
#2276=CARTESIAN_POINT ( 'NONE',  ( 111.9999999999999716, 2.500000000000002220, 0.000000000000000000 ) ) ;
#2279=CARTESIAN_POINT ( 'NONE',  ( 107.1877832217621886, 0.7662911109078588412, -1.849990392679231599 ) ) ;
#2280=CARTESIAN_POINT ( 'NONE',  ( 0.000000000000000000, 0.000000000000000000, 0.000000000000000000 ) ) ;
#2282=CARTESIAN_POINT ( 'NONE',  ( 0.000000000000000000, 0.000000000000000000, 0.000000000000000000 ) ) ;
#2284=CARTESIAN_POINT ( 'NONE',  ( 105.4372167782375413, 0.7662911109078888172, -1.849990392679291551 ) ) ;
#2297=CARTESIAN_POINT ( 'NONE',  ( 110.3749999999999289, -1.767766952966209892, 1.767766952966542959 ) ) ;
#2304=CARTESIAN_POINT ( 'NONE',  ( 112.4613248654051461, 0.000000000000000000, -2.000000000000001776 ) ) ;
#2305=CARTESIAN_POINT ( 'NONE',  ( 108.5002832217622313, 1.308140751793696044, 1.308140751793640533 ) ) ;
#2320=CARTESIAN_POINT ( 'NONE',  ( 110.2497167782375698, -1.308140751793585022, -1.308140751793529510 ) ) ;
#2332=AXIS2_PLACEMENT_3D ( 'NONE', #9625, #28338, #7457 ) ;
#2346=CARTESIAN_POINT ( 'NONE',  ( 110.8124999999999574, 1.035533905932719101, -2.499999999999904521 ) ) ;
#2354=EDGE_LOOP ( 'NONE', ( #6191, #27822, #18065, #3558 ) ) ;
#2355=CARTESIAN_POINT ( 'NONE',  ( 106.3749999999999574, -1.767766952966320915, 1.767766952966431937 ) ) ;
#2361=CARTESIAN_POINT ( 'NONE',  ( 119.1249999999999432, 1.767766952966348670, 1.767766952966431937 ) ) ;
#2368=CARTESIAN_POINT ( 'NONE',  ( 115.2738248654048760, -1.999999999999911626, -0.8284271247460553989 ) ) ;
#2370=CARTESIAN_POINT ( 'NONE',  ( 109.1636751345948113, 1.414213562373145550, -1.414213562372812483 ) ) ;
#2373=CARTESIAN_POINT ( 'NONE',  ( 106.2497167782374845, -1.308140751793585022, -1.308140751793640533 ) ) ;
#2375=CARTESIAN_POINT ( 'NONE',  ( 119.8127832217621460, -1.849990392679381701, 0.7662911109078287542 ) ) ;
#2386=CARTESIAN_POINT ( 'NONE',  ( 119.9553615878004393, -1.023503819640848800, -1.804923305105176290 ) ) ;
#2387=CARTESIAN_POINT ( 'NONE',  ( 118.3747167782375129, 0.000000000000000000, -1.849990392679301543 ) ) ;
#2392=CARTESIAN_POINT ( 'NONE',  ( 115.9377832217620323, -1.849990392679441875, -0.7662911109075283278 ) ) ;
#2413=CARTESIAN_POINT ( 'NONE',  ( 112.8124999999998579, 1.035533905932779275, -2.499999999999904521 ) ) ;
#2416=CARTESIAN_POINT ( 'NONE',  ( 115.4761751345947118, 0.8284271247462654530, 2.000000000000151879 ) ) ;
#2423=CARTESIAN_POINT ( 'NONE',  ( 113.6874999999998437, -1.035533905932749299, -2.499999999999904521 ) ) ;
#2425=ADVANCED_FACE ( 'NONE', ( #18922 ), #28244, .F. ) ;
#2432=CARTESIAN_POINT ( 'NONE',  ( 106.1247167782374987, -1.849990392679412565, 2.220446049250313081E-13 ) ) ;
#2446=CARTESIAN_POINT ( 'NONE',  ( 109.4374999999998721, -2.499999999999934719, 1.035533905932929599 ) ) ;
#2452=CARTESIAN_POINT ( 'NONE',  ( 106.3752832217622171, 1.849990392679523588, 0.000000000000000000 ) ) ;
#2454=DIRECTION ( 'NONE',  ( 5.551115123125785167E-17, -1.000000000000000000, -8.881784197001256268E-16 ) ) ;
#2465=STYLED_ITEM ( 'NONE', ( #15153 ), #14219 ) ;
#2466=CARTESIAN_POINT ( 'NONE',  ( 118.3363248654051176, -1.414213562373201061, -1.414213562373034527 ) ) ;
#2478=CARTESIAN_POINT ( 'NONE',  ( 117.2738248654048476, -1.999999999999911626, -0.8284271247460553989 ) ) ;
#2486=CARTESIAN_POINT ( 'NONE',  ( 109.8749999999998437, 1.767766952966320915, -1.767766952966209892 ) ) ;
#2493=CARTESIAN_POINT ( 'NONE',  ( 120.0622167782374419, -1.849990392679472073, 0.7662911109078888172 ) ) ;
#2501=EDGE_LOOP ( 'NONE', ( #3910, #381, #12584, #28216 ) ) ;
#2509=CARTESIAN_POINT ( 'NONE',  ( 107.3122167782375413, -0.7662911109077087390, -1.849990392679291551 ) ) ;
#2512=CARTESIAN_POINT ( 'NONE',  ( 118.3127832217620750, 1.849990392679532247, -0.7662911109075883909 ) ) ;
#2525=CARTESIAN_POINT ( 'NONE',  ( 108.7886751345946834, -1.999999999999946265, 1.110223024625156540E-13 ) ) ;
#2531=CYLINDRICAL_SURFACE ( 'NONE', #14609, 2.000000000000012879 ) ;
#2532=CARTESIAN_POINT ( 'NONE',  ( 118.4372167782374135, 0.7662911109079189043, -1.849990392679291551 ) ) ;
#2538=CARTESIAN_POINT ( 'NONE',  ( 114.0627832217621602, -0.7662911109077388261, -1.849990392679231599 ) ) ;
#2548=CARTESIAN_POINT ( 'NONE',  ( 0.000000000000000000, 0.000000000000000000, 0.000000000000000000 ) ) ;
#2553=CARTESIAN_POINT ( 'NONE',  ( 113.3749999999999289, -1.767766952966293159, 1.767766952966431937 ) ) ;
#2561=CARTESIAN_POINT ( 'NONE',  ( 107.1011751345945981, 0.8284271247463257382, -1.999999999999791278 ) ) ;
#2565=CARTESIAN_POINT ( 'NONE',  ( 111.4374999999997300, -2.499999999999904521, 1.035533905932869425 ) ) ;
#2567=CARTESIAN_POINT ( 'NONE',  ( 105.0002832217622029, -1.308140751793612777, -1.308140751793640533 ) ) ;
#2573=ORIENTED_EDGE ( 'NONE', *, *, #23425, .F. ) ;
#2583=CARTESIAN_POINT ( 'NONE',  ( 106.8124999999997016, 1.035533905932749299, -2.499999999999784173 ) ) ;
#2592=CARTESIAN_POINT ( 'NONE',  ( 109.0002832217621034, -1.308140751793640533, -1.308140751793640533 ) ) ;
#2594=CYLINDRICAL_SURFACE ( 'NONE', #849, 6.000000000000005329 ) ;
#2624=CARTESIAN_POINT ( 'NONE',  ( 117.2113248654051034, -1.999999999999890754, 3.330669073875469621E-13 ) ) ;
#2630=CARTESIAN_POINT ( 'NONE',  ( 107.2499999999999147, 0.000000000000000000, 2.499999999999946709 ) ) ;
#2639=CARTESIAN_POINT ( 'NONE',  ( 116.5622167782374135, 1.849990392679562001, -0.7662911109077087390 ) ) ;
#2645=CARTESIAN_POINT ( 'NONE',  ( 118.4999999999998437, -2.499999999999919176, 0.000000000000000000 ) ) ;
#2658=CARTESIAN_POINT ( 'NONE',  ( 117.1252832217621460, -5.551115123125782702E-14, -1.849990392679523588 ) ) ;
#2663=CARTESIAN_POINT ( 'NONE',  ( 105.6488248654050182, 2.000000000000061728, -0.8284271247459350507 ) ) ;
#2665=DIRECTION ( 'NONE',  ( -1.000000000000000000, -1.665334536937736783E-16, -2.220446049250315546E-16 ) ) ;
#2671=DIRECTION ( 'NONE',  ( 5.551115123125785167E-17, -1.000000000000000000, -8.881784197001256268E-16 ) ) ;
#2672=CARTESIAN_POINT ( 'NONE',  ( 115.1247167782376692, -1.849990392679523588, 0.000000000000000000 ) ) ;
#2676=CARTESIAN_POINT ( 'NONE',  ( 113.9377832217623450, -1.849990392679441875, -0.7662911109076485650 ) ) ;
#2677=EDGE_CURVE ( 'NONE', #17448, #20178, #12832, .T. ) ;
#2688=AXIS2_PLACEMENT_3D ( 'NONE', #28731, #7703, #26438 ) ;
#2689=DIRECTION ( 'NONE',  ( -1.000000000000000000, -1.665334536937736783E-16, -2.220446049250315546E-16 ) ) ;
#2697=CARTESIAN_POINT ( 'NONE',  ( 112.0624999999997868, 2.500000000000055067, 1.035533905932989551 ) ) ;
#2704=CARTESIAN_POINT ( 'NONE',  ( 112.4374999999998010, -2.499999999999934719, 1.035533905932989551 ) ) ;
#2711=CARTESIAN_POINT ( 'NONE',  ( 106.2497167782374845, -1.308140751793585022, -1.308140751793640533 ) ) ;
#2721=VERTEX_POINT ( 'NONE', #12353 ) ;
#2724=CARTESIAN_POINT ( 'NONE',  ( 109.9374999999996874, 2.500000000000114575, -1.035533905932448873 ) ) ;
#2726=ORIENTED_EDGE ( 'NONE', *, *, #46, .T. ) ;
#2729=CARTESIAN_POINT ( 'NONE',  ( 108.7502832217622881, -1.308140751793640533, 1.308140751793862577 ) ) ;
#2735=CARTESIAN_POINT ( 'NONE',  ( 0.000000000000000000, 0.000000000000000000, 0.000000000000000000 ) ) ;
#2736=( BOUNDED_CURVE ( )  B_SPLINE_CURVE ( 2, ( #9079, #27345, #27485, #1552, #11573, #1855, #30266, #27793, #8937 ),
 .UNSPECIFIED., .F., .T. ) 
 B_SPLINE_CURVE_WITH_KNOTS ( ( 3, 2, 2, 2, 3 ),
 ( 0.5882352941176470784, 0.5955882352941176405, 0.6029411764705882026, 0.6102941176470588758, 0.6176470588235294379 ),
 .UNSPECIFIED. ) 
 CURVE ( )  GEOMETRIC_REPRESENTATION_ITEM ( )  RATIONAL_B_SPLINE_CURVE ( ( 1.000000000000000000, 0.9238795325112867385, 1.000000000000000000, 0.9238795325112867385, 1.000000000000000000, 0.9238795325112867385, 1.000000000000000000, 0.9238795325112867385, 1.000000000000000000 ) ) 
 REPRESENTATION_ITEM ( '' )  );
#2747=( BOUNDED_CURVE ( )  B_SPLINE_CURVE ( 2, ( #12411, #24190, #2843, #12264, #539, #28779, #21606, #21755, #696 ),
 .UNSPECIFIED., .F., .T. ) 
 B_SPLINE_CURVE_WITH_KNOTS ( ( 3, 2, 2, 2, 3 ),
 ( 0.5294117647058823595, 0.5367647058823529216, 0.5441176470588234837, 0.5514705882352941568, 0.5588235294117647189 ),
 .UNSPECIFIED. ) 
 CURVE ( )  GEOMETRIC_REPRESENTATION_ITEM ( )  RATIONAL_B_SPLINE_CURVE ( ( 1.000000000000000000, 0.9238795325112867385, 1.000000000000000000, 0.9238795325112867385, 1.000000000000000000, 0.9238795325112867385, 1.000000000000000000, 0.9238795325112867385, 1.000000000000000000 ) ) 
 REPRESENTATION_ITEM ( '' )  );
#2750=CARTESIAN_POINT ( 'NONE',  ( 111.2886751345946834, 2.000000000000001776, 3.330669073875469621E-13 ) ) ;
#2776=CARTESIAN_POINT ( 'NONE',  ( 107.1874999999997584, 1.035533905932779275, 2.500000000000205169 ) ) ;
#2778=CARTESIAN_POINT ( 'NONE',  ( 104.7401757384976975, 1.138422607625655392, -1.478012502211212054 ) ) ;
#2784=AXIS2_PLACEMENT_3D ( 'NONE', #19725, #29071, #26756 ) ;
#2785=CARTESIAN_POINT ( 'NONE',  ( 117.5622167782373992, 1.849990392679562001, -0.7662911109076485650 ) ) ;
#2792=CARTESIAN_POINT ( 'NONE',  ( 118.4374999999998721, -2.499999999999964473, 1.035533905932929599 ) ) ;
#2797=CARTESIAN_POINT ( 'NONE',  ( 115.5238248654051176, 0.8284271247462955401, -1.999999999999851674 ) ) ;
#2800=CARTESIAN_POINT ( 'NONE',  ( 109.1011751345947687, 0.8284271247462955401, -1.999999999999911626 ) ) ;
#2803=VECTOR ( 'NONE', #6598, 1000.000000000000000 ) ;
#2805=CARTESIAN_POINT ( 'NONE',  ( 107.6247167782376124, 1.849990392679523588, 0.000000000000000000 ) ) ;
#2808=CARTESIAN_POINT ( 'NONE',  ( 115.1877832217620892, 0.7662911109078588412, -1.849990392679231599 ) ) ;
#2830=CARTESIAN_POINT ( 'NONE',  ( 112.6877832217621034, -0.7662911109076184779, 1.849990392679652151 ) ) ;
#2841=CARTESIAN_POINT ( 'NONE',  ( 111.1636751345946976, 1.414213562373145550, -1.414213562373145550 ) ) ;
#2843=CARTESIAN_POINT ( 'NONE',  ( 111.5863248654051887, 1.414213562373090038, -1.414213562373145550 ) ) ;
#2856=CARTESIAN_POINT ( 'NONE',  ( 107.0386751345946550, 5.551115123125782702E-14, -2.000000000000001776 ) ) ;
#2858=CARTESIAN_POINT ( 'NONE',  ( 114.9374999999997868, 2.500000000000055067, -1.035533905932629173 ) ) ;
#2865=CARTESIAN_POINT ( 'NONE',  ( 121.3752832217622881, 1.849990392679579099, 0.000000000000000000 ) ) ;
#2877=CARTESIAN_POINT ( 'NONE',  ( 107.5624999999998153, -2.499999999999874767, -1.035533905932629173 ) ) ;
#2885=CARTESIAN_POINT ( 'NONE',  ( 109.2502832217621602, 1.308140751793751555, -1.308140751793640533 ) ) ;
#2899=EDGE_CURVE ( 'NONE', #15450, #9582, #1401, .T. ) ;
#2900=EDGE_CURVE ( 'NONE', #12068, #17448, #1468, .T. ) ;
#2907=CARTESIAN_POINT ( 'NONE',  ( 1.110223024625164183E-16, -2.000000000000012879, -1.776356839400262692E-15 ) ) ;
#2909=ORIENTED_EDGE ( 'NONE', *, *, #2900, .F. ) ;
#2923=CARTESIAN_POINT ( 'NONE',  ( 105.0624999999998437, 2.500000000000054623, 1.035533905932869425 ) ) ;
#2924=ADVANCED_FACE ( 'NONE', ( #29583 ), #21847, .F. ) ;
#2930=CARTESIAN_POINT ( 'NONE',  ( 108.1011751345946692, 0.8284271247463257382, -1.999999999999731104 ) ) ;
#2933=CARTESIAN_POINT ( 'NONE',  ( 112.2886751345947118, 2.000000000000112799, 3.330669073875469621E-13 ) ) ;
#2935=CARTESIAN_POINT ( 'NONE',  ( 117.8747167782375840, 2.775557561562891351E-14, 1.849990392679523588 ) ) ;
#2940=CARTESIAN_POINT ( 'NONE',  ( 118.8124999999998579, 1.035533905932749299, -2.499999999999784173 ) ) ;
#2957=CARTESIAN_POINT ( 'NONE',  ( 115.9377832217620323, -1.849990392679441875, -0.7662911109075283278 ) ) ;
#2969=CARTESIAN_POINT ( 'NONE',  ( 1.110223024625164183E-16, -2.000000000000012879, -1.776356839400262692E-15 ) ) ;
#2974=DIRECTION ( 'NONE',  ( -1.000000000000000000, -1.665334536937736783E-16, -2.220446049250315546E-16 ) ) ;
#2986=CARTESIAN_POINT ( 'NONE',  ( 119.9999999999998153, 0.1805100831983324217, 2.088914846013814053 ) ) ;
#2990=DIRECTION ( 'NONE',  ( 5.551115123125785167E-17, -1.000000000000000000, -8.881784197001256268E-16 ) ) ;
#3003=CARTESIAN_POINT ( 'NONE',  ( 109.8749999999998437, 1.767766952966320915, -1.767766952966209892 ) ) ;
#3011=CIRCLE ( 'NONE', #10378, 5.999999999999999112 ) ;
#3012=CARTESIAN_POINT ( 'NONE',  ( 119.8752832217623450, -1.849990392679523588, 0.000000000000000000 ) ) ;
#3034=CARTESIAN_POINT ( 'NONE',  ( 119.0624999999998295, 2.500000000000024425, 1.035533905932809473 ) ) ;
#3046=CARTESIAN_POINT ( 'NONE',  ( 120.5624999999997442, -2.499999999999964473, -1.035533905932508825 ) ) ;
#3052=CARTESIAN_POINT ( 'NONE',  ( 115.7113248654050466, 2.000000000000112799, 0.000000000000000000 ) ) ;
#3080=MECHANICAL_DESIGN_GEOMETRIC_PRESENTATION_REPRESENTATION('',(#11964),#7020);
#3082=CARTESIAN_POINT ( 'NONE',  ( 119.5622167782373708, 1.849990392679621953, -0.7662911109075283278 ) ) ;
#3085=CARTESIAN_POINT ( 'NONE',  ( 112.4999999999999147, -2.499999999999835687, 0.000000000000000000 ) ) ;
#3102=CARTESIAN_POINT ( 'NONE',  ( 114.2502832217621602, 1.308140751793640533, -1.308140751793640533 ) ) ;
#3112=ORIENTED_EDGE ( 'NONE', *, *, #25964, .F. ) ;
#3118=CLOSED_SHELL ( 'NONE', ( #27297, #16480, #4324, #11762, #15815, #460, #22447, #20192, #29348, #11691, #20753, #3993, #7311, #18109, #15673, #23345, #23384, #9993, #10570, #2425, #6503, #4560, #19088, #11359, #2103, #23683, #10066, #7714, #3329, #6432, #15990, #1973, #11478, #2924, #10844, #28411, #17418, #1004, #9611, #18567, #27710, #16544, #5718, #26824, #13035 ) ) ;
#3119=CYLINDRICAL_SURFACE ( 'NONE', #17544, 2.000000000000012879 ) ;
#3120=CARTESIAN_POINT ( 'NONE',  ( 115.3747167782374987, -5.551115123125782702E-14, -1.849990392679523588 ) ) ;
#3128=ORIENTED_EDGE ( 'NONE', *, *, #13890, .F. ) ;
#3147=CARTESIAN_POINT ( 'NONE',  ( 109.4999999999998579, -2.499999999999891198, 2.220446049250313081E-13 ) ) ;
#3155=CARTESIAN_POINT ( 'NONE',  ( 104.1872167782373708, -1.849990392679351725, -0.7662911109074682647 ) ) ;
#3164=ORIENTED_EDGE ( 'NONE', *, *, #18341, .F. ) ;
#3165=CARTESIAN_POINT ( 'NONE',  ( 113.8363248654050892, 1.414213562373145550, 1.414213562373034527 ) ) ;
#3167=CARTESIAN_POINT ( 'NONE',  ( 105.1874999999998437, 1.035533905932749299, 2.500000000000265121 ) ) ;
#3177=CARTESIAN_POINT ( 'NONE',  ( 120.1874999999997016, 1.035533905932809473, 2.500000000000205169 ) ) ;
#3186=ORIENTED_EDGE ( 'NONE', *, *, #20352, .T. ) ;
#3188=CARTESIAN_POINT ( 'NONE',  ( 120.9999999999997300, 2.500000000000113243, 3.330669073875469621E-13 ) ) ;
#3209=DIRECTION ( 'NONE',  ( -1.000000000000000000, -1.665334536937736783E-16, -2.220446049250315546E-16 ) ) ;
#3213=CARTESIAN_POINT ( 'NONE',  ( 106.4374999999997442, -2.499999999999994671, 1.035533905932989551 ) ) ;
#3220=CARTESIAN_POINT ( 'NONE',  ( 1101.535898384862321, 1.665334536937736830E-13, 2.220446049250315605E-13 ) ) ;
#3221=CARTESIAN_POINT ( 'NONE',  ( 112.4136751345946692, 1.414213562373145550, 1.414213562373034527 ) ) ;
#3223=CARTESIAN_POINT ( 'NONE',  ( 113.8747167782375556, 0.000000000000000000, 1.849990392679523588 ) ) ;
#3226=AXIS2_PLACEMENT_3D ( 'NONE', #9017, #29737, #16279 ) ;
#3231=CARTESIAN_POINT ( 'NONE',  ( 115.6874999999997584, -1.035533905932719101, -2.499999999999844569 ) ) ;
#3241=CARTESIAN_POINT ( 'NONE',  ( 116.4613248654051034, 5.551115123125782702E-14, -2.000000000000001776 ) ) ;
#3262=CARTESIAN_POINT ( 'NONE',  ( 114.2497167782375698, -1.308140751793557266, -1.308140751793640533 ) ) ;
#3300=CARTESIAN_POINT ( 'NONE',  ( 104.9999999999999432, 2.775557561562891351E-14, 1.110223024625156540E-13 ) ) ;
#3324=CARTESIAN_POINT ( 'NONE',  ( 120.8124999999997726, 1.035533905932899401, -2.499999999999844569 ) ) ;
#3329=ADVANCED_FACE ( 'NONE', ( #7951 ), #29286, .F. ) ;
#3337=CARTESIAN_POINT ( 'NONE',  ( 119.5624999999998153, -2.499999999999874767, -1.035533905932629173 ) ) ;
#3364=CARTESIAN_POINT ( 'NONE',  ( 107.3988248654050182, -0.8284271247461153509, -1.999999999999791278 ) ) ;
#3374=CARTESIAN_POINT ( 'NONE',  ( 104.9087725016132140, -1.661713789967635524, -1.038312543894557294 ) ) ;
#3377=CARTESIAN_POINT ( 'NONE',  ( 112.9372167782374987, -0.7662911109076785410, 1.849990392679591977 ) ) ;
#3383=CARTESIAN_POINT ( 'NONE',  ( 114.4999999999998721, -2.499999999999891198, 0.000000000000000000 ) ) ;
#3386=ORIENTED_EDGE ( 'NONE', *, *, #15305, .T. ) ;
#3396=FACE_OUTER_BOUND ( 'NONE', #18441, .T. ) ;
#3404=CARTESIAN_POINT ( 'NONE',  ( 105.6011751345947260, -0.8284271247461453269, 2.000000000000212275 ) ) ;
#3425=CARTESIAN_POINT ( 'NONE',  ( 119.9999999999998579, 2.265773637426599318, 0.8226836970540328808 ) ) ;
#3443=CARTESIAN_POINT ( 'NONE',  ( 112.0238248654050608, -0.8284271247460852639, 2.000000000000332179 ) ) ;
#3449=CARTESIAN_POINT ( 'NONE',  ( 110.1011751345946692, 0.8284271247462654530, -1.999999999999851674 ) ) ;
#3450=CARTESIAN_POINT ( 'NONE',  ( 120.4377832217621176, 1.849990392679562001, 0.7662911109080692285 ) ) ;
#3462=CARTESIAN_POINT ( 'NONE',  ( 105.8124999999999574, 1.035533905932839449, -2.499999999999724221 ) ) ;
#3468=CARTESIAN_POINT ( 'NONE',  ( 116.0386751345946834, 5.551115123125782702E-14, -1.999999999999890754 ) ) ;
#3470=LINE ( 'NONE', #5626, #19221 ) ;
#3472=CARTESIAN_POINT ( 'NONE',  ( 105.2502832217622881, 1.308140751793668288, -1.308140751793640533 ) ) ;
#3480=CARTESIAN_POINT ( 'NONE',  ( 0.000000000000000000, 0.000000000000000000, 0.000000000000000000 ) ) ;
#3485=VERTEX_POINT ( 'NONE', #18724 ) ;
#3488=CARTESIAN_POINT ( 'NONE',  ( 118.9374999999996589, 2.500000000000234479, -1.035533905932568777 ) ) ;
#3509=DIRECTION ( 'NONE',  ( 1.665334536937739001E-16, -1.000000000000000000, -8.881784197001260212E-16 ) ) ;
#3530=CARTESIAN_POINT ( 'NONE',  ( 111.9372167782374703, -0.7662911109077388261, 1.849990392679652151 ) ) ;
#3536=CARTESIAN_POINT ( 'NONE',  ( 115.1249999999998863, 1.767766952966376426, 1.767766952966320915 ) ) ;
#3558=ORIENTED_EDGE ( 'NONE', *, *, #13066, .F. ) ;
#3567=CARTESIAN_POINT ( 'NONE',  ( 110.8122167782374987, 0.7662911109077388261, 1.849990392679772278 ) ) ;
#3572=ORIENTED_EDGE ( 'NONE', *, *, #29688, .T. ) ;
#3585=CARTESIAN_POINT ( 'NONE',  ( 106.3988248654049471, -0.8284271247462053900, -1.999999999999791278 ) ) ;
#3594=CARTESIAN_POINT ( 'NONE',  ( 104.3122167782373992, -0.7662911109076785410, -1.849990392679291551 ) ) ;
#3603=CARTESIAN_POINT ( 'NONE',  ( 120.4372167782375271, 0.7662911109078588412, -1.849990392679291551 ) ) ;
#3606=LINE ( 'NONE', #15340, #27311 ) ;
#3621=CARTESIAN_POINT ( 'NONE',  ( 115.9761751345946408, -0.8284271247461753029, -1.999999999999851674 ) ) ;
#3626=CARTESIAN_POINT ( 'NONE',  ( 118.8749999999998295, 1.767766952966320915, -1.767766952966320915 ) ) ;
#3640=CARTESIAN_POINT ( 'NONE',  ( 110.4377832217621034, 1.849990392679562001, 0.7662911109079489913 ) ) ;
#3644=CARTESIAN_POINT ( 'NONE',  ( 109.5622167782374277, 1.849990392679501827, -0.7662911109077087390 ) ) ;
#3649=CARTESIAN_POINT ( 'NONE',  ( 116.0238248654051034, -0.8284271247460852639, 2.000000000000212275 ) ) ;
#3650=ORIENTED_EDGE ( 'NONE', *, *, #4461, .F. ) ;
#3658=( NAMED_UNIT ( * ) SI_UNIT ( $, .STERADIAN. ) SOLID_ANGLE_UNIT ( ) );
#3667=CARTESIAN_POINT ( 'NONE',  ( 114.9377832217620750, -1.849990392679501827, -0.7662911109076485650 ) ) ;
#3670=CARTESIAN_POINT ( 'NONE',  ( 119.6488248654049755, 2.000000000000091926, -0.8284271247460553989 ) ) ;
#3673=CARTESIAN_POINT ( 'NONE',  ( 107.4613248654051176, 5.551115123125782702E-14, -1.999999999999890754 ) ) ;
#3684=CARTESIAN_POINT ( 'NONE',  ( 112.5622167782374703, 1.849990392679562001, -0.7662911109077087390 ) ) ;
#3690=CARTESIAN_POINT ( 'NONE',  ( 113.8749999999998721, 1.767766952966431937, -1.767766952966209892 ) ) ;
#3717=DIRECTION ( 'NONE',  ( -1.000000000000000000, -1.665334536937736783E-16, -2.220446049250315546E-16 ) ) ;
#3723=CARTESIAN_POINT ( 'NONE',  ( 109.3124999999999147, -1.035533905932598975, 2.500000000000265121 ) ) ;
#3730=VERTEX_POINT ( 'NONE', #4823 ) ;
#3734=ORIENTED_EDGE ( 'NONE', *, *, #29061, .F. ) ;
#3753=CARTESIAN_POINT ( 'NONE',  ( 104.6817643459960578, 1.849990392679531137, 0.6994407051579113466 ) ) ;
#3767=CARTESIAN_POINT ( 'NONE',  ( 117.5002832217622455, 1.308140751793696044, 1.308140751793862577 ) ) ;
#3770=AXIS2_PLACEMENT_3D ( 'NONE', #2548, #21754, #538 ) ;
#3775=EDGE_LOOP ( 'NONE', ( #15878, #21323, #16042, #5177 ) ) ;
#3785=CARTESIAN_POINT ( 'NONE',  ( 115.4374999999997868, -2.499999999999934719, 1.035533905932929599 ) ) ;
#3795=CARTESIAN_POINT ( 'NONE',  ( 117.5624999999997584, -2.499999999999904521, -1.035533905932508825 ) ) ;
#3797=CARTESIAN_POINT ( 'NONE',  ( 110.5627832217621318, 0.7662911109079189043, 1.849990392679652151 ) ) ;
#3823=CARTESIAN_POINT ( 'NONE',  ( 111.0002832217622597, -1.308140751793557266, -1.308140751793640533 ) ) ;
#3826=CARTESIAN_POINT ( 'NONE',  ( 119.3363248654050324, -1.414213562373228816, -1.414213562373034527 ) ) ;
#3828=CARTESIAN_POINT ( 'NONE',  ( 119.9999999999996447, 1.338994316733504109, -1.808804601859313133 ) ) ;
#3833=CARTESIAN_POINT ( 'NONE',  ( 104.7401757384972711, -1.469686010816039889, -1.130075799885433163 ) ) ;
#3840=CARTESIAN_POINT ( 'NONE',  ( 115.1247167782376692, -1.849990392679523588, 0.000000000000000000 ) ) ;
#3871=CARTESIAN_POINT ( 'NONE',  ( 110.6249999999998437, -1.767766952966376426, -1.767766952966320915 ) ) ;
#3873=CYLINDRICAL_SURFACE ( 'NONE', #24616, 2.000000000000012879 ) ;
#3901=AXIS2_PLACEMENT_3D ( 'NONE', #12409, #12858, #694 ) ;
#3904=CARTESIAN_POINT ( 'NONE',  ( 1.110223024625164183E-16, -2.000000000000012879, -1.776356839400262692E-15 ) ) ;
#3906=CARTESIAN_POINT ( 'NONE',  ( 114.5863248654051887, 1.414213562373145550, -1.414213562373145550 ) ) ;
#3910=ORIENTED_EDGE ( 'NONE', *, *, #19622, .F. ) ;
#3930=CARTESIAN_POINT ( 'NONE',  ( 116.8124999999998010, 1.035533905932719101, -2.499999999999784173 ) ) ;
#3937=EDGE_LOOP ( 'NONE', ( #2254, #7187, #22109 ) ) ;
#3939=CARTESIAN_POINT ( 'NONE',  ( 117.4999999999999574, -2.499999999999891198, 0.000000000000000000 ) ) ;
#3941=CARTESIAN_POINT ( 'NONE',  ( 111.1252832217622597, -5.551115123125782702E-14, -1.849990392679523588 ) ) ;
#3946=CARTESIAN_POINT ( 'NONE',  ( 108.9372167782374987, -0.7662911109077087390, 1.849990392679591977 ) ) ;
#3950=LINE ( 'NONE', #27150, #20502 ) ;
#3973=CARTESIAN_POINT ( 'NONE',  ( 112.6488248654049045, 2.000000000000061728, -0.8284271247459952248 ) ) ;
#3974=CARTESIAN_POINT ( 'NONE',  ( 113.1877832217620892, 0.7662911109079189043, -1.849990392679291551 ) ) ;
#3979=CARTESIAN_POINT ( 'NONE',  ( 119.9999999999998153, -0.1589013571467045582, -2.047736629971486977 ) ) ;
#3990=CARTESIAN_POINT ( 'NONE',  ( 109.1872167782375413, -1.849990392679441875, -0.7662911109077087390 ) ) ;
#3993=ADVANCED_FACE ( 'NONE', ( #29367 ), #5867, .F. ) ;
#4027=CARTESIAN_POINT ( 'NONE',  ( 108.3749999999998437, -1.767766952966209892, 1.767766952966431937 ) ) ;
#4035=SHAPE_REPRESENTATION ( 'Handle', ( #18805 ), #1104 ) ;
#4054=CARTESIAN_POINT ( 'NONE',  ( 104.2497167782374845, -1.308140751793640533, -1.308140751793640533 ) ) ;
#4061=CARTESIAN_POINT ( 'NONE',  ( 114.2738248654049045, -1.999999999999941602, -0.8284271247459350507 ) ) ;
#4068=ORIENTED_EDGE ( 'NONE', *, *, #27920, .F. ) ;
#4072=CARTESIAN_POINT ( 'NONE',  ( 118.5002832217622171, 1.308140751793723799, 1.308140751793862577 ) ) ;
#4092=CARTESIAN_POINT ( 'NONE',  ( 117.9374999999998721, 2.500000000000114575, -1.035533905932448873 ) ) ;
#4095=DIRECTION ( 'NONE',  ( -1.000000000000000000, -1.665334536937736783E-16, -2.220446049250315546E-16 ) ) ;
#4096=DIRECTION ( 'NONE',  ( 5.551115123125783935E-17, -1.000000000000000000, -8.881784197001254296E-16 ) ) ;
#4103=CARTESIAN_POINT ( 'NONE',  ( 117.0624999999998579, 2.500000000000234479, 1.035533905932989551 ) ) ;
#4104=CARTESIAN_POINT ( 'NONE',  ( 111.0627832217621602, -0.7662911109077987781, -1.849990392679291551 ) ) ;
#4105=CARTESIAN_POINT ( 'NONE',  ( 108.1488248654049755, -2.000000000000001776, 0.8284271247464157772 ) ) ;
#4118=ORIENTED_EDGE ( 'NONE', *, *, #26758, .T. ) ;
#4130=CARTESIAN_POINT ( 'NONE',  ( 111.4377832217621744, 1.849990392679532247, 0.7662911109078888172 ) ) ;
#4139=CARTESIAN_POINT ( 'NONE',  ( 104.7401757384972285, 0.4802581235374116519, -1.790660471610974636 ) ) ;
#4148=CARTESIAN_POINT ( 'NONE',  ( 107.9372167782375840, -0.7662911109077987781, 1.849990392679532247 ) ) ;
#4150=CARTESIAN_POINT ( 'NONE',  ( 113.2497167782375982, -1.308140751793585022, -1.308140751793640533 ) ) ;
#4188=CARTESIAN_POINT ( 'NONE',  ( 119.6872167782376408, 1.849990392679562001, 0.7662911109079489913 ) ) ;
#4192=CARTESIAN_POINT ( 'NONE',  ( 119.8749999999998863, 1.767766952966320915, -1.767766952966320915 ) ) ;
#4223=CARTESIAN_POINT ( 'NONE',  ( 117.9372167782374419, -0.7662911109077987781, 1.849990392679591977 ) ) ;
#4228=CARTESIAN_POINT ( 'NONE',  ( 118.7502832217622455, -1.308140751793529510, 1.308140751793640533 ) ) ;
#4242=CARTESIAN_POINT ( 'NONE',  ( 1.110223024625164183E-16, -2.000000000000012879, -1.776356839400262692E-15 ) ) ;
#4245=VECTOR ( 'NONE', #9431, 1000.000000000000000 ) ;
#4246=CARTESIAN_POINT ( 'NONE',  ( 117.6250000000000000, -1.767766952966376426, -1.767766952966320915 ) ) ;
#4249=EDGE_CURVE ( 'NONE', #23925, #25684, #5337, .T. ) ;
#4255=ORIENTED_EDGE ( 'NONE', *, *, #16710, .F. ) ;
#4257=CARTESIAN_POINT ( 'NONE',  ( 118.4999999999998437, -2.499999999999919176, 0.000000000000000000 ) ) ;
#4259=CARTESIAN_POINT ( 'NONE',  ( 111.5627832217621744, 0.7662911109078588412, 1.849990392679712103 ) ) ;
#4263=CARTESIAN_POINT ( 'NONE',  ( 107.9372167782375840, -0.7662911109077987781, 1.849990392679532247 ) ) ;
#4265=EDGE_LOOP ( 'NONE', ( #2573, #14572, #29950, #29119 ) ) ;
#4280=AXIS2_PLACEMENT_3D ( 'NONE', #12252, #2974, #23885 ) ;
#4290=CARTESIAN_POINT ( 'NONE',  ( 110.5627832217621318, 0.7662911109079189043, 1.849990392679652151 ) ) ;
#4296=AXIS2_PLACEMENT_3D ( 'NONE', #3300, #29098, #8058 ) ;
#4307=CARTESIAN_POINT ( 'NONE',  ( 108.8122167782374703, 0.7662911109077987781, 1.849990392679712103 ) ) ;
#4309=CARTESIAN_POINT ( 'NONE',  ( 113.9372167782373566, -0.7662911109077388261, 1.849990392679652151 ) ) ;
#4312=CARTESIAN_POINT ( 'NONE',  ( 104.7401757384975411, 1.651227484510909616, 0.8637895383429113894 ) ) ;
#4324=ADVANCED_FACE ( 'NONE', ( #11797 ), #2531, .F. ) ;
#4330=CARTESIAN_POINT ( 'NONE',  ( 110.3124999999999005, -1.035533905932659149, 2.500000000000144773 ) ) ;
#4333=LINE ( 'NONE', #25062, #16235 ) ;
#4343=EDGE_LOOP ( 'NONE', ( #26254, #10604, #6763 ) ) ;
#4352=( GEOMETRIC_REPRESENTATION_CONTEXT ( 3 ) GLOBAL_UNCERTAINTY_ASSIGNED_CONTEXT ( ( #15325 ) ) GLOBAL_UNIT_ASSIGNED_CONTEXT ( ( #20636, #6791, #22206 ) ) REPRESENTATION_CONTEXT ( 'NONE', 'WORKASPACE' ) );
#4353=CARTESIAN_POINT ( 'NONE',  ( 112.7113248654049897, 2.000000000000057288, 0.000000000000000000 ) ) ;
#4355=CARTESIAN_POINT ( 'NONE',  ( 119.5627832217620750, 0.7662911109078588412, 1.849990392679712103 ) ) ;
#4365=CARTESIAN_POINT ( 'NONE',  ( 116.8988248654051176, 0.8284271247462654530, 2.000000000000212275 ) ) ;
#4370=DIRECTION ( 'NONE',  ( -1.000000000000000000, -1.665334536937736783E-16, -2.220446049250315546E-16 ) ) ;
#4373=CARTESIAN_POINT ( 'NONE',  ( 117.8747167782375840, 2.775557561562891351E-14, 1.849990392679523588 ) ) ;
#4378=CARTESIAN_POINT ( 'NONE',  ( 115.6877832217621744, -0.7662911109077087390, 1.849990392679712103 ) ) ;
#4399=CARTESIAN_POINT ( 'NONE',  ( 115.1874999999998437, 1.035533905932719101, 2.500000000000265121 ) ) ;
#4409=CARTESIAN_POINT ( 'NONE',  ( 116.8749999999998863, 1.767766952966320915, -1.767766952966320915 ) ) ;
#4411=CARTESIAN_POINT ( 'NONE',  ( 107.5627832217621744, 0.7662911109077987781, 1.849990392679772278 ) ) ;
#4413=ORIENTED_EDGE ( 'NONE', *, *, #30050, .F. ) ;
#4415=CARTESIAN_POINT ( 'NONE',  ( 105.6247167782375271, 1.849990392679495832, 0.000000000000000000 ) ) ;
#4417=EDGE_CURVE ( 'NONE', #283, #29510, #24460, .T. ) ;
#4441=CARTESIAN_POINT ( 'NONE',  ( 112.2502832217622739, 1.308140751793640533, -1.308140751793640533 ) ) ;
#4457=CARTESIAN_POINT ( 'NONE',  ( 109.4997167782374845, 1.308140751793696044, -1.308140751793640533 ) ) ;
#4459=CARTESIAN_POINT ( 'NONE',  ( 112.1872167782374135, -1.849990392679411677, -0.7662911109075883909 ) ) ;
#4461=EDGE_CURVE ( 'NONE', #30108, #1220, #18940, .T. ) ;
#4469=AXIS2_PLACEMENT_3D ( 'NONE', #18296, #27610, #6587 ) ;
#4484=CARTESIAN_POINT ( 'NONE',  ( 110.2499999999998010, -5.551115123125782702E-14, 2.500000000000168754 ) ) ;
#4496=CARTESIAN_POINT ( 'NONE',  ( 120.1872167782373992, -1.849990392679441875, -0.7662911109076485650 ) ) ;
#4512=CARTESIAN_POINT ( 'NONE',  ( 119.9800011666190755, -0.2475512722491883533, 2.000000000000047073 ) ) ;
#4514=CARTESIAN_POINT ( 'NONE',  ( 104.8122167782375129, 0.7662911109077388261, 1.849990392679712103 ) ) ;
#4517=CARTESIAN_POINT ( 'NONE',  ( 120.0002832217621886, -1.308140751793557266, -1.308140751793529510 ) ) ;
#4539=CARTESIAN_POINT ( 'NONE',  ( 116.0627832217622029, -0.7662911109076785410, -1.849990392679291551 ) ) ;
#4559=CARTESIAN_POINT ( 'NONE',  ( 112.1874999999998295, 1.035533905932719101, 2.500000000000205169 ) ) ;
#4560=ADVANCED_FACE ( 'NONE', ( #12541 ), #3119, .F. ) ;
#4568=CARTESIAN_POINT ( 'NONE',  ( 114.7499999999999147, -5.551115123125782702E-14, -2.499999999999946709 ) ) ;
#4570=CARTESIAN_POINT ( 'NONE',  ( 105.1252832217623023, -5.551115123125782702E-14, -1.849990392679523588 ) ) ;
#4573=VERTEX_POINT ( 'NONE', #13606 ) ;
#4574=FACE_OUTER_BOUND ( 'NONE', #29910, .T. ) ;
#4583=VERTEX_POINT ( 'NONE', #1890 ) ;
#4586=CARTESIAN_POINT ( 'NONE',  ( 108.9999999999998579, 2.500000000000030198, 1.110223024625156540E-13 ) ) ;
#4592=CARTESIAN_POINT ( 'NONE',  ( 109.4377832217621460, 1.849990392679562001, 0.7662911109080692285 ) ) ;
#4599=CARTESIAN_POINT ( 'NONE',  ( 114.4136751345946976, 1.414213562373145550, 1.414213562373034527 ) ) ;
#4607=CARTESIAN_POINT ( 'NONE',  ( 110.6872167782375840, 1.849990392679562001, 0.7662911109078287542 ) ) ;
#4608=CARTESIAN_POINT ( 'NONE',  ( 118.5238248654050608, 0.8284271247463257382, -1.999999999999911626 ) ) ;
#4614=CARTESIAN_POINT ( 'NONE',  ( 106.2261751345945129, 2.000000000000122125, -0.8284271247460553989 ) ) ;
#4628=CARTESIAN_POINT ( 'NONE',  ( 108.3749999999998437, -1.767766952966209892, 1.767766952966431937 ) ) ;
#4641=CARTESIAN_POINT ( 'NONE',  ( 106.4374999999997442, -2.499999999999994671, 1.035533905932989551 ) ) ;
#4657=CARTESIAN_POINT ( 'NONE',  ( 114.2113248654050750, -1.999999999999890754, 0.000000000000000000 ) ) ;
#4658=CARTESIAN_POINT ( 'NONE',  ( 106.8747167782375840, 2.775557561562891351E-14, 1.849990392679745632 ) ) ;
#4662=CARTESIAN_POINT ( 'NONE',  ( 118.6252832217622029, 5.551115123125782702E-14, 1.849990392679634610 ) ) ;
#4679=CARTESIAN_POINT ( 'NONE',  ( 118.8747167782375840, 5.551115123125782702E-14, 1.849990392679523588 ) ) ;
#4683=CARTESIAN_POINT ( 'NONE',  ( 113.6252832217621460, 1.665334536937734811E-13, 1.849990392679745632 ) ) ;
#4691=VERTEX_POINT ( 'NONE', #1584 ) ;
#4703=CARTESIAN_POINT ( 'NONE',  ( 112.9374999999997868, 2.500000000000114575, -1.035533905932448873 ) ) ;
#4713=CARTESIAN_POINT ( 'NONE',  ( 111.9374999999997868, 2.500000000000114575, -1.035533905932508825 ) ) ;
#4715=CARTESIAN_POINT ( 'NONE',  ( 104.8752832217621602, -1.849990392679495832, 2.220446049250313081E-13 ) ) ;
#4717=( BOUNDED_CURVE ( )  B_SPLINE_CURVE ( 2, ( #14421, #5136, #23202, #23046, #28491, #1985, #2841, #30240, #24043 ),
 .UNSPECIFIED., .F., .T. ) 
 B_SPLINE_CURVE_WITH_KNOTS ( ( 3, 2, 2, 2, 3 ),
 ( 0.3529411764705882026, 0.3602941176470587648, 0.3676470588235294379, 0.3750000000000000000, 0.3823529411764705621 ),
 .UNSPECIFIED. ) 
 CURVE ( )  GEOMETRIC_REPRESENTATION_ITEM ( )  RATIONAL_B_SPLINE_CURVE ( ( 1.000000000000000000, 0.9238795325112867385, 1.000000000000000000, 0.9238795325112867385, 1.000000000000000000, 0.9238795325112867385, 1.000000000000000000, 0.9238795325112867385, 1.000000000000000000 ) ) 
 REPRESENTATION_ITEM ( '' )  );
#4721=CARTESIAN_POINT ( 'NONE',  ( 105.2497167782374845, -1.308140751793585022, -1.308140751793640533 ) ) ;
#4725=( BOUNDED_CURVE ( )  B_SPLINE_CURVE ( 2, ( #28572, #16951, #26279, #23987, #14787, #2930, #10018, #19397, #28719 ),
 .UNSPECIFIED., .F., .T. ) 
 B_SPLINE_CURVE_WITH_KNOTS ( ( 3, 2, 2, 2, 3 ),
 ( 0.1764705882352941568, 0.1838235294117647189, 0.1911764705882352811, 0.1985294117647058432, 0.2058823529411765163 ),
 .UNSPECIFIED. ) 
 CURVE ( )  GEOMETRIC_REPRESENTATION_ITEM ( )  RATIONAL_B_SPLINE_CURVE ( ( 1.000000000000000000, 0.9238795325112867385, 1.000000000000000000, 0.9238795325112867385, 1.000000000000000000, 0.9238795325112867385, 1.000000000000000000, 0.9238795325112867385, 1.000000000000000000 ) ) 
 REPRESENTATION_ITEM ( '' )  );
#4728=VERTEX_POINT ( 'NONE', #7106 ) ;
#4733=ORIENTED_EDGE ( 'NONE', *, *, #6608, .T. ) ;
#4736=CARTESIAN_POINT ( 'NONE',  ( 108.4374999999998863, -2.499999999999934719, 1.035533905932929599 ) ) ;
#4745=CARTESIAN_POINT ( 'NONE',  ( 106.5002832217622881, 1.308140751793696044, 1.308140751793640533 ) ) ;
#4748=CYLINDRICAL_SURFACE ( 'NONE', #17264, 2.000000000000012879 ) ;
#4756=CARTESIAN_POINT ( 'NONE',  ( 116.7261751345945981, -1.999999999999911626, 0.8284271247463557142 ) ) ;
#4785=CARTESIAN_POINT ( 'NONE',  ( 110.9999999999999147, 2.500000000000057732, 0.000000000000000000 ) ) ;
#4791=CARTESIAN_POINT ( 'NONE',  ( 120.3122167782375413, -0.7662911109077686911, -1.849990392679411677 ) ) ;
#4797=CARTESIAN_POINT ( 'NONE',  ( 116.3749999999998579, -1.767766952966209892, 1.767766952966542959 ) ) ;
#4810=CARTESIAN_POINT ( 'NONE',  ( 119.8363248654050039, 1.414213562373201061, 1.414213562373367594 ) ) ;
#4811=CARTESIAN_POINT ( 'NONE',  ( 105.5622167782374419, 1.849990392679591977, -0.7662911109075883909 ) ) ;
#4814=CARTESIAN_POINT ( 'NONE',  ( 120.1877832217620750, 0.7662911109077987781, -1.849990392679532247 ) ) ;
#4817=DIRECTION ( 'NONE',  ( 1.000000000000000000, 5.551115123125765446E-17, 2.220446049250314560E-16 ) ) ;
#4823=CARTESIAN_POINT ( 'NONE',  ( 115.7886751345947118, -1.999999999999974021, 0.000000000000000000 ) ) ;
#4830=CARTESIAN_POINT ( 'NONE',  ( 119.9136751345946266, -1.414213562373228816, -1.414213562373034527 ) ) ;
#4831=CARTESIAN_POINT ( 'NONE',  ( 117.3747167782375271, 0.000000000000000000, -1.849990392679301543 ) ) ;
#4833=ORIENTED_EDGE ( 'NONE', *, *, #17918, .F. ) ;
#4835=CARTESIAN_POINT ( 'NONE',  ( 115.4377832217621744, 1.849990392679591977, 0.7662911109078888172 ) ) ;
#4841=ORIENTED_EDGE ( 'NONE', *, *, #2677, .T. ) ;
#4850=CARTESIAN_POINT ( 'NONE',  ( 113.8124999999998437, 1.035533905932749299, -2.499999999999904521 ) ) ;
#4861=CARTESIAN_POINT ( 'NONE',  ( 111.8124999999997584, 1.035533905932779275, -2.499999999999964473 ) ) ;
#4863=CARTESIAN_POINT ( 'NONE',  ( 105.9377832217620323, -1.849990392679441875, -0.7662911109074682647 ) ) ;
#4864=DIRECTION ( 'NONE',  ( -1.000000000000000000, -1.665334536937736783E-16, -2.220446049250315546E-16 ) ) ;
#4879=CARTESIAN_POINT ( 'NONE',  ( 107.8749999999999858, 1.767766952966431937, -1.767766952966209892 ) ) ;
#4885=CARTESIAN_POINT ( 'NONE',  ( 108.8127832217621176, -1.849990392679501827, 0.7662911109078287542 ) ) ;
#4890=( BOUNDED_CURVE ( )  B_SPLINE_CURVE ( 2, ( #14281, #10092, #21311, #2416, #19315, #9939, #28195, #24051, #19462 ),
 .UNSPECIFIED., .F., .T. ) 
 B_SPLINE_CURVE_WITH_KNOTS ( ( 3, 2, 2, 2, 3 ),
 ( 0.6176470588235294379, 0.6250000000000000000, 0.6323529411764705621, 0.6397058823529411242, 0.6470588235294116863 ),
 .UNSPECIFIED. ) 
 CURVE ( )  GEOMETRIC_REPRESENTATION_ITEM ( )  RATIONAL_B_SPLINE_CURVE ( ( 1.000000000000000000, 0.9238795325112867385, 1.000000000000000000, 0.9238795325112867385, 1.000000000000000000, 0.9238795325112867385, 1.000000000000000000, 0.9238795325112867385, 1.000000000000000000 ) ) 
 REPRESENTATION_ITEM ( '' )  );
#4899=CARTESIAN_POINT ( 'NONE',  ( 116.6636751345947829, -1.414213562373090038, 1.414213562373256572 ) ) ;
#4910=CARTESIAN_POINT ( 'NONE',  ( 106.2886751345948255, 2.000000000000029310, 1.110223024625156540E-13 ) ) ;
#4917=CARTESIAN_POINT ( 'NONE',  ( 117.6636751345947545, -1.414213562373034527, 1.414213562373367594 ) ) ;
#4925=CARTESIAN_POINT ( 'NONE',  ( 110.5624999999998295, -2.499999999999994671, -1.035533905932568999 ) ) ;
#4936=CARTESIAN_POINT ( 'NONE',  ( 116.8747167782375556, 0.000000000000000000, 1.849990392679523588 ) ) ;
#4943=CARTESIAN_POINT ( 'NONE',  ( 116.2499999999998437, 5.551115123125782702E-14, 2.500000000000168754 ) ) ;
#4945=ORIENTED_EDGE ( 'NONE', *, *, #7767, .T. ) ;
#4946=CARTESIAN_POINT ( 'NONE',  ( 115.3988248654050182, -0.8284271247460852639, -1.999999999999791278 ) ) ;
#4949=CARTESIAN_POINT ( 'NONE',  ( 109.2886751345947971, 2.000000000000057288, 1.110223024625156540E-13 ) ) ;
#4952=CARTESIAN_POINT ( 'NONE',  ( 107.4372167782373850, 0.7662911109078287542, -1.849990392679351725 ) ) ;
#4956=CARTESIAN_POINT ( 'NONE',  ( 113.6877832217621460, -0.7662911109077987781, 1.849990392679591977 ) ) ;
#4962=CARTESIAN_POINT ( 'NONE',  ( 105.7113248654051461, 2.000000000000057288, 0.000000000000000000 ) ) ;
#4973=CARTESIAN_POINT ( 'NONE',  ( 115.8747167782375840, 0.000000000000000000, 1.849990392679523588 ) ) ;
#4977=CARTESIAN_POINT ( 'NONE',  ( 119.1636751345946834, 1.414213562373145550, -1.414213562373145550 ) ) ;
#4978=CARTESIAN_POINT ( 'NONE',  ( 115.0627832217623592, -0.7662911109076785410, -1.849990392679171425 ) ) ;
#4981=( BOUNDED_CURVE ( )  B_SPLINE_CURVE ( 2, ( #20451, #29810, #8788, #12187, #21373, #12032, #16492, #4614, #4910 ),
 .UNSPECIFIED., .F., .T. ) 
 B_SPLINE_CURVE_WITH_KNOTS ( ( 3, 2, 2, 2, 3 ),
 ( 0.05882352941176471894, 0.06617647058823528106, 0.07352941176470584317, 0.08088235294117651630, 0.08823529411764707842 ),
 .UNSPECIFIED. ) 
 CURVE ( )  GEOMETRIC_REPRESENTATION_ITEM ( )  RATIONAL_B_SPLINE_CURVE ( ( 1.000000000000000000, 0.9238795325112867385, 1.000000000000000000, 0.9238795325112867385, 1.000000000000000000, 0.9238795325112867385, 1.000000000000000000, 0.9238795325112867385, 1.000000000000000000 ) ) 
 REPRESENTATION_ITEM ( '' )  );
#4996=CARTESIAN_POINT ( 'NONE',  ( 112.1249999999998437, 1.767766952966293159, 1.767766952966431937 ) ) ;
#5002=CARTESIAN_POINT ( 'NONE',  ( 109.5863248654051603, 1.414213562373201061, -1.414213562373145550 ) ) ;
#5006=CARTESIAN_POINT ( 'NONE',  ( 113.5624999999997158, -2.499999999999964473, -1.035533905932689347 ) ) ;
#5008=CARTESIAN_POINT ( 'NONE',  ( 106.0627832217622455, -0.7662911109077388261, -1.849990392679351725 ) ) ;
#5013=CARTESIAN_POINT ( 'NONE',  ( 107.4997167782375982, 1.308140751793723799, -1.308140751793640533 ) ) ;
#5014=ORIENTED_EDGE ( 'NONE', *, *, #9803, .F. ) ;
#5020=ORIENTED_EDGE ( 'NONE', *, *, #14294, .T. ) ;
#5023=CARTESIAN_POINT ( 'NONE',  ( 106.4374999999997442, -2.499999999999994671, 1.035533905932989551 ) ) ;
#5029=CARTESIAN_POINT ( 'NONE',  ( 106.1877832217621318, 0.7662911109077987781, -1.849990392679351725 ) ) ;
#5049=CARTESIAN_POINT ( 'NONE',  ( 110.3122167782374419, -0.7662911109077388261, -1.849990392679411677 ) ) ;
#5074=CARTESIAN_POINT ( 'NONE',  ( 105.1874999999998437, 1.035533905932749299, 2.500000000000265121 ) ) ;
#5082=CARTESIAN_POINT ( 'NONE',  ( 115.8747167782375840, 0.000000000000000000, 1.849990392679523588 ) ) ;
#5086=CARTESIAN_POINT ( 'NONE',  ( 118.6249999999998010, -1.767766952966431937, -1.767766952966209892 ) ) ;
#5095=CARTESIAN_POINT ( 'NONE',  ( 119.9999999999998721, -0.4876318259425804769, -1.939643060543838615 ) ) ;
#5097=PRODUCT_DEFINITION_CONTEXT ( 'detailed design', #7328, 'design' ) ;
#5100=CARTESIAN_POINT ( 'NONE',  ( 105.4372167782375413, 0.7662911109078888172, -1.849990392679291551 ) ) ;
#5103=CARTESIAN_POINT ( 'NONE',  ( 114.6877832217621318, -0.7662911109077987781, 1.849990392679591977 ) ) ;
#5116=CARTESIAN_POINT ( 'NONE',  ( 108.2886751345946834, 2.000000000000057288, 2.220446049250313081E-13 ) ) ;
#5121=CARTESIAN_POINT ( 'NONE',  ( 112.6252832217622597, 1.665334536937734811E-13, 1.849990392679745632 ) ) ;
#5124=CARTESIAN_POINT ( 'NONE',  ( 104.7623688579944741, 1.279647136099528737, 1.365257574501548721 ) ) ;
#5133=ORIENTED_EDGE ( 'NONE', *, *, #12364, .F. ) ;
#5136=CARTESIAN_POINT ( 'NONE',  ( 110.8511751345946692, -1.999999999999911626, -0.8284271247459952248 ) ) ;
#5138=PLANE ( 'NONE',  #19141 ) ;
#5145=CARTESIAN_POINT ( 'NONE',  ( 113.7499999999997584, 0.000000000000000000, -2.500000000000057732 ) ) ;
#5148=DIRECTION ( 'NONE',  ( -2.498001805406611091E-16, 8.049116928532385904E-16, -1.000000000000000000 ) ) ;
#5152=CARTESIAN_POINT ( 'NONE',  ( 109.4613248654051745, 0.000000000000000000, -2.000000000000001776 ) ) ;
#5154=CARTESIAN_POINT ( 'NONE',  ( 113.7499999999997584, 0.000000000000000000, -2.500000000000057732 ) ) ;
#5162=CARTESIAN_POINT ( 'NONE',  ( 119.3127832217621034, 1.849990392679501827, -0.7662911109077087390 ) ) ;
#5163=ORIENTED_EDGE ( 'NONE', *, *, #12036, .T. ) ;
#5174=CARTESIAN_POINT ( 'NONE',  ( 109.9999999999999432, 2.500000000000030198, 0.000000000000000000 ) ) ;
#5177=ORIENTED_EDGE ( 'NONE', *, *, #26758, .F. ) ;
#5183=CARTESIAN_POINT ( 'NONE',  ( 108.9377832217621886, -1.849990392679411677, -0.7662911109076485650 ) ) ;
#5187=CARTESIAN_POINT ( 'NONE',  ( 119.4761751345946834, 0.8284271247463257382, 2.000000000000212275 ) ) ;
#5223=CARTESIAN_POINT ( 'NONE',  ( 108.7738248654050182, 2.000000000000031530, 0.8284271247463557142 ) ) ;
#5224=CARTESIAN_POINT ( 'NONE',  ( 104.4999999999998863, -2.499999999999919176, 0.000000000000000000 ) ) ;
#5233=CARTESIAN_POINT ( 'NONE',  ( 117.3122167782375840, -0.7662911109077388261, -1.849990392679351725 ) ) ;
#5239=CARTESIAN_POINT ( 'NONE',  ( 119.4374999999997868, -2.499999999999994671, 1.035533905932809473 ) ) ;
#5245=( BOUNDED_CURVE ( )  B_SPLINE_CURVE ( 2, ( #28421, #7537, #2193, #18648, #27966, #6942, #9563, #16361, #16659 ),
 .UNSPECIFIED., .F., .T. ) 
 B_SPLINE_CURVE_WITH_KNOTS ( ( 3, 2, 2, 2, 3 ),
 ( 0.5882352941176470784, 0.5955882352941176405, 0.6029411764705882026, 0.6102941176470588758, 0.6176470588235294379 ),
 .UNSPECIFIED. ) 
 CURVE ( )  GEOMETRIC_REPRESENTATION_ITEM ( )  RATIONAL_B_SPLINE_CURVE ( ( 1.000000000000000000, 0.9238795325112867385, 1.000000000000000000, 0.9238795325112867385, 1.000000000000000000, 0.9238795325112867385, 1.000000000000000000, 0.9238795325112867385, 1.000000000000000000 ) ) 
 REPRESENTATION_ITEM ( '' )  );
#5248=CARTESIAN_POINT ( 'NONE',  ( 115.2113248654050750, -1.999999999999918510, 1.110223024625156540E-13 ) ) ;
#5251=CARTESIAN_POINT ( 'NONE',  ( 109.0386751345947118, 0.000000000000000000, -2.000000000000001776 ) ) ;
#5259=CARTESIAN_POINT ( 'NONE',  ( 113.3752832217622881, 1.849990392679523588, 0.000000000000000000 ) ) ;
#5271=EDGE_CURVE ( 'NONE', #15734, #30347, #3950, .T. ) ;
#5273=CARTESIAN_POINT ( 'NONE',  ( 114.9997167782375698, -1.308140751793612777, 1.308140751793862577 ) ) ;
#5285=CARTESIAN_POINT ( 'NONE',  ( 120.0000000000000568, 1.621546429797428024, 1.617766924401469186 ) ) ;
#5292=CARTESIAN_POINT ( 'NONE',  ( 117.2261751345945697, 2.000000000000061728, -0.8284271247459952248 ) ) ;
#5302=CARTESIAN_POINT ( 'NONE',  ( 109.9374999999996874, 2.500000000000114575, -1.035533905932448873 ) ) ;
#5309=CARTESIAN_POINT ( 'NONE',  ( 104.9997167782376692, -1.308140751793585022, 1.308140751793640533 ) ) ;
#5329=CARTESIAN_POINT ( 'NONE',  ( 120.4374999999997442, -2.499999999999964473, 1.035533905932989551 ) ) ;
#5332=CARTESIAN_POINT ( 'NONE',  ( 113.2886751345947118, 1.999999999999946265, 1.110223024625156540E-13 ) ) ;
#5337=( BOUNDED_CURVE ( )  B_SPLINE_CURVE ( 2, ( #25876, #18694, #4830, #2386, #27867 ),
 .UNSPECIFIED., .F., .T. ) 
 B_SPLINE_CURVE_WITH_KNOTS ( ( 3, 2, 3 ),
 ( 0.8823529411764705621, 0.8897058823529411242, 0.8947377251129212672 ),
 .UNSPECIFIED. ) 
 CURVE ( )  GEOMETRIC_REPRESENTATION_ITEM ( )  RATIONAL_B_SPLINE_CURVE ( ( 1.000000000000000000, 0.9238795325112867385, 1.000000000000000000, 0.9479084336421641499, 0.9671125746054942685 ) ) 
 REPRESENTATION_ITEM ( '' )  );
#5372=CARTESIAN_POINT ( 'NONE',  ( 105.8124999999999574, 1.035533905932839227, -2.499999999999724221 ) ) ;
#5373=CIRCLE ( 'NONE', #29420, 5.999999999999998224 ) ;
#5385=CARTESIAN_POINT ( 'NONE',  ( 117.1872167782373708, -1.849990392679441875, -0.7662911109077087390 ) ) ;
#5386=CARTESIAN_POINT ( 'NONE',  ( 118.4761751345946692, 0.8284271247463257382, 2.000000000000151879 ) ) ;
#5391=CARTESIAN_POINT ( 'NONE',  ( 116.4374999999997726, -2.499999999999934719, 1.035533905932929599 ) ) ;
#5393=STYLED_ITEM ( 'NONE', ( #21823 ), #27297 ) ;
#5396=ORIENTED_EDGE ( 'NONE', *, *, #19432, .T. ) ;
#5404=CARTESIAN_POINT ( 'NONE',  ( 116.1252832217622881, -5.551115123125782702E-14, -1.849990392679412565 ) ) ;
#5445=EDGE_CURVE ( 'NONE', #10146, #13609, #12684, .T. ) ;
#5449=CARTESIAN_POINT ( 'NONE',  ( 108.9374999999997442, 2.500000000000114575, -1.035533905932508825 ) ) ;
#5457=CARTESIAN_POINT ( 'NONE',  ( 110.2261751345946124, 2.000000000000122125, -0.8284271247459350507 ) ) ;
#5458=CARTESIAN_POINT ( 'NONE',  ( 120.8752832217622029, -1.849990392679523588, 0.000000000000000000 ) ) ;
#5466=CARTESIAN_POINT ( 'NONE',  ( 114.1488248654049187, -1.999999999999941602, 0.8284271247462955401 ) ) ;
#5468=CARTESIAN_POINT ( 'NONE',  ( 104.9999999999998579, 2.500000000000002220, 0.000000000000000000 ) ) ;
#5479=CARTESIAN_POINT ( 'NONE',  ( 119.9999999999999289, 2.500000000000057732, 1.110223024625156540E-13 ) ) ;
#5491=CARTESIAN_POINT ( 'NONE',  ( 120.6249999999998295, -1.767766952966376426, -1.767766952966320915 ) ) ;
#5508=EDGE_CURVE ( 'NONE', #9582, #11212, #21625, .T. ) ;
#5519=CARTESIAN_POINT ( 'NONE',  ( 108.1249999999999574, 1.767766952966293159, 1.767766952966431937 ) ) ;
#5520=CARTESIAN_POINT ( 'NONE',  ( 107.2738248654051176, -1.999999999999941602, -0.8284271247460553989 ) ) ;
#5532=CARTESIAN_POINT ( 'NONE',  ( 116.8122167782373992, 0.7662911109079189043, 1.849990392679652151 ) ) ;
#5537=CARTESIAN_POINT ( 'NONE',  ( 104.9999999999999716, -0.4876318259226519736, 1.939643060552054266 ) ) ;
#5538=CARTESIAN_POINT ( 'NONE',  ( 114.3124999999997726, -1.035533905932719101, 2.500000000000205169 ) ) ;
#5540=ORIENTED_EDGE ( 'NONE', *, *, #642, .F. ) ;
#5541=FACE_OUTER_BOUND ( 'NONE', #5801, .T. ) ;
#5547=LINE ( 'NONE', #13130, #7321 ) ;
#5550=CARTESIAN_POINT ( 'NONE',  ( 116.5863248654051461, 1.414213562373201061, -1.414213562373145550 ) ) ;
#5568=DIRECTION ( 'NONE',  ( -1.000000000000000000, -1.665334536937736783E-16, -2.220446049250315546E-16 ) ) ;
#5582=CARTESIAN_POINT ( 'NONE',  ( 119.9999999999999574, 2.481996037641524655, 0.1722232477803059547 ) ) ;
#5585=FACE_BOUND ( 'NONE', #196, .T. ) ;
#5597=( BOUNDED_CURVE ( )  B_SPLINE_CURVE ( 2, ( #20760, #25489, #23522, #18771, #28540, #28245, #4899, #4756, #25807 ),
 .UNSPECIFIED., .F., .T. ) 
 B_SPLINE_CURVE_WITH_KNOTS ( ( 3, 2, 2, 2, 3 ),
 ( 0.6764705882352941568, 0.6838235294117647189, 0.6911764705882352811, 0.6985294117647058432, 0.7058823529411764053 ),
 .UNSPECIFIED. ) 
 CURVE ( )  GEOMETRIC_REPRESENTATION_ITEM ( )  RATIONAL_B_SPLINE_CURVE ( ( 1.000000000000000000, 0.9238795325112867385, 1.000000000000000000, 0.9238795325112867385, 1.000000000000000000, 0.9238795325112867385, 1.000000000000000000, 0.9238795325112867385, 1.000000000000000000 ) ) 
 REPRESENTATION_ITEM ( '' )  );
#5606=DIRECTION ( 'NONE',  ( 5.551115123125785167E-17, -1.000000000000000000, -8.881784197001256268E-16 ) ) ;
#5608=CARTESIAN_POINT ( 'NONE',  ( 120.5627832217621460, 0.7662911109078287542, 1.849990392679652151 ) ) ;
#5619=CARTESIAN_POINT ( 'NONE',  ( 106.0624999999998295, 2.500000000000114575, 1.035533905933049725 ) ) ;
#5620=VECTOR ( 'NONE', #15943, 1000.000000000000227 ) ;
#5626=CARTESIAN_POINT ( 'NONE',  ( -1.110223024625164676E-16, 2.000000000000012879, 2.021286199229734960E-15 ) ) ;
#5628=CARTESIAN_POINT ( 'NONE',  ( 119.7499999999998721, 1.110223024625156540E-13, -2.499999999999946709 ) ) ;
#5643=CARTESIAN_POINT ( 'NONE',  ( 119.8749999999998863, 1.767766952966320915, -1.767766952966320915 ) ) ;
#5660=FACE_OUTER_BOUND ( 'NONE', #2354, .T. ) ;
#5662=CARTESIAN_POINT ( 'NONE',  ( 111.2113248654051176, -1.999999999999946265, 0.000000000000000000 ) ) ;
#5670=CARTESIAN_POINT ( 'NONE',  ( 119.9999999999997584, 2.338294422933281602, -0.6637900606688733607 ) ) ;
#5674=EDGE_LOOP ( 'NONE', ( #20692, #26403, #27338, #8502 ) ) ;
#5680=CARTESIAN_POINT ( 'NONE',  ( 114.7497167782374561, 1.308140751793751555, 1.308140751793973600 ) ) ;
#5688=CARTESIAN_POINT ( 'NONE',  ( 113.3124999999997300, -1.035533905932598975, 2.500000000000144773 ) ) ;
#5692=ORIENTED_EDGE ( 'NONE', *, *, #4417, .F. ) ;
#5697=B_SPLINE_CURVE_WITH_KNOTS ( 'NONE', 1,
 ( #26409, #24112 ),
 .UNSPECIFIED., .F., .F.,
 ( 2, 2 ),
 ( 0.000000000000000000, 1.000000000000000000 ),
 .UNSPECIFIED. ) ;
#5708=CARTESIAN_POINT ( 'NONE',  ( 105.2886751345946550, 2.000000000000057288, 0.000000000000000000 ) ) ;
#5718=ADVANCED_FACE ( 'NONE', ( #29251 ), #16437, .T. ) ;
#5720=CARTESIAN_POINT ( 'NONE',  ( 111.2497167782375982, -1.308140751793640533, -1.308140751793640533 ) ) ;
#5758=CARTESIAN_POINT ( 'NONE',  ( 104.8122167782375129, 0.7662911109077388261, 1.849990392679712103 ) ) ;
#5763=ORIENTED_EDGE ( 'NONE', *, *, #7595, .T. ) ;
#5772=ORIENTED_EDGE ( 'NONE', *, *, #11999, .F. ) ;
#5774=CARTESIAN_POINT ( 'NONE',  ( 115.9136751345946266, -1.414213562373006772, -1.414213562373034527 ) ) ;
#5778=CARTESIAN_POINT ( 'NONE',  ( 118.2499999999997584, -8.326672684688674053E-14, 2.500000000000057732 ) ) ;
#5789=CARTESIAN_POINT ( 'NONE',  ( 119.0624999999998295, 2.500000000000024425, 1.035533905932809473 ) ) ;
#5795=CARTESIAN_POINT ( 'NONE',  ( 109.9372167782373424, -0.7662911109076785410, 1.849990392679712103 ) ) ;
#5801=EDGE_LOOP ( 'NONE', ( #16858, #5133, #14904, #5772 ) ) ;
#5821=CARTESIAN_POINT ( 'NONE',  ( 119.9999999999997584, 0.8621349162983860115, -2.008502556962187491 ) ) ;
#5825=CARTESIAN_POINT ( 'NONE',  ( 104.7401757384973138, -0.4781124843705381045, -1.791203832787282790 ) ) ;
#5836=CARTESIAN_POINT ( 'NONE',  ( 111.9997167782376550, -1.308140751793640533, 1.308140751793640533 ) ) ;
#5842=CARTESIAN_POINT ( 'NONE',  ( 112.4374999999998010, -2.499999999999934719, 1.035533905932989551 ) ) ;
#5867=CYLINDRICAL_SURFACE ( 'NONE', #22417, 2.000000000000012879 ) ;
#5872=CARTESIAN_POINT ( 'NONE',  ( 113.6247167782374987, 1.849990392679551343, 0.000000000000000000 ) ) ;
#5873=( BOUNDED_CURVE ( )  B_SPLINE_CURVE ( 2, ( #29952, #14186, #18927, #4608, #160, #25183, #2466, #22909, #23524 ),
 .UNSPECIFIED., .F., .T. ) 
 B_SPLINE_CURVE_WITH_KNOTS ( ( 3, 2, 2, 2, 3 ),
 ( 0.1176470588235294101, 0.1250000000000000000, 0.1323529411764705899, 0.1397058823529411797, 0.1470588235294117696 ),
 .UNSPECIFIED. ) 
 CURVE ( )  GEOMETRIC_REPRESENTATION_ITEM ( )  RATIONAL_B_SPLINE_CURVE ( ( 1.000000000000000000, 0.9238795325112867385, 1.000000000000000000, 0.9238795325112867385, 1.000000000000000000, 0.9238795325112867385, 1.000000000000000000, 0.9238795325112867385, 1.000000000000000000 ) ) 
 REPRESENTATION_ITEM ( '' )  );
#5891=CARTESIAN_POINT ( 'NONE',  ( 110.3511751345946266, 2.000000000000122125, 0.8284271247462955401 ) ) ;
#5898=CARTESIAN_POINT ( 'NONE',  ( 104.7401757384973138, 1.387249626875697306, 1.223929297688219897 ) ) ;
#5913=CARTESIAN_POINT ( 'NONE',  ( 118.5627832217621034, 0.7662911109077087390, 1.849990392679772278 ) ) ;
#5917=AXIS2_PLACEMENT_3D ( 'NONE', #23911, #5148, #25905 ) ;
#5937=CARTESIAN_POINT ( 'NONE',  ( 119.2499999999999574, -5.551115123125782702E-14, 2.500000000000168754 ) ) ;
#5938=CARTESIAN_POINT ( 'NONE',  ( 119.9999999999999574, -0.4876318259219858398, 1.939643060552387333 ) ) ;
#5949=ORIENTED_EDGE ( 'NONE', *, *, #17393, .F. ) ;
#5953=CARTESIAN_POINT ( 'NONE',  ( 111.7502832217623165, -1.308140751793585022, 1.308140751793862577 ) ) ;
#5984=CARTESIAN_POINT ( 'NONE',  ( 116.7502832217622171, -1.308140751793529510, 1.308140751793640533 ) ) ;
#5998=CARTESIAN_POINT ( 'NONE',  ( 113.1872167782373992, -1.849990392679441875, -0.7662911109075883909 ) ) ;
#6004=CARTESIAN_POINT ( 'NONE',  ( 114.4374999999998010, -2.499999999999964473, 1.035533905932929599 ) ) ;
#6017=CARTESIAN_POINT ( 'NONE',  ( 116.5238248654049471, 0.8284271247462654530, -1.999999999999851674 ) ) ;
#6024=CARTESIAN_POINT ( 'NONE',  ( 105.7886751345946550, -1.999999999999946265, 0.000000000000000000 ) ) ;
#6032=CARTESIAN_POINT ( 'NONE',  ( 107.7499999999998579, 5.551115123125782702E-14, -2.499999999999946709 ) ) ;
#6067=CARTESIAN_POINT ( 'NONE',  ( 104.6247167782375271, 1.849990392679523588, 0.000000000000000000 ) ) ;
#6071=CARTESIAN_POINT ( 'NONE',  ( 112.2886751345947118, 2.000000000000112799, 3.330669073875469621E-13 ) ) ;
#6080=CARTESIAN_POINT ( 'NONE',  ( 118.1252832217622881, -2.775557561562891351E-14, -1.849990392679523588 ) ) ;
#6086=DIRECTION ( 'NONE',  ( 5.551115123125785167E-17, -1.000000000000000000, -8.881784197001256268E-16 ) ) ;
#6101=CARTESIAN_POINT ( 'NONE',  ( 115.8124999999997584, 1.035533905932719101, -2.499999999999784173 ) ) ;
#6112=CARTESIAN_POINT ( 'NONE',  ( 120.6874999999997584, -1.035533905932719101, -2.499999999999844569 ) ) ;
#6113=CARTESIAN_POINT ( 'NONE',  ( 110.0002832217622597, -1.308140751793585022, -1.308140751793640533 ) ) ;
#6135=CARTESIAN_POINT ( 'NONE',  ( 5.000000000000018652, 8.326672684688674053E-14, 1.110223024625156540E-13 ) ) ;
#6136=EDGE_LOOP ( 'NONE', ( #24105, #3650, #30260, #28696 ) ) ;
#6140=VECTOR ( 'NONE', #9996, 1000.000000000000000 ) ;
#6143=CARTESIAN_POINT ( 'NONE',  ( 111.3752832217622739, 1.849990392679468076, 0.000000000000000000 ) ) ;
#6147=CARTESIAN_POINT ( 'NONE',  ( 119.9999999999998721, -0.4876318259425804769, -1.939643060543838615 ) ) ;
#6150=CARTESIAN_POINT ( 'NONE',  ( 104.7401757384972427, 0.5979633189608006827, -1.754835448641252293 ) ) ;
#6151=ORIENTED_EDGE ( 'NONE', *, *, #10133, .T. ) ;
#6158=CARTESIAN_POINT ( 'NONE',  ( 115.0622167782373850, -1.849990392679411677, 0.7662911109078888172 ) ) ;
#6160=CARTESIAN_POINT ( 'NONE',  ( 114.0386751345946834, 1.110223024625156540E-13, -1.999999999999668709 ) ) ;
#6167=CARTESIAN_POINT ( 'NONE',  ( 112.8749999999998437, 1.767766952966320915, -1.767766952966320915 ) ) ;
#6191=ORIENTED_EDGE ( 'NONE', *, *, #7767, .F. ) ;
#6192=CARTESIAN_POINT ( 'NONE',  ( 109.4374999999998721, -2.499999999999934719, 1.035533905932929599 ) ) ;
#6231=CARTESIAN_POINT ( 'NONE',  ( 116.4377832217621602, 1.849990392679621953, 0.7662911109081291805 ) ) ;
#6250=CARTESIAN_POINT ( 'NONE',  ( 116.1249999999999574, 1.767766952966265404, 1.767766952966431937 ) ) ;
#6260=CARTESIAN_POINT ( 'NONE',  ( 116.6874999999997726, -1.035533905932659149, -2.499999999999784173 ) ) ;
#6261=CARTESIAN_POINT ( 'NONE',  ( 111.6252832217622739, 0.000000000000000000, 1.849990392679523588 ) ) ;
#6264=ORIENTED_EDGE ( 'NONE', *, *, #24154, .T. ) ;
#6265=CARTESIAN_POINT ( 'NONE',  ( 109.1247167782376124, -1.849990392679523588, 1.110223024625156540E-13 ) ) ;
#6271=ORIENTED_EDGE ( 'NONE', *, *, #15305, .F. ) ;
#6286=CARTESIAN_POINT ( 'NONE',  ( 113.0002832217622455, -1.308140751793585022, -1.308140751793640533 ) ) ;
#6297=CARTESIAN_POINT ( 'NONE',  ( 104.7401757384971859, -1.662314916401979259, -0.8208299140997361576 ) ) ;
#6307=CARTESIAN_POINT ( 'NONE',  ( 119.7113248654050750, 2.000000000000001776, 1.110223024625156540E-13 ) ) ;
#6309=DIRECTION ( 'NONE',  ( 0.000000000000000000, -1.000000000000000000, -8.881784197001264156E-16 ) ) ;
#6330=CARTESIAN_POINT ( 'NONE',  ( 0.000000000000000000, 0.000000000000000000, 0.000000000000000000 ) ) ;
#6375=CARTESIAN_POINT ( 'NONE',  ( 117.3752832217622029, 1.849990392679523588, 0.000000000000000000 ) ) ;
#6383=ORIENTED_EDGE ( 'NONE', *, *, #25573, .T. ) ;
#6394=CARTESIAN_POINT ( 'NONE',  ( 114.8749999999998295, 1.767766952966320915, -1.767766952966209892 ) ) ;
#6404=CARTESIAN_POINT ( 'NONE',  ( 118.6874999999998295, -1.035533905932719101, -2.499999999999844569 ) ) ;
#6405=CARTESIAN_POINT ( 'NONE',  ( 108.6877832217621318, -0.7662911109077388261, 1.849990392679712103 ) ) ;
#6406=CARTESIAN_POINT ( 'NONE',  ( 107.8988248654050750, 0.8284271247461753029, 2.000000000000212275 ) ) ;
#6408=CARTESIAN_POINT ( 'NONE',  ( 109.8988248654049755, 0.8284271247462654530, 2.000000000000212275 ) ) ;
#6426=LINE ( 'NONE', #7452, #1996 ) ;
#6432=ADVANCED_FACE ( 'NONE', ( #13048 ), #29264, .F. ) ;
#6438=CARTESIAN_POINT ( 'NONE',  ( 111.7502832217623165, -1.308140751793585022, 1.308140751793862577 ) ) ;
#6456=CARTESIAN_POINT ( 'NONE',  ( 108.0622167782374703, -1.849990392679381701, 0.7662911109080090544 ) ) ;
#6458=CARTESIAN_POINT ( 'NONE',  ( 114.1011751345946834, 0.8284271247462654530, -1.999999999999731104 ) ) ;
#6459=CARTESIAN_POINT ( 'NONE',  ( 113.1247167782375556, -1.849990392679523588, 1.110223024625156540E-13 ) ) ;
#6474=PRODUCT ( 'Handle', 'Handle', '', ( #10857 ) ) ;
#6478=CARTESIAN_POINT ( 'NONE',  ( 105.2113248654051745, -1.999999999999974021, 0.000000000000000000 ) ) ;
#6496=CARTESIAN_POINT ( 'NONE',  ( 104.6874999999998579, -1.035533905932689347, -2.499999999999724221 ) ) ;
#6503=ADVANCED_FACE ( 'NONE', ( #22380 ), #8708, .F. ) ;
#6506=ORIENTED_EDGE ( 'NONE', *, *, #18026, .F. ) ;
#6526=CYLINDRICAL_SURFACE ( 'NONE', #25572, 2.000000000000012879 ) ;
#6556=CARTESIAN_POINT ( 'NONE',  ( 114.3749999999998010, -1.767766952966154381, 1.767766952966653982 ) ) ;
#6564=CARTESIAN_POINT ( 'NONE',  ( 115.1249999999998863, 1.767766952966376426, 1.767766952966320915 ) ) ;
#6566=CARTESIAN_POINT ( 'NONE',  ( 109.5627832217622455, 0.7662911109077987781, 1.849990392679652151 ) ) ;
#6570=CARTESIAN_POINT ( 'NONE',  ( 108.0622167782374703, -1.849990392679381701, 0.7662911109080090544 ) ) ;
#6572=ORIENTED_EDGE ( 'NONE', *, *, #9803, .T. ) ;
#6574=EDGE_CURVE ( 'NONE', #11262, #30108, #19709, .T. ) ;
#6576=EDGE_LOOP ( 'NONE', ( #9913, #6506 ) ) ;
#6587=DIRECTION ( 'NONE',  ( 0.000000000000000000, 1.000000000000000000, 8.881784197001252323E-16 ) ) ;
#6592=CARTESIAN_POINT ( 'NONE',  ( 112.5238248654049755, 0.8284271247463257382, -1.999999999999731104 ) ) ;
#6593=CARTESIAN_POINT ( 'NONE',  ( 112.4377832217622455, 1.849990392679621953, 0.7662911109081291805 ) ) ;
#6598=DIRECTION ( 'NONE',  ( -1.000000000000000000, -1.665334536937736783E-16, -2.220446049250315546E-16 ) ) ;
#6608=EDGE_CURVE ( 'NONE', #12110, #21920, #654, .T. ) ;
#6611=( BOUNDED_CURVE ( )  B_SPLINE_CURVE ( 2, ( #5708, #25321, #10666, #24301, #20011, #3404, #17734, #27059, #6024 ),
 .UNSPECIFIED., .F., .T. ) 
 B_SPLINE_CURVE_WITH_KNOTS ( ( 3, 2, 2, 2, 3 ),
 ( 0.02941176470588236294, 0.03676470588235292158, 0.04411764705882348370, 0.05147058823529415683, 0.05882352941176471894 ),
 .UNSPECIFIED. ) 
 CURVE ( )  GEOMETRIC_REPRESENTATION_ITEM ( )  RATIONAL_B_SPLINE_CURVE ( ( 1.000000000000000000, 0.9238795325112867385, 1.000000000000000000, 0.9238795325112867385, 1.000000000000000000, 0.9238795325112867385, 1.000000000000000000, 0.9238795325112867385, 1.000000000000000000 ) ) 
 REPRESENTATION_ITEM ( '' )  );
#6613=CARTESIAN_POINT ( 'NONE',  ( 110.3747167782375271, -5.551115123125782702E-14, -1.849990392679523588 ) ) ;
#6615=CARTESIAN_POINT ( 'NONE',  ( 113.1872167782373992, -1.849990392679441875, -0.7662911109075883909 ) ) ;
#6619=CARTESIAN_POINT ( 'NONE',  ( 113.5863248654051318, 1.414213562373145550, -1.414213562373145550 ) ) ;
#6640=CARTESIAN_POINT ( 'NONE',  ( 112.0624999999997868, 2.500000000000054623, 1.035533905932989551 ) ) ;
#6654=CARTESIAN_POINT ( 'NONE',  ( 105.9999999999998863, 2.500000000000002220, 1.110223024625156540E-13 ) ) ;
#6671=CARTESIAN_POINT ( 'NONE',  ( 0.000000000000000000, 0.000000000000000000, 0.000000000000000000 ) ) ;
#6683=FACE_OUTER_BOUND ( 'NONE', #9105, .T. ) ;
#6688=CARTESIAN_POINT ( 'NONE',  ( 116.0622167782373566, -1.849990392679381701, 0.7662911109079489913 ) ) ;
#6713=CARTESIAN_POINT ( 'NONE',  ( 118.1874999999997158, 1.035533905932719101, 2.500000000000205169 ) ) ;
#6724=CARTESIAN_POINT ( 'NONE',  ( 107.0002832217622597, -1.308140751793585022, -1.308140751793640533 ) ) ;
#6763=ORIENTED_EDGE ( 'NONE', *, *, #7915, .T. ) ;
#6764=CARTESIAN_POINT ( 'NONE',  ( 110.0622167782374987, -1.849990392679441875, 0.7662911109079489913 ) ) ;
#6766=CARTESIAN_POINT ( 'NONE',  ( 112.6872167782374419, 1.849990392679621953, 0.7662911109081291805 ) ) ;
#6769=CARTESIAN_POINT ( 'NONE',  ( 104.7401757384973280, 1.387249626875697306, 1.223929297688219897 ) ) ;
#6770=AXIS2_PLACEMENT_3D ( 'NONE', #3480, #24691, #15200 ) ;
#6783=CARTESIAN_POINT ( 'NONE',  ( 115.2113248654050750, -1.999999999999918510, 1.110223024625156540E-13 ) ) ;
#6786=CARTESIAN_POINT ( 'NONE',  ( 110.1874999999997584, 1.035533905932779275, 2.500000000000205169 ) ) ;
#6791=( NAMED_UNIT ( * ) PLANE_ANGLE_UNIT ( ) SI_UNIT ( $, .RADIAN. ) );
#6797=CARTESIAN_POINT ( 'NONE',  ( 120.5622167782374419, 1.849990392679652151, -0.7662911109075283278 ) ) ;
#6805=B_SPLINE_CURVE_WITH_KNOTS ( 'NONE', 3,
 ( #22042, #5582, #17155, #7593, #3425, #21901, #26334, #14987, #5285, #980, #10379, #14694, #24040, #24326, #2986, #8044, #13465, #1903 ),
 .UNSPECIFIED., .F., .F.,
 ( 4, 2, 2, 2, 2, 2, 2, 2, 4 ),
 ( 0.000000000000000000, 0.0005121067916087861365, 0.001024213583217572273, 0.001536320374826358626, 0.002048427166435145413, 0.002560533958043931767, 0.003072640749652718120, 0.003584747541261505341, 0.004096854332870291694 ),
 .UNSPECIFIED. ) ;
#6808=ORIENTED_EDGE ( 'NONE', *, *, #10567, .T. ) ;
#6816=CARTESIAN_POINT ( 'NONE',  ( 117.9377832217621744, -1.849990392679441875, -0.7662911109075883909 ) ) ;
#6823=CARTESIAN_POINT ( 'NONE',  ( 105.4613248654050324, 0.000000000000000000, -2.000000000000001776 ) ) ;
#6836=CARTESIAN_POINT ( 'NONE',  ( 119.0622167782374561, -1.849990392679381701, 0.7662911109078888172 ) ) ;
#6838=ORIENTED_EDGE ( 'NONE', *, *, #8248, .F. ) ;
#6862=CARTESIAN_POINT ( 'NONE',  ( 113.6874999999998437, -1.035533905932749299, -2.499999999999904521 ) ) ;
#6872=CARTESIAN_POINT ( 'NONE',  ( 113.3749999999999289, -1.767766952966293159, 1.767766952966431937 ) ) ;
#6874=CARTESIAN_POINT ( 'NONE',  ( 106.1877832217621318, 0.7662911109077987781, -1.849990392679351725 ) ) ;
#6896=CARTESIAN_POINT ( 'NONE',  ( 112.2738248654049471, -1.999999999999941602, -0.8284271247459952248 ) ) ;
#6897=CARTESIAN_POINT ( 'NONE',  ( 109.3752832217621744, 1.849990392679579099, 1.110223024625156540E-13 ) ) ;
#6903=COLOUR_RGB ( '', 0.09019608, 0.27058824, 0.51372549) ;
#6907=CARTESIAN_POINT ( 'NONE',  ( 114.4761751345946266, 0.8284271247463257382, 2.000000000000271783 ) ) ;
#6908=VERTEX_POINT ( 'NONE', #15256 ) ;
#6913=CARTESIAN_POINT ( 'NONE',  ( 111.3122167782374277, -0.7662911109076785410, -1.849990392679291551 ) ) ;
#6940=CARTESIAN_POINT ( 'NONE',  ( 111.5624999999997584, -2.499999999999964473, -1.035533905932689347 ) ) ;
#6942=CARTESIAN_POINT ( 'NONE',  ( 115.1011751345945981, 0.8284271247463257382, -1.999999999999791278 ) ) ;
#6944=VERTEX_POINT ( 'NONE', #5537 ) ;
#6950=CARTESIAN_POINT ( 'NONE',  ( 104.6249999999999005, -1.767766952966376426, -1.767766952966320915 ) ) ;
#6967=CARTESIAN_POINT ( 'NONE',  ( 107.1247167782375556, -1.849990392679301543, 2.220446049250313081E-13 ) ) ;
#6970=CARTESIAN_POINT ( 'NONE',  ( 117.4377832217621602, 1.849990392679562001, 0.7662911109079489913 ) ) ;
#6990=CARTESIAN_POINT ( 'NONE',  ( 116.3122167782374845, -0.7662911109077388261, -1.849990392679351725 ) ) ;
#6995=CARTESIAN_POINT ( 'NONE',  ( 113.1252832217622029, -1.110223024625156540E-13, -1.849990392679523588 ) ) ;
#7014=CARTESIAN_POINT ( 'NONE',  ( 111.6249999999998153, -1.767766952966376426, -1.767766952966431937 ) ) ;
#7020=( GEOMETRIC_REPRESENTATION_CONTEXT ( 3 ) GLOBAL_UNCERTAINTY_ASSIGNED_CONTEXT ( ( #21415 ) ) GLOBAL_UNIT_ASSIGNED_CONTEXT ( ( #21905, #10083, #26628 ) ) REPRESENTATION_CONTEXT ( 'NONE', 'WORKASPACE' ) );
#7024=CARTESIAN_POINT ( 'NONE',  ( 111.5624999999997584, -2.499999999999964473, -1.035533905932689347 ) ) ;
#7026=CARTESIAN_POINT ( 'NONE',  ( 10.00000000000002309, -5.999999999999914735, 1.056932319443149026E-13 ) ) ;
#7027=CARTESIAN_POINT ( 'NONE',  ( 107.8752832217621602, -1.849990392679329299, 3.330669073875469621E-13 ) ) ;
#7032=CARTESIAN_POINT ( 'NONE',  ( 105.3122167782374277, -0.7662911109076785410, -1.849990392679231599 ) ) ;
#7046=VERTEX_POINT ( 'NONE', #10254 ) ;
#7049=CARTESIAN_POINT ( 'NONE',  ( 107.2499999999999147, 0.000000000000000000, 2.499999999999946709 ) ) ;
#7054=CARTESIAN_POINT ( 'NONE',  ( 109.9377832217622029, -1.849990392679472073, -0.7662911109076485650 ) ) ;
#7067=CARTESIAN_POINT ( 'NONE',  ( 115.7113248654050466, 2.000000000000112799, 0.000000000000000000 ) ) ;
#7069=CARTESIAN_POINT ( 'NONE',  ( 111.4372167782375271, 0.7662911109078888172, -1.849990392679231599 ) ) ;
#7073=ORIENTED_EDGE ( 'NONE', *, *, #22255, .F. ) ;
#7092=CARTESIAN_POINT ( 'NONE',  ( 112.1874999999998153, 1.035533905932719101, 2.500000000000205169 ) ) ;
#7102=CARTESIAN_POINT ( 'NONE',  ( 106.5624999999998295, -2.499999999999874767, -1.035533905932629173 ) ) ;
#7106=CARTESIAN_POINT ( 'NONE',  ( 112.2113248654051176, -1.999999999999946265, 0.000000000000000000 ) ) ;
#7118=CARTESIAN_POINT ( 'NONE',  ( 107.1872167782375840, -1.849990392679441875, -0.7662911109076485650 ) ) ;
#7121=CARTESIAN_POINT ( 'NONE',  ( 118.2502832217622739, 1.308140751793640533, -1.308140751793418488 ) ) ;
#7123=CARTESIAN_POINT ( 'NONE',  ( -2.775557561562891351E-14, 6.000000000000088818, 1.110223024625156540E-13 ) ) ;
#7124=CIRCLE ( 'NONE', #2688, 5.000000000000004441 ) ;
#7127=CARTESIAN_POINT ( 'NONE',  ( 105.2738248654049329, -1.999999999999941602, -0.8284271247460553989 ) ) ;
#7139=CARTESIAN_POINT ( 'NONE',  ( 119.2497167782374987, -1.308140751793557266, -1.308140751793640533 ) ) ;
#7145=CARTESIAN_POINT ( 'NONE',  ( 115.3127832217621886, 1.849990392679562001, -0.7662911109076485650 ) ) ;
#7166=CARTESIAN_POINT ( 'NONE',  ( 110.5624999999998295, -2.499999999999994671, -1.035533905932568777 ) ) ;
#7179=CARTESIAN_POINT ( 'NONE',  ( 112.3124999999997726, -1.035533905932598975, 2.500000000000265121 ) ) ;
#7181=CARTESIAN_POINT ( 'NONE',  ( 108.5627832217621886, 0.7662911109077987781, 1.849990392679652151 ) ) ;
#7187=ORIENTED_EDGE ( 'NONE', *, *, #14160, .T. ) ;
#7199=CARTESIAN_POINT ( 'NONE',  ( 108.2499999999998863, 5.551115123125782702E-14, 2.499999999999946709 ) ) ;
#7203=CARTESIAN_POINT ( 'NONE',  ( 109.4761751345945839, 0.8284271247462654530, 2.000000000000271783 ) ) ;
#7206=CARTESIAN_POINT ( 'NONE',  ( 107.2502832217623450, 1.308140751793640533, -1.308140751793640533 ) ) ;
#7208=CARTESIAN_POINT ( 'NONE',  ( 119.6011751345946692, -0.8284271247462354770, 2.000000000000212275 ) ) ;
#7214=CARTESIAN_POINT ( 'NONE',  ( 114.6011751345946692, -0.8284271247461453269, 2.000000000000271783 ) ) ;
#7218=CARTESIAN_POINT ( 'NONE',  ( 0.000000000000000000, 0.000000000000000000, 0.000000000000000000 ) ) ;
#7226=CARTESIAN_POINT ( 'NONE',  ( 110.3747167782375271, -5.551115123125782702E-14, -1.849990392679523588 ) ) ;
#7249=CARTESIAN_POINT ( 'NONE',  ( 108.8988248654050608, 0.8284271247462354770, 2.000000000000212275 ) ) ;
#7250=CARTESIAN_POINT ( 'NONE',  ( 109.1874999999997584, 1.035533905932839227, 2.500000000000205169 ) ) ;
#7259=CARTESIAN_POINT ( 'NONE',  ( 119.0622167782374561, -1.849990392679381701, 0.7662911109078888172 ) ) ;
#7268=CARTESIAN_POINT ( 'NONE',  ( 119.5624999999998153, -2.499999999999874767, -1.035533905932629173 ) ) ;
#7281=CARTESIAN_POINT ( 'NONE',  ( 104.3747167782376124, -5.551115123125782702E-14, -1.849990392679523588 ) ) ;
#7284=CARTESIAN_POINT ( 'NONE',  ( 118.4377832217621034, 1.849990392679591977, 0.7662911109080090544 ) ) ;
#7295=CARTESIAN_POINT ( 'NONE',  ( 108.3511751345945981, 2.000000000000122125, 0.8284271247464157772 ) ) ;
#7298=B_SPLINE_CURVE_WITH_KNOTS ( 'NONE', 1,
 ( #10503, #24768 ),
 .UNSPECIFIED., .F., .F.,
 ( 2, 2 ),
 ( 0.1800073590160146952, 1.000000000000000000 ),
 .UNSPECIFIED. ) ;
#7304=CARTESIAN_POINT ( 'NONE',  ( 118.7886751345946692, -1.999999999999918510, 2.220446049250313081E-13 ) ) ;
#7305=CARTESIAN_POINT ( 'NONE',  ( 115.3752832217622881, 1.849990392679579099, 0.000000000000000000 ) ) ;
#7311=ADVANCED_FACE ( 'NONE', ( #13815 ), #27724, .F. ) ;
#7319=CARTESIAN_POINT ( 'NONE',  ( 112.7499999999998579, -5.551115123125782702E-14, -2.499999999999946709 ) ) ;
#7321=VECTOR ( 'NONE', #10816, 1000.000000000000000 ) ;
#7323=( BOUNDED_CURVE ( )  B_SPLINE_CURVE ( 2, ( #27536, #1751, #2222, #1905, #8983, #8833, #29854, #25707, #11626 ),
 .UNSPECIFIED., .F., .F. ) 
 B_SPLINE_CURVE_WITH_KNOTS ( ( 3, 2, 2, 2, 3 ),
 ( 0.4705882352941176405, 0.4779411764705882026, 0.4852941176470588203, 0.4926470588235293824, 0.5000000000000000000 ),
 .UNSPECIFIED. ) 
 CURVE ( )  GEOMETRIC_REPRESENTATION_ITEM ( )  RATIONAL_B_SPLINE_CURVE ( ( 1.000000000000000000, 0.9238795325112867385, 1.000000000000000000, 0.9238795325112867385, 1.000000000000000000, 0.9238795325112867385, 1.000000000000000000, 0.9238795325112867385, 1.000000000000000000 ) ) 
 REPRESENTATION_ITEM ( '' )  );
#7328=APPLICATION_CONTEXT ( 'automotive_design' ) ;
#7329=CARTESIAN_POINT ( 'NONE',  ( 111.7499999999998010, 0.000000000000000000, -2.499999999999946709 ) ) ;
#7331=CARTESIAN_POINT ( 'NONE',  ( 108.0627832217621034, -0.7662911109077388261, -1.849990392679351725 ) ) ;
#7332=CARTESIAN_POINT ( 'NONE',  ( 112.7738248654049755, 2.000000000000091926, 0.8284271247462955401 ) ) ;
#7337=CARTESIAN_POINT ( 'NONE',  ( 107.4372167782373850, 0.7662911109078287542, -1.849990392679351725 ) ) ;
#7339=CARTESIAN_POINT ( 'NONE',  ( 110.8363248654051034, 1.414213562373117794, 1.414213562373034527 ) ) ;
#7342=VERTEX_POINT ( 'NONE', #1943 ) ;
#7351=CARTESIAN_POINT ( 'NONE',  ( 109.1249999999999289, 1.767766952966265404, 1.767766952966431937 ) ) ;
#7358=CARTESIAN_POINT ( 'NONE',  ( 106.8752832217622739, -1.849990392679301543, 2.220446049250313081E-13 ) ) ;
#7360=CARTESIAN_POINT ( 'NONE',  ( 119.6636751345947687, -1.414213562373173305, 1.414213562373145550 ) ) ;
#7378=CARTESIAN_POINT ( 'NONE',  ( 1.110223024625164183E-16, -2.000000000000012879, -1.776356839400262692E-15 ) ) ;
#7379=VERTEX_POINT ( 'NONE', #27882 ) ;
#7400=CARTESIAN_POINT ( 'NONE',  ( 105.6874999999997584, -1.035533905932659149, -2.499999999999724221 ) ) ;
#7407=CARTESIAN_POINT ( 'NONE',  ( 117.9997167782376266, -1.308140751793696044, 1.308140751793751555 ) ) ;
#7413=CARTESIAN_POINT ( 'NONE',  ( 119.0624999999998295, 2.500000000000024425, 1.035533905932809473 ) ) ;
#7423=CARTESIAN_POINT ( 'NONE',  ( 106.6247167782375840, 1.849990392679523588, 0.000000000000000000 ) ) ;
#7444=CARTESIAN_POINT ( 'NONE',  ( 104.7401757384973280, 1.387249626875697306, 1.223929297688219897 ) ) ;
#7452=CARTESIAN_POINT ( 'NONE',  ( -1.110223024625164676E-16, 2.000000000000012879, 2.021286199229734960E-15 ) ) ;
#7455=( BOUNDED_CURVE ( )  B_SPLINE_CURVE ( 2, ( #10608, #15394, #10778, #22430, #1368, #20126, #8440, #14556, #30086 ),
 .UNSPECIFIED., .F., .F. ) 
 B_SPLINE_CURVE_WITH_KNOTS ( ( 3, 2, 2, 2, 3 ),
 ( 0.1470588235294117974, 0.1544117647058823595, 0.1617647058823529216, 0.1691176470588234837, 0.1764705882352941568 ),
 .UNSPECIFIED. ) 
 CURVE ( )  GEOMETRIC_REPRESENTATION_ITEM ( )  RATIONAL_B_SPLINE_CURVE ( ( 1.000000000000000000, 0.9238795325112867385, 1.000000000000000000, 0.9238795325112867385, 1.000000000000000000, 0.9238795325112867385, 1.000000000000000000, 0.9238795325112867385, 1.000000000000000000 ) ) 
 REPRESENTATION_ITEM ( '' )  );
#7456=DIRECTION ( 'NONE',  ( 5.551115123125785167E-17, -1.000000000000000000, -8.881784197001256268E-16 ) ) ;
#7457=DIRECTION ( 'NONE',  ( 5.551115123125785167E-17, -1.000000000000000000, -8.881784197001256268E-16 ) ) ;
#7462=CARTESIAN_POINT ( 'NONE',  ( 111.5624999999997584, -2.499999999999964473, -1.035533905932689347 ) ) ;
#7468=CARTESIAN_POINT ( 'NONE',  ( 109.6488248654050466, 2.000000000000061728, -0.8284271247459952248 ) ) ;
#7470=CARTESIAN_POINT ( 'NONE',  ( 114.3749999999998010, -1.767766952966154381, 1.767766952966653982 ) ) ;
#7478=CARTESIAN_POINT ( 'NONE',  ( 106.7497167782375129, 1.308140751793612777, 1.308140751793529510 ) ) ;
#7486=ORIENTED_EDGE ( 'NONE', *, *, #13440, .T. ) ;
#7489=CARTESIAN_POINT ( 'NONE',  ( 107.6874999999997726, -1.035533905932659149, -2.499999999999724221 ) ) ;
#7493=CARTESIAN_POINT ( 'NONE',  ( 107.0627832217620892, -0.7662911109076184779, -1.849990392679351725 ) ) ;
#7496=CARTESIAN_POINT ( 'NONE',  ( 113.3511751345947403, 2.000000000000001776, 0.8284271247464157772 ) ) ;
#7516=ORIENTED_EDGE ( 'NONE', *, *, #17878, .F. ) ;
#7518=LINE ( 'NONE', #2907, #6140 ) ;
#7534=CARTESIAN_POINT ( 'NONE',  ( 104.9999999999998579, 2.500000000000002220, 0.000000000000000000 ) ) ;
#7537=CARTESIAN_POINT ( 'NONE',  ( 114.8511751345945981, -2.000000000000001776, -0.8284271247460553989 ) ) ;
#7543=CARTESIAN_POINT ( 'NONE',  ( 117.8511751345945129, -1.999999999999941602, -0.8284271247459952248 ) ) ;
#7546=CARTESIAN_POINT ( 'NONE',  ( 118.9372167782374277, -0.7662911109077686911, 1.849990392679652151 ) ) ;
#7547=CARTESIAN_POINT ( 'NONE',  ( 118.4136751345946834, 1.414213562373173305, 1.414213562373034527 ) ) ;
#7551=CARTESIAN_POINT ( 'NONE',  ( 118.1249999999999147, 1.767766952966320915, 1.767766952966431937 ) ) ;
#7563=CARTESIAN_POINT ( 'NONE',  ( 114.8752832217623165, -1.849990392679523588, 0.000000000000000000 ) ) ;
#7565=CARTESIAN_POINT ( 'NONE',  ( 110.7113248654050182, 2.000000000000057288, 0.000000000000000000 ) ) ;
#7580=CARTESIAN_POINT ( 'NONE',  ( 115.4372167782374561, 0.7662911109078287542, -1.849990392679231599 ) ) ;
#7582=( BOUNDED_CURVE ( )  B_SPLINE_CURVE ( 2, ( #1193, #10600, #19953, #23028, #11532, #13687, #27905, #8742, #30072 ),
 .UNSPECIFIED., .F., .T. ) 
 B_SPLINE_CURVE_WITH_KNOTS ( ( 3, 2, 2, 2, 3 ),
 ( 0.7941176470588234837, 0.8014705882352941568, 0.8088235294117647189, 0.8161764705882352811, 0.8235294117647058432 ),
 .UNSPECIFIED. ) 
 CURVE ( )  GEOMETRIC_REPRESENTATION_ITEM ( )  RATIONAL_B_SPLINE_CURVE ( ( 1.000000000000000000, 0.9238795325112867385, 1.000000000000000000, 0.9238795325112867385, 1.000000000000000000, 0.9238795325112867385, 1.000000000000000000, 0.9238795325112867385, 1.000000000000000000 ) ) 
 REPRESENTATION_ITEM ( '' )  );
#7593=CARTESIAN_POINT ( 'NONE',  ( 119.9999999999998295, 2.338294422934558803, 0.6637900606655252611 ) ) ;
#7595=EDGE_CURVE ( 'NONE', #14551, #3730, #7518, .T. ) ;
#7607=EDGE_CURVE ( 'NONE', #28323, #1437, #17075, .T. ) ;
#7612=CARTESIAN_POINT ( 'NONE',  ( 109.2113248654051745, -1.999999999999946265, 0.000000000000000000 ) ) ;
#7614=CARTESIAN_POINT ( 'NONE',  ( 109.6874999999997868, -1.035533905932659149, -2.499999999999724221 ) ) ;
#7621=CARTESIAN_POINT ( 'NONE',  ( 120.5002832217621886, 1.308140751793723799, 1.308140751793751555 ) ) ;
#7632=CARTESIAN_POINT ( 'NONE',  ( 108.6874999999998010, -1.035533905932749299, -2.499999999999844569 ) ) ;
#7642=CARTESIAN_POINT ( 'NONE',  ( 105.6877832217623023, -0.7662911109077987781, 1.849990392679532247 ) ) ;
#7652=CARTESIAN_POINT ( 'NONE',  ( 110.2113248654050608, -1.999999999999946265, 0.000000000000000000 ) ) ;
#7685=CARTESIAN_POINT ( 'NONE',  ( 106.4999999999999147, -2.499999999999946709, 1.110223024625156540E-13 ) ) ;
#7695=CARTESIAN_POINT ( 'NONE',  ( 117.3747167782375271, 0.000000000000000000, -1.849990392679301543 ) ) ;
#7700=CARTESIAN_POINT ( 'NONE',  ( 117.7499999999998721, 1.387778780781445676E-13, -2.499999999999835687 ) ) ;
#7703=DIRECTION ( 'NONE',  ( -2.220446049250313574E-16, -1.010643099614860775E-15, 1.000000000000000000 ) ) ;
#7714=ADVANCED_FACE ( 'NONE', ( #5541 ), #1236, .F. ) ;
#7719=CARTESIAN_POINT ( 'NONE',  ( 116.8127832217622597, -1.849990392679441875, 0.7662911109078888172 ) ) ;
#7732=CARTESIAN_POINT ( 'NONE',  ( 115.1872167782374987, -1.849990392679441875, -0.7662911109075283278 ) ) ;
#7748=SHAPE_REPRESENTATION_RELATIONSHIP ( 'NONE' , 'NONE' ,  #4035, #24617 ) ;
#7754=CARTESIAN_POINT ( 'NONE',  ( 1.110223024625164183E-16, -2.000000000000012879, -1.776356839400262692E-15 ) ) ;
#7759=CARTESIAN_POINT ( 'NONE',  ( 110.9999999999999147, 2.500000000000057732, 0.000000000000000000 ) ) ;
#7766=CARTESIAN_POINT ( 'NONE',  ( 121.1877832217620750, 0.7662911109077987781, -1.849990392679291551 ) ) ;
#7767=EDGE_CURVE ( 'NONE', #24100, #13876, #7124, .T. ) ;
#7778=LINE ( 'NONE', #26518, #24024 ) ;
#7786=CARTESIAN_POINT ( 'NONE',  ( 105.8752832217621602, -1.849990392679412565, 2.220446049250313081E-13 ) ) ;
#7789=CARTESIAN_POINT ( 'NONE',  ( 113.6636751345946408, -1.414213562373034527, 1.414213562373034527 ) ) ;
#7816=DIRECTION ( 'NONE',  ( -1.000000000000000000, -1.665334536937736783E-16, -2.220446049250315546E-16 ) ) ;
#7828=CARTESIAN_POINT ( 'NONE',  ( 106.6249999999999289, -1.767766952966376426, -1.767766952966320915 ) ) ;
#7833=CARTESIAN_POINT ( 'NONE',  ( 104.7401757384972569, 0.9320968428604275990, -1.616116470751321144 ) ) ;
#7842=CARTESIAN_POINT ( 'NONE',  ( 117.1247167782376408, -1.849990392679579099, 1.110223024625156540E-13 ) ) ;
#7849=CARTESIAN_POINT ( 'NONE',  ( 113.9374999999997158, 2.500000000000115019, -1.035533905932629173 ) ) ;
#7880=DIRECTION ( 'NONE',  ( 5.551115123125785167E-17, -1.000000000000000000, -8.881784197001256268E-16 ) ) ;
#7881=CARTESIAN_POINT ( 'NONE',  ( 114.5622167782375556, 1.849990392679682127, -0.7662911109076485650 ) ) ;
#7915=EDGE_CURVE ( 'NONE', #13609, #6944, #12065, .T. ) ;
#7919=B_SPLINE_CURVE_WITH_KNOTS ( 'NONE', 3,
 ( #1764, #11165, #20512, #29866, #3374, #26166, #10479, #19130, #26717, #14403 ),
 .UNSPECIFIED., .F., .F.,
 ( 4, 2, 2, 2, 4 ),
 ( 0.000000000000000000, 0.0006454309646850751002, 0.001290861929370150200, 0.001936292894055225301, 0.002581723858740300401 ),
 .UNSPECIFIED. ) ;
#7925=AXIS2_PLACEMENT_3D ( 'NONE', #7123, #4817, #28308 ) ;
#7929=ORIENTED_EDGE ( 'NONE', *, *, #26868, .T. ) ;
#7938=CARTESIAN_POINT ( 'NONE',  ( 116.1636751345946976, 1.414213562373145550, -1.414213562373145550 ) ) ;
#7943=CARTESIAN_POINT ( 'NONE',  ( 120.6249999999998295, -1.767766952966376426, -1.767766952966320915 ) ) ;
#7951=FACE_OUTER_BOUND ( 'NONE', #22339, .T. ) ;
#7954=CARTESIAN_POINT ( 'NONE',  ( 120.8749999999998863, 1.767766952966348670, -1.767766952966209892 ) ) ;
#7956=EDGE_CURVE ( 'NONE', #23930, #10100, #4981, .T. ) ;
#7972=ORIENTED_EDGE ( 'NONE', *, *, #26900, .F. ) ;
#7984=CARTESIAN_POINT ( 'NONE',  ( 106.8124999999997016, 1.035533905932749299, -2.499999999999784173 ) ) ;
#7991=( BOUNDED_CURVE ( )  B_SPLINE_CURVE ( 2, ( #12440, #5466, #12149, #28966, #26516, #24073, #3165, #19188, #17490 ),
 .UNSPECIFIED., .F., .F. ) 
 B_SPLINE_CURVE_WITH_KNOTS ( ( 3, 2, 2, 2, 3 ),
 ( 0.3823529411764705621, 0.3897058823529411797, 0.3970588235294117418, 0.4044117647058823595, 0.4117647058823529216 ),
 .UNSPECIFIED. ) 
 CURVE ( )  GEOMETRIC_REPRESENTATION_ITEM ( )  RATIONAL_B_SPLINE_CURVE ( ( 1.000000000000000000, 0.9238795325112867385, 1.000000000000000000, 0.9238795325112867385, 1.000000000000000000, 0.9238795325112867385, 1.000000000000000000, 0.9238795325112867385, 1.000000000000000000 ) ) 
 REPRESENTATION_ITEM ( '' )  );
#7998=ORIENTED_EDGE ( 'NONE', *, *, #7607, .F. ) ;
#7999=CARTESIAN_POINT ( 'NONE',  ( 113.4997167782376550, 1.308140751793640533, -1.308140751793640533 ) ) ;
#8004=CARTESIAN_POINT ( 'NONE',  ( 113.3749999999999289, -1.767766952966293159, 1.767766952966431937 ) ) ;
#8030=CYLINDRICAL_SURFACE ( 'NONE', #8449, 2.000000000000012879 ) ;
#8033=CARTESIAN_POINT ( 'NONE',  ( 111.8122167782374419, 0.7662911109077987781, 1.849990392679772278 ) ) ;
#8044=CARTESIAN_POINT ( 'NONE',  ( 119.9999999999998437, -0.1589013571266416347, 2.047736629975339451 ) ) ;
#8058=DIRECTION ( 'NONE',  ( 0.000000000000000000, -1.000000000000000000, -8.881784197001264156E-16 ) ) ;
#8063=CARTESIAN_POINT ( 'NONE',  ( 105.1872167782375556, -1.849990392679441875, -0.7662911109075883909 ) ) ;
#8085=CARTESIAN_POINT ( 'NONE',  ( 105.6252832217623592, 0.000000000000000000, 1.849990392679523588 ) ) ;
#8096=CARTESIAN_POINT ( 'NONE',  ( 119.3124999999998437, -1.035533905932689347, 2.500000000000265121 ) ) ;
#8121=CARTESIAN_POINT ( 'NONE',  ( 0.000000000000000000, 0.000000000000000000, 0.000000000000000000 ) ) ;
#8133=CARTESIAN_POINT ( 'NONE',  ( 104.7401757384972285, -1.801236194818849778, -0.4861741747051813167 ) ) ;
#8138=CARTESIAN_POINT ( 'NONE',  ( 108.5386751345947403, 5.551115123125782702E-14, 2.000000000000001776 ) ) ;
#8140=CARTESIAN_POINT ( 'NONE',  ( 115.6247167782374561, 1.849990392679523588, 0.000000000000000000 ) ) ;
#8145=CARTESIAN_POINT ( 'NONE',  ( 115.9374999999998010, 2.500000000000054623, -1.035533905932629173 ) ) ;
#8177=CARTESIAN_POINT ( 'NONE',  ( 113.4372167782374277, 0.7662911109077987781, -1.849990392679291551 ) ) ;
#8178=AXIS2_PLACEMENT_3D ( 'NONE', #7218, #16630, #25950 ) ;
#8193=CARTESIAN_POINT ( 'NONE',  ( 106.2738248654049187, -1.999999999999941602, -0.8284271247460553989 ) ) ;
#8195=CARTESIAN_POINT ( 'NONE',  ( 110.5386751345947403, 0.000000000000000000, 2.000000000000001776 ) ) ;
#8208=LINE ( 'NONE', #3904, #25824 ) ;
#8210=FACE_OUTER_BOUND ( 'NONE', #638, .T. ) ;
#8220=CARTESIAN_POINT ( 'NONE',  ( 117.5627832217621460, 0.7662911109078588412, 1.849990392679772278 ) ) ;
#8227=ORIENTED_EDGE ( 'NONE', *, *, #11335, .T. ) ;
#8238=CARTESIAN_POINT ( 'NONE',  ( 106.0002832217622029, -1.308140751793585022, -1.308140751793640533 ) ) ;
#8248=EDGE_CURVE ( 'NONE', #16270, #28423, #23967, .T. ) ;
#8251=CARTESIAN_POINT ( 'NONE',  ( 111.2502832217621886, 1.308140751793696044, -1.308140751793640533 ) ) ;
#8255=CARTESIAN_POINT ( 'NONE',  ( 109.6247167782375840, 1.849990392679634610, 1.110223024625156540E-13 ) ) ;
#8268=SURFACE_STYLE_FILL_AREA ( #8437 ) ;
#8271=( NAMED_UNIT ( * ) SI_UNIT ( $, .STERADIAN. ) SOLID_ANGLE_UNIT ( ) );
#8280=CARTESIAN_POINT ( 'NONE',  ( 115.8752832217622313, -1.849990392679468076, 1.110223024625156540E-13 ) ) ;
#8285=CARTESIAN_POINT ( 'NONE',  ( 119.9999999999998437, 0.3537249946064329187, -2.089338094882287056 ) ) ;
#8299=CARTESIAN_POINT ( 'NONE',  ( 115.3747167782374987, -5.551115123125782702E-14, -1.849990392679523588 ) ) ;
#8306=CARTESIAN_POINT ( 'NONE',  ( 114.6249999999999574, -1.767766952966431937, -1.767766952966431937 ) ) ;
#8309=ORIENTED_EDGE ( 'NONE', *, *, #21885, .F. ) ;
#8321=CIRCLE ( 'NONE', #12297, 2.000000000000012879 ) ;
#8333=CARTESIAN_POINT ( 'NONE',  ( 110.3749999999999289, -1.767766952966209892, 1.767766952966542959 ) ) ;
#8339=CARTESIAN_POINT ( 'NONE',  ( 110.5622167782373992, 1.849990392679501827, -0.7662911109077087390 ) ) ;
#8341=EDGE_CURVE ( 'NONE', #14551, #11262, #24442, .T. ) ;
#8378=CARTESIAN_POINT ( 'NONE',  ( 120.1872167782373992, -1.849990392679441875, -0.7662911109076485650 ) ) ;
#8385=CARTESIAN_POINT ( 'NONE',  ( 118.6252832217622029, 5.551115123125782702E-14, 1.849990392679634610 ) ) ;
#8386=CIRCLE ( 'NONE', #4469, 5.000000000000004441 ) ;
#8400=CARTESIAN_POINT ( 'NONE',  ( 115.8511751345946976, -1.999999999999971800, -0.8284271247459350507 ) ) ;
#8404=CARTESIAN_POINT ( 'NONE',  ( 115.6249999999998295, -1.767766952966376426, -1.767766952966320915 ) ) ;
#8410=CARTESIAN_POINT ( 'NONE',  ( 106.1488248654049187, -2.000000000000001776, 0.8284271247463557142 ) ) ;
#8420=CARTESIAN_POINT ( 'NONE',  ( 109.8752832217622739, -1.849990392679468076, 1.110223024625156540E-13 ) ) ;
#8437=FILL_AREA_STYLE ('',( #901 ) ) ;
#8440=CARTESIAN_POINT ( 'NONE',  ( 107.6636751345946692, -1.414213562373173305, 1.414213562373145550 ) ) ;
#8447=CARTESIAN_POINT ( 'NONE',  ( 117.0002832217621602, -1.308140751793557266, -1.308140751793529510 ) ) ;
#8449=AXIS2_PLACEMENT_3D ( 'NONE', #10835, #17436, #29371 ) ;
#8451=CARTESIAN_POINT ( 'NONE',  ( 104.1247167782375556, -1.849990392679468076, 0.000000000000000000 ) ) ;
#8457=ORIENTED_EDGE ( 'NONE', *, *, #24672, .F. ) ;
#8463=CARTESIAN_POINT ( 'NONE',  ( 115.1872167782374987, -1.849990392679441875, -0.7662911109075283278 ) ) ;
#8468=CARTESIAN_POINT ( 'NONE',  ( 112.9374999999997726, 2.500000000000115019, -1.035533905932448873 ) ) ;
#8478=DIRECTION ( 'NONE',  ( -1.000000000000000000, -1.665334536937736783E-16, -2.220446049250315546E-16 ) ) ;
#8495=CARTESIAN_POINT ( 'NONE',  ( 107.9999999999998863, 2.500000000000002220, 0.000000000000000000 ) ) ;
#8502=ORIENTED_EDGE ( 'NONE', *, *, #16577, .F. ) ;
#8508=EDGE_CURVE ( 'NONE', #19788, #18908, #7582, .T. ) ;
#8512=CARTESIAN_POINT ( 'NONE',  ( 106.2113248654051745, -1.999999999999946265, 0.000000000000000000 ) ) ;
#8514=CARTESIAN_POINT ( 'NONE',  ( 110.6636751345946976, -1.414213562373090038, 1.414213562373034527 ) ) ;
#8532=CARTESIAN_POINT ( 'NONE',  ( 111.7738248654051745, 2.000000000000061728, 0.8284271247463557142 ) ) ;
#8535=ORIENTED_EDGE ( 'NONE', *, *, #2677, .F. ) ;
#8539=CARTESIAN_POINT ( 'NONE',  ( 116.6252832217622313, 0.000000000000000000, 1.849990392679523588 ) ) ;
#8559=CARTESIAN_POINT ( 'NONE',  ( 115.7499999999998153, -1.110223024625156540E-13, -2.499999999999946709 ) ) ;
#8569=CARTESIAN_POINT ( 'NONE',  ( 115.3749999999999574, -1.767766952966320915, 1.767766952966431937 ) ) ;
#8593=( NAMED_UNIT ( * ) PLANE_ANGLE_UNIT ( ) SI_UNIT ( $, .RADIAN. ) );
#8599=CARTESIAN_POINT ( 'NONE',  ( 111.9377832217620465, -1.849990392679441875, -0.7662911109075883909 ) ) ;
#8607=CARTESIAN_POINT ( 'NONE',  ( 104.7401757384973990, -1.393188515088598312, -1.223208600277094993 ) ) ;
#8614=CARTESIAN_POINT ( 'NONE',  ( 113.4372167782374277, 0.7662911109077987781, -1.849990392679291551 ) ) ;
#8620=CARTESIAN_POINT ( 'NONE',  ( 104.7401757384974275, 1.849990392679526918, 0.1116904995936761485 ) ) ;
#8622=DIRECTION ( 'NONE',  ( -1.000000000000000000, -1.665334536937736783E-16, -2.220446049250315546E-16 ) ) ;
#8647=CARTESIAN_POINT ( 'NONE',  ( 1.110223024625164183E-16, -2.000000000000012879, -1.776356839400262692E-15 ) ) ;
#8654=CARTESIAN_POINT ( 'NONE',  ( 108.4374999999998863, -2.499999999999934719, 1.035533905932929599 ) ) ;
#8661=CYLINDRICAL_SURFACE ( 'NONE', #8700, 2.000000000000012879 ) ;
#8666=EDGE_LOOP ( 'NONE', ( #14150, #20737, #18158, #24900 ) ) ;
#8672=( BOUNDED_CURVE ( )  B_SPLINE_CURVE ( 2, ( #5116, #7295, #14536, #21433, #8138, #26020, #15089, #19689, #2525 ),
 .UNSPECIFIED., .F., .T. ) 
 B_SPLINE_CURVE_WITH_KNOTS ( ( 3, 2, 2, 2, 3 ),
 ( 0.2058823529411765163, 0.2132352941176470784, 0.2205882352941176405, 0.2279411764705882026, 0.2352941176470587648 ),
 .UNSPECIFIED. ) 
 CURVE ( )  GEOMETRIC_REPRESENTATION_ITEM ( )  RATIONAL_B_SPLINE_CURVE ( ( 1.000000000000000000, 0.9238795325112867385, 1.000000000000000000, 0.9238795325112867385, 1.000000000000000000, 0.9238795325112867385, 1.000000000000000000, 0.9238795325112867385, 1.000000000000000000 ) ) 
 REPRESENTATION_ITEM ( '' )  );
#8676=CARTESIAN_POINT ( 'NONE',  ( 121.1877832217620750, 0.7662911109077987781, -1.849990392679291551 ) ) ;
#8700=AXIS2_PLACEMENT_3D ( 'NONE', #11134, #20485, #23112 ) ;
#8701=CARTESIAN_POINT ( 'NONE',  ( 116.3127832217621034, 1.849990392679532247, -0.7662911109075883909 ) ) ;
#8708=CYLINDRICAL_SURFACE ( 'NONE', #11140, 2.000000000000012879 ) ;
#8720=CARTESIAN_POINT ( 'NONE',  ( 117.2499999999998721, 0.000000000000000000, 2.499999999999946709 ) ) ;
#8731=CARTESIAN_POINT ( 'NONE',  ( 118.2499999999997584, -8.326672684688674053E-14, 2.500000000000057732 ) ) ;
#8734=CARTESIAN_POINT ( 'NONE',  ( 110.6877832217622739, -0.7662911109076785410, 1.849990392679712103 ) ) ;
#8742=CARTESIAN_POINT ( 'NONE',  ( 106.7738248654051603, 2.000000000000061728, 0.8284271247464157772 ) ) ;
#8744=VECTOR ( 'NONE', #2665, 1000.000000000000000 ) ;
#8762=CARTESIAN_POINT ( 'NONE',  ( 111.8752832217622881, -1.849990392679579099, 1.110223024625156540E-13 ) ) ;
#8780=CARTESIAN_POINT ( 'NONE',  ( 109.2497167782375413, -1.308140751793585022, -1.308140751793640533 ) ) ;
#8785=CARTESIAN_POINT ( 'NONE',  ( 113.7113248654051034, 2.000000000000057288, 0.000000000000000000 ) ) ;
#8786=ORIENTED_EDGE ( 'NONE', *, *, #22255, .T. ) ;
#8788=CARTESIAN_POINT ( 'NONE',  ( 105.9136751345946976, -1.414213562373145550, -1.414213562373034527 ) ) ;
#8795=CARTESIAN_POINT ( 'NONE',  ( 117.3511751345945981, 2.000000000000061728, 0.8284271247463557142 ) ) ;
#8816=CARTESIAN_POINT ( 'NONE',  ( 120.4372167782375271, 0.7662911109078588412, -1.849990392679291551 ) ) ;
#8833=CARTESIAN_POINT ( 'NONE',  ( 113.1011751345946266, 0.8284271247462654530, -1.999999999999791278 ) ) ;
#8857=CARTESIAN_POINT ( 'NONE',  ( 118.1877832217622029, 0.7662911109078588412, -1.849990392679351725 ) ) ;
#8861=( BOUNDED_CURVE ( )  B_SPLINE_CURVE ( 2, ( #25483, #23516, #4599, #6907, #20594, #7214, #18460, #25648, #14179 ),
 .UNSPECIFIED., .F., .T. ) 
 B_SPLINE_CURVE_WITH_KNOTS ( ( 3, 2, 2, 2, 3 ),
 ( 0.5588235294117647189, 0.5661764705882352811, 0.5735294117647058432, 0.5808823529411764053, 0.5882352941176470784 ),
 .UNSPECIFIED. ) 
 CURVE ( )  GEOMETRIC_REPRESENTATION_ITEM ( )  RATIONAL_B_SPLINE_CURVE ( ( 1.000000000000000000, 0.9238795325112867385, 1.000000000000000000, 0.9238795325112867385, 1.000000000000000000, 0.9238795325112867385, 1.000000000000000000, 0.9238795325112867385, 1.000000000000000000 ) ) 
 REPRESENTATION_ITEM ( '' )  );
#8873=DIRECTION ( 'NONE',  ( -1.000000000000000000, -1.665334536937736783E-16, -2.220446049250315546E-16 ) ) ;
#8876=CARTESIAN_POINT ( 'NONE',  ( 117.4999999999999574, -2.499999999999891198, 0.000000000000000000 ) ) ;
#8886=CARTESIAN_POINT ( 'NONE',  ( 115.7499999999998153, -1.110223024625156540E-13, -2.499999999999946709 ) ) ;
#8887=CARTESIAN_POINT ( 'NONE',  ( 112.0627832217620750, -0.7662911109077388261, -1.849990392679231599 ) ) ;
#8895=ORIENTED_EDGE ( 'NONE', *, *, #17918, .T. ) ;
#8914=CARTESIAN_POINT ( 'NONE',  ( 111.8127832217621460, -1.849990392679441875, 0.7662911109079489913 ) ) ;
#8921=EDGE_CURVE ( 'NONE', #27307, #7379, #17809, .T. ) ;
#8931=CARTESIAN_POINT ( 'NONE',  ( 108.9372167782374987, -0.7662911109077087390, 1.849990392679591977 ) ) ;
#8933=CARTESIAN_POINT ( 'NONE',  ( 112.8747167782376124, 2.775557561562891351E-14, 1.849990392679634610 ) ) ;
#8937=CARTESIAN_POINT ( 'NONE',  ( 110.2113248654050608, -1.999999999999946265, 0.000000000000000000 ) ) ;
#8955=CARTESIAN_POINT ( 'NONE',  ( 111.4374999999997300, -2.499999999999904521, 1.035533905932869425 ) ) ;
#8968=CARTESIAN_POINT ( 'NONE',  ( 104.7499999999998295, 5.551115123125782702E-14, -2.499999999999835687 ) ) ;
#8983=CARTESIAN_POINT ( 'NONE',  ( 113.0386751345947687, 0.000000000000000000, -1.999999999999890754 ) ) ;
#8984=CARTESIAN_POINT ( 'NONE',  ( 118.5002832217622171, 1.308140751793723799, 1.308140751793862577 ) ) ;
#9002=CARTESIAN_POINT ( 'NONE',  ( 116.1872167782374987, -1.849990392679532247, -0.7662911109077087390 ) ) ;
#9003=CARTESIAN_POINT ( 'NONE',  ( 101.5358983848621932, 1.203706215242021998E-32, 1.069105884036878258E-47 ) ) ;
#9007=CARTESIAN_POINT ( 'NONE',  ( 116.0002832217622171, -1.308140751793585022, -1.308140751793640533 ) ) ;
#9017=CARTESIAN_POINT ( 'NONE',  ( 0.000000000000000000, 0.000000000000000000, 0.000000000000000000 ) ) ;
#9024=CARTESIAN_POINT ( 'NONE',  ( 116.9374999999998295, 2.500000000000024425, -1.035533905932629173 ) ) ;
#9033=CARTESIAN_POINT ( 'NONE',  ( 116.1249999999999574, 1.767766952966265404, 1.767766952966431937 ) ) ;
#9035=CARTESIAN_POINT ( 'NONE',  ( 108.3752832217622739, 1.849990392679523588, 0.000000000000000000 ) ) ;
#9059=CARTESIAN_POINT ( 'NONE',  ( 111.5627832217621744, 0.7662911109078588412, 1.849990392679712103 ) ) ;
#9070=CARTESIAN_POINT ( 'NONE',  ( -1.110223024625164676E-16, 2.000000000000012879, 2.021286199229734960E-15 ) ) ;
#9073=CARTESIAN_POINT ( 'NONE',  ( 110.6247167782374987, 1.849990392679551343, 0.000000000000000000 ) ) ;
#9075=CARTESIAN_POINT ( 'NONE',  ( 111.3122167782374277, -0.7662911109076785410, -1.849990392679291551 ) ) ;
#9079=CARTESIAN_POINT ( 'NONE',  ( 110.7113248654050182, 2.000000000000057288, 0.000000000000000000 ) ) ;
#9093=CARTESIAN_POINT ( 'NONE',  ( 111.7886751345948255, -1.999999999999974021, 0.000000000000000000 ) ) ;
#9098=CARTESIAN_POINT ( 'NONE',  ( 109.8124999999997868, 1.035533905932779275, -2.499999999999784173 ) ) ;
#9105=EDGE_LOOP ( 'NONE', ( #9735, #24788, #5949, #7998 ) ) ;
#9110=ORIENTED_EDGE ( 'NONE', *, *, #16274, .T. ) ;
#9111=CARTESIAN_POINT ( 'NONE',  ( 106.9999999999999716, 2.500000000000030198, 0.000000000000000000 ) ) ;
#9131=CARTESIAN_POINT ( 'NONE',  ( 119.1877832217621034, 0.7662911109078588412, -1.849990392679411677 ) ) ;
#9155=CARTESIAN_POINT ( 'NONE',  ( 113.7502832217623023, -1.308140751793585022, 1.308140751793640533 ) ) ;
#9157=ORIENTED_EDGE ( 'NONE', *, *, #1011, .T. ) ;
#9172=CARTESIAN_POINT ( 'NONE',  ( 113.1874999999998295, 1.035533905932779275, 2.500000000000205169 ) ) ;
#9182=CARTESIAN_POINT ( 'NONE',  ( 117.1249999999999432, 1.767766952966320915, 1.767766952966431937 ) ) ;
#9185=CARTESIAN_POINT ( 'NONE',  ( 105.6252832217623592, 0.000000000000000000, 1.849990392679523588 ) ) ;
#9190=AXIS2_PLACEMENT_3D ( 'NONE', #17704, #22451, #22605 ) ;
#9207=DIRECTION ( 'NONE',  ( -1.000000000000000000, -1.665334536937736783E-16, -2.220446049250315546E-16 ) ) ;
#9208=CARTESIAN_POINT ( 'NONE',  ( 112.3988248654050039, -0.8284271247461453269, -1.999999999999731104 ) ) ;
#9210=CARTESIAN_POINT ( 'NONE',  ( 112.1877832217621886, 0.7662911109079189043, -1.849990392679291551 ) ) ;
#9216=CARTESIAN_POINT ( 'NONE',  ( 118.2113248654050466, -1.999999999999946265, 2.220446049250313081E-13 ) ) ;
#9226=CARTESIAN_POINT ( 'NONE',  ( 110.4372167782375840, 0.7662911109078888172, -1.849990392679231599 ) ) ;
#9249=CARTESIAN_POINT ( 'NONE',  ( 111.8749999999998437, 1.767766952966348670, -1.767766952966209892 ) ) ;
#9259=EDGE_CURVE ( 'NONE', #283, #7046, #11959, .T. ) ;
#9264=CARTESIAN_POINT ( 'NONE',  ( 106.6874999999998010, -1.035533905932689347, -2.499999999999784173 ) ) ;
#9280=CARTESIAN_POINT ( 'NONE',  ( 105.8747167782375271, -2.775557561562891351E-14, 1.849990392679523588 ) ) ;
#9282=CARTESIAN_POINT ( 'NONE',  ( 118.1252832217622881, -2.775557561562891351E-14, -1.849990392679523588 ) ) ;
#9303=CARTESIAN_POINT ( 'NONE',  ( 117.1872167782373708, -1.849990392679441875, -0.7662911109077087390 ) ) ;
#9309=CARTESIAN_POINT ( 'NONE',  ( 113.1877832217620892, 0.7662911109079189043, -1.849990392679291551 ) ) ;
#9329=CARTESIAN_POINT ( 'NONE',  ( 110.9374999999997442, 2.500000000000055067, -1.035533905932388699 ) ) ;
#9339=CARTESIAN_POINT ( 'NONE',  ( 114.4999999999998721, -2.499999999999891198, 0.000000000000000000 ) ) ;
#9341=CARTESIAN_POINT ( 'NONE',  ( 106.8752832217622739, -1.849990392679301543, 2.220446049250313081E-13 ) ) ;
#9346=CARTESIAN_POINT ( 'NONE',  ( 106.3122167782376124, -0.7662911109076184779, -1.849990392679351725 ) ) ;
#9359=CARTESIAN_POINT ( 'NONE',  ( 107.4999999999999716, -2.499999999999891198, 3.330669073875469621E-13 ) ) ;
#9365=CARTESIAN_POINT ( 'NONE',  ( 107.5002832217622881, 1.308140751793585022, 1.308140751793751555 ) ) ;
#9372=VECTOR ( 'NONE', #18872, 1000.000000000000000 ) ;
#9380=CARTESIAN_POINT ( 'NONE',  ( 110.9372167782374277, -0.7662911109077686911, 1.849990392679591977 ) ) ;
#9403=CARTESIAN_POINT ( 'NONE',  ( 112.1011751345946124, 0.8284271247463257382, -1.999999999999851674 ) ) ;
#9408=CARTESIAN_POINT ( 'NONE',  ( 109.2113248654051745, -1.999999999999946265, 0.000000000000000000 ) ) ;
#9409=CARTESIAN_POINT ( 'NONE',  ( 111.2499999999999432, -1.110223024625156540E-13, 2.500000000000057732 ) ) ;
#9413=ORIENTED_EDGE ( 'NONE', *, *, #19386, .T. ) ;
#9420=CARTESIAN_POINT ( 'NONE',  ( 106.8124999999997016, 1.035533905932749299, -2.499999999999784173 ) ) ;
#9425=CARTESIAN_POINT ( 'NONE',  ( 117.0624999999998579, 2.500000000000234479, 1.035533905932989551 ) ) ;
#9431=DIRECTION ( 'NONE',  ( -1.000000000000000000, -1.665334536937736783E-16, -2.220446049250315546E-16 ) ) ;
#9436=CARTESIAN_POINT ( 'NONE',  ( 108.9761751345945697, -0.8284271247461453269, -1.999999999999791278 ) ) ;
#9441=CARTESIAN_POINT ( 'NONE',  ( 106.0622167782373708, -1.849990392679441875, 0.7662911109080090544 ) ) ;
#9444=CARTESIAN_POINT ( 'NONE',  ( 117.8127832217621744, -1.849990392679501827, 0.7662911109078287542 ) ) ;
#9461=CARTESIAN_POINT ( 'NONE',  ( 117.3122167782375840, -0.7662911109077388261, -1.849990392679351725 ) ) ;
#9486=CARTESIAN_POINT ( 'NONE',  ( 111.3749999999999289, -1.767766952966320915, 1.767766952966431937 ) ) ;
#9499=CARTESIAN_POINT ( 'NONE',  ( 105.3752832217622739, 1.849990392679523588, 0.000000000000000000 ) ) ;
#9519=CARTESIAN_POINT ( 'NONE',  ( 108.8749999999999574, 1.767766952966265404, -1.767766952966320915 ) ) ;
#9525=CARTESIAN_POINT ( 'NONE',  ( 107.8752832217621602, -1.849990392679329299, 3.330669073875469621E-13 ) ) ;
#9531=ORIENTED_EDGE ( 'NONE', *, *, #25322, .F. ) ;
#9543=LINE ( 'NONE', #7378, #14301 ) ;
#9560=CARTESIAN_POINT ( 'NONE',  ( -3.330669073875475045E-16, 6.000000000000005329, 6.063858597689169383E-15 ) ) ;
#9562=CARTESIAN_POINT ( 'NONE',  ( 109.5624999999997016, -2.499999999999994671, -1.035533905932508825 ) ) ;
#9563=CARTESIAN_POINT ( 'NONE',  ( 115.1636751345947545, 1.414213562373145550, -1.414213562372812483 ) ) ;
#9571=CARTESIAN_POINT ( 'NONE',  ( 117.7497167782374987, 1.308140751793723799, 1.308140751793640533 ) ) ;
#9578=CARTESIAN_POINT ( 'NONE',  ( 119.1874999999998010, 1.035533905932779275, 2.500000000000205169 ) ) ;
#9582=VERTEX_POINT ( 'NONE', #7565 ) ;
#9590=CARTESIAN_POINT ( 'NONE',  ( 104.4997167782375413, 1.308140751793668288, -1.308140751793640533 ) ) ;
#9593=CARTESIAN_POINT ( 'NONE',  ( 118.0627832217622455, -0.7662911109076485650, -1.849990392679171425 ) ) ;
#9609=CARTESIAN_POINT ( 'NONE',  ( 117.4997167782374987, 1.308140751793696044, -1.308140751793640533 ) ) ;
#9611=ADVANCED_FACE ( 'NONE', ( #16546 ), #12235, .F. ) ;
#9625=CARTESIAN_POINT ( 'NONE',  ( 0.000000000000000000, 0.000000000000000000, 0.000000000000000000 ) ) ;
#9631=CARTESIAN_POINT ( 'NONE',  ( 111.1874999999999858, 1.035533905932749299, 2.500000000000265121 ) ) ;
#9644=CARTESIAN_POINT ( 'NONE',  ( 113.4999999999999147, -2.499999999999919176, 0.000000000000000000 ) ) ;
#9645=CARTESIAN_POINT ( 'NONE',  ( 112.2113248654051176, -1.999999999999946265, 0.000000000000000000 ) ) ;
#9646=CARTESIAN_POINT ( 'NONE',  ( 108.2502832217622029, 1.308140751793640533, -1.308140751793640533 ) ) ;
#9662=ORIENTED_EDGE ( 'NONE', *, *, #23072, .T. ) ;
#9664=CARTESIAN_POINT ( 'NONE',  ( 106.4999999999999147, -2.499999999999946709, 1.110223024625156540E-13 ) ) ;
#9671=CARTESIAN_POINT ( 'NONE',  ( 107.8127832217621318, -1.849990392679472073, 0.7662911109079489913 ) ) ;
#9687=AXIS2_PLACEMENT_3D ( 'NONE', #1083, #10475, #17399 ) ;
#9690=ORIENTED_EDGE ( 'NONE', *, *, #2161, .F. ) ;
#9714=CARTESIAN_POINT ( 'NONE',  ( 107.6249999999998721, -1.767766952966376426, -1.767766952966320915 ) ) ;
#9727=CARTESIAN_POINT ( 'NONE',  ( 115.9997167782376266, -1.308140751793668288, 1.308140751793751555 ) ) ;
#9735=ORIENTED_EDGE ( 'NONE', *, *, #11335, .F. ) ;
#9742=CARTESIAN_POINT ( 'NONE',  ( 105.3747167782376550, -5.551115123125782702E-14, -1.849990392679523588 ) ) ;
#9743=CARTESIAN_POINT ( 'NONE',  ( 119.7886751345947829, -1.999999999999946265, 3.330669073875469621E-13 ) ) ;
#9745=CARTESIAN_POINT ( 'NONE',  ( 113.5002832217622455, 1.308140751793696044, 1.308140751793640533 ) ) ;
#9746=EDGE_CURVE ( 'NONE', #28423, #23930, #6611, .T. ) ;
#9758=CARTESIAN_POINT ( 'NONE',  ( 0.000000000000000000, 0.000000000000000000, 0.000000000000000000 ) ) ;
#9763=CARTESIAN_POINT ( 'NONE',  ( 118.9761751345946266, -0.8284271247460250898, -1.999999999999851674 ) ) ;
#9764=CARTESIAN_POINT ( 'NONE',  ( 113.0002832217622455, -1.308140751793585022, -1.308140751793640533 ) ) ;
#9767=COLOUR_RGB ( '', 0.40784314, 0.44705882, 0.49803922) ;
#9784=CARTESIAN_POINT ( 'NONE',  ( 112.2499999999998153, -5.551115123125782702E-14, 2.500000000000168754 ) ) ;
#9791=CARTESIAN_POINT ( 'NONE',  ( 112.0624999999997868, 2.500000000000055067, 1.035533905932989551 ) ) ;
#9794=CARTESIAN_POINT ( 'NONE',  ( 112.8988248654050892, 0.8284271247463257382, 2.000000000000271783 ) ) ;
#9798=CARTESIAN_POINT ( 'NONE',  ( 107.3122167782375413, -0.7662911109077087390, -1.849990392679291551 ) ) ;
#9803=EDGE_CURVE ( 'NONE', #10990, #13661, #7298, .T. ) ;
#9811=CARTESIAN_POINT ( 'NONE',  ( 109.5624999999997158, -2.499999999999994671, -1.035533905932508825 ) ) ;
#9819=CARTESIAN_POINT ( 'NONE',  ( 109.6877832217621318, -0.7662911109076485650, 1.849990392679652151 ) ) ;
#9824=FACE_OUTER_BOUND ( 'NONE', #21597, .T. ) ;
#9834=CARTESIAN_POINT ( 'NONE',  ( 111.4761751345947260, 0.8284271247462354770, 2.000000000000212275 ) ) ;
#9864=CARTESIAN_POINT ( 'NONE',  ( 109.1488248654050750, -1.999999999999941602, 0.8284271247463557142 ) ) ;
#9865=CARTESIAN_POINT ( 'NONE',  ( 106.7499999999999147, -8.326672684688674053E-14, -2.499999999999946709 ) ) ;
#9866=B_SPLINE_CURVE_WITH_KNOTS ( 'NONE', 3,
 ( #24267, #21695, #10015, #26277, #19393, #26710, #918, #2778, #7833, #6150, #4139, #27472, #15877, #13561, #24735, #5825, #15566, #29172, #18015, #8607, #3833, #1844, #6297, #8133, #1219, #10630 ),
 .UNSPECIFIED., .F., .F.,
 ( 4, 2, 2, 2, 2, 2, 2, 2, 2, 2, 2, 2, 4 ),
 ( 0.001330568787003978985, 0.001691992223416138690, 0.002053415659828298177, 0.002776262532652618020, 0.003499109405476936996, 0.003860532841889096484, 0.004221956278301255971, 0.004583379714713415459, 0.004944803151125575814, 0.005667650023949893923, 0.006029073460362054278, 0.006390496896774213766, 0.007113343769598531874 ),
 .UNSPECIFIED. ) ;
#9873=ORIENTED_EDGE ( 'NONE', *, *, #1725, .F. ) ;
#9874=CARTESIAN_POINT ( 'NONE',  ( 115.6872167782374561, 1.849990392679532247, 0.7662911109080692285 ) ) ;
#9880=CARTESIAN_POINT ( 'NONE',  ( 117.9999999999997868, 2.500000000000002220, 2.220446049250313081E-13 ) ) ;
#9886=EDGE_LOOP ( 'NONE', ( #6838, #29262, #13298, #27995 ) ) ;
#9893=DIRECTION ( 'NONE',  ( -1.000000000000000000, -1.665334536937736783E-16, -2.220446049250315546E-16 ) ) ;
#9895=CARTESIAN_POINT ( 'NONE',  ( 105.1872167782375556, -1.849990392679441875, -0.7662911109075883909 ) ) ;
#9898=CARTESIAN_POINT ( 'NONE',  ( 116.3752832217622597, 1.849990392679523588, 0.000000000000000000 ) ) ;
#9911=CARTESIAN_POINT ( 'NONE',  ( 115.9372167782375129, -0.7662911109076785410, 1.849990392679712103 ) ) ;
#9913=ORIENTED_EDGE ( 'NONE', *, *, #30074, .F. ) ;
#9915=CARTESIAN_POINT ( 'NONE',  ( 118.9136751345948113, -1.414213562373173305, -1.414213562373034527 ) ) ;
#9939=CARTESIAN_POINT ( 'NONE',  ( 115.6011751345946550, -0.8284271247461453269, 2.000000000000332179 ) ) ;
#9943=CARTESIAN_POINT ( 'NONE',  ( 107.2886751345947118, 2.000000000000085265, 1.110223024625156540E-13 ) ) ;
#9945=CARTESIAN_POINT ( 'NONE',  ( 113.0624999999997726, 2.500000000000084821, 1.035533905932989551 ) ) ;
#9947=CARTESIAN_POINT ( 'NONE',  ( 113.0238248654049613, -0.8284271247460852639, 2.000000000000271783 ) ) ;
#9951=CARTESIAN_POINT ( 'NONE',  ( 121.1252832217622597, -5.551115123125782702E-14, -1.849990392679523588 ) ) ;
#9963=CARTESIAN_POINT ( 'NONE',  ( 109.6874999999997868, -1.035533905932659149, -2.499999999999724221 ) ) ;
#9971=CARTESIAN_POINT ( 'NONE',  ( 120.7499999999998721, 1.110223024625156540E-13, -2.499999999999946709 ) ) ;
#9991=ORIENTED_EDGE ( 'NONE', *, *, #20556, .F. ) ;
#9993=ADVANCED_FACE ( 'NONE', ( #9824 ), #15040, .F. ) ;
#9996=DIRECTION ( 'NONE',  ( -1.000000000000000000, -1.665334536937736783E-16, -2.220446049250315546E-16 ) ) ;
#10012=CARTESIAN_POINT ( 'NONE',  ( 107.4999999999999716, -2.499999999999891198, 3.330669073875469621E-13 ) ) ;
#10014=CARTESIAN_POINT ( 'NONE',  ( 108.6488248654049045, 2.000000000000061728, -0.8284271247459350507 ) ) ;
#10015=CARTESIAN_POINT ( 'NONE',  ( 104.7401757384974132, 1.838163912978949099, -0.2412767149991470184 ) ) ;
#10018=CARTESIAN_POINT ( 'NONE',  ( 108.1636751345946976, 1.414213562373145550, -1.414213562373034527 ) ) ;
#10022=CARTESIAN_POINT ( 'NONE',  ( 116.3747167782375840, 5.551115123125782702E-14, -1.849990392679190521 ) ) ;
#10023=CARTESIAN_POINT ( 'NONE',  ( 118.5386751345946124, 8.326672684688674053E-14, 2.000000000000112799 ) ) ;
#10029=CARTESIAN_POINT ( 'NONE',  ( 118.0624999999997868, 2.500000000000054623, 1.035533905932929599 ) ) ;
#10045=CARTESIAN_POINT ( 'NONE',  ( 114.8127832217620465, -1.849990392679591977, 0.7662911109078888172 ) ) ;
#10063=CARTESIAN_POINT ( 'NONE',  ( 115.0622167782373850, -1.849990392679411677, 0.7662911109078888172 ) ) ;
#10066=ADVANCED_FACE ( 'NONE', ( #29602 ), #17967, .F. ) ;
#10070=CARTESIAN_POINT ( 'NONE',  ( 104.9172689374427279, 0.2127325526458908322, 1.948528123138198120 ) ) ;
#10083=( NAMED_UNIT ( * ) PLANE_ANGLE_UNIT ( ) SI_UNIT ( $, .RADIAN. ) );
#10087=CARTESIAN_POINT ( 'NONE',  ( 117.1011751345945981, 0.8284271247463257382, -1.999999999999731104 ) ) ;
#10092=CARTESIAN_POINT ( 'NONE',  ( 115.3511751345947403, 2.000000000000122125, 0.8284271247462955401 ) ) ;
#10097=CARTESIAN_POINT ( 'NONE',  ( 108.8124999999997442, 1.035533905932839449, -2.499999999999964473 ) ) ;
#10100=VERTEX_POINT ( 'NONE', #22706 ) ;
#10104=CARTESIAN_POINT ( 'NONE',  ( 119.2502832217621886, 1.308140751793612777, -1.308140751793418488 ) ) ;
#10115=CARTESIAN_POINT ( 'NONE',  ( 105.7499999999998010, 1.110223024625156540E-13, -2.499999999999946709 ) ) ;
#10124=CARTESIAN_POINT ( 'NONE',  ( 105.5002832217622313, 1.308140751793696044, 1.308140751793640533 ) ) ;
#10126=DIRECTION ( 'NONE',  ( -1.000000000000000000, -1.665334536937736783E-16, -2.220446049250315546E-16 ) ) ;
#10133=EDGE_CURVE ( 'NONE', #6908, #16270, #23674, .T. ) ;
#10139=CARTESIAN_POINT ( 'NONE',  ( 119.9374999999996874, 2.500000000000114575, -1.035533905932388699 ) ) ;
#10146=VERTEX_POINT ( 'NONE', #11201 ) ;
#10163=CARTESIAN_POINT ( 'NONE',  ( 106.1874999999999147, 1.035533905932839227, 2.500000000000265121 ) ) ;
#10173=CARTESIAN_POINT ( 'NONE',  ( 112.7886751345947403, -1.999999999999946265, 0.000000000000000000 ) ) ;
#10176=CARTESIAN_POINT ( 'NONE',  ( 117.2497167782375129, -1.308140751793585022, -1.308140751793640533 ) ) ;
#10180=CARTESIAN_POINT ( 'NONE',  ( 115.8124999999997584, 1.035533905932719101, -2.499999999999784173 ) ) ;
#10196=DIRECTION ( 'NONE',  ( -3.845925372767118265E-16, 1.000000000000000000, 8.881784197001258240E-16 ) ) ;
#10218=CARTESIAN_POINT ( 'NONE',  ( 114.9372167782374135, -0.7662911109077987781, 1.849990392679591977 ) ) ;
#10223=CARTESIAN_POINT ( 'NONE',  ( 104.9999999999999716, -0.4876318259226519736, 1.939643060552054266 ) ) ;
#10253=ORIENTED_EDGE ( 'NONE', *, *, #16311, .F. ) ;
#10254=CARTESIAN_POINT ( 'NONE',  ( 117.7113248654050466, 2.000000000000085265, 0.000000000000000000 ) ) ;
#10266=CARTESIAN_POINT ( 'NONE',  ( 105.9374999999997584, 2.500000000000144773, -1.035533905932568777 ) ) ;
#10275=CARTESIAN_POINT ( 'NONE',  ( 120.8749999999998863, 1.767766952966348670, -1.767766952966209892 ) ) ;
#10292=( BOUNDED_CURVE ( )  B_SPLINE_CURVE ( 2, ( #2933, #19984, #3221, #29177, #21990, #17553, #14935, #22142, #10173 ),
 .UNSPECIFIED., .F., .T. ) 
 B_SPLINE_CURVE_WITH_KNOTS ( ( 3, 2, 2, 2, 3 ),
 ( 0.4411764705882352811, 0.4485294117647058432, 0.4558823529411765163, 0.4632352941176470784, 0.4705882352941176405 ),
 .UNSPECIFIED. ) 
 CURVE ( )  GEOMETRIC_REPRESENTATION_ITEM ( )  RATIONAL_B_SPLINE_CURVE ( ( 1.000000000000000000, 0.9238795325112867385, 1.000000000000000000, 0.9238795325112867385, 1.000000000000000000, 0.9238795325112867385, 1.000000000000000000, 0.9238795325112867385, 1.000000000000000000 ) ) 
 REPRESENTATION_ITEM ( '' )  );
#10312=CARTESIAN_POINT ( 'NONE',  ( 105.5624999999997726, -2.499999999999874767, -1.035533905932568999 ) ) ;
#10325=CARTESIAN_POINT ( 'NONE',  ( 112.6872167782374419, 1.849990392679621953, 0.7662911109081291805 ) ) ;
#10331=CARTESIAN_POINT ( 'NONE',  ( 114.8124999999998010, 1.035533905932749299, -2.499999999999844569 ) ) ;
#10334=COLOUR_RGB ( '', 0.40784314, 0.44705882, 0.49803922) ;
#10378=AXIS2_PLACEMENT_3D ( 'NONE', #28747, #10499, #19851 ) ;
#10379=CARTESIAN_POINT ( 'NONE',  ( 119.9999999999998579, 1.183822024857545507, 1.888846423990942158 ) ) ;
#10406=CARTESIAN_POINT ( 'NONE',  ( 119.9377832217623023, -1.849990392679501827, -0.7662911109076485650 ) ) ;
#10409=EDGE_CURVE ( 'NONE', #15581, #13661, #27757, .T. ) ;
#10417=CARTESIAN_POINT ( 'NONE',  ( 105.2499999999999147, -2.775557561562891351E-14, 2.499999999999946709 ) ) ;
#10421=CARTESIAN_POINT ( 'NONE',  ( 116.2886751345946124, 2.000000000000168310, 3.330669073875469621E-13 ) ) ;
#10423=CARTESIAN_POINT ( 'NONE',  ( 118.7113248654050750, 1.999999999999946265, 1.110223024625156540E-13 ) ) ;
#10425=CARTESIAN_POINT ( 'NONE',  ( 105.0002832217622029, -1.308140751793612777, -1.308140751793640533 ) ) ;
#10437=CARTESIAN_POINT ( 'NONE',  ( 119.4374999999997868, -2.499999999999994671, 1.035533905932809473 ) ) ;
#10453=SURFACE_STYLE_USAGE ( .BOTH. , #15391 ) ;
#10467=CARTESIAN_POINT ( 'NONE',  ( 119.9999999999998010, 0.1805100831798492900, -2.088914846013065318 ) ) ;
#10475=DIRECTION ( 'NONE',  ( -1.000000000000000000, -1.665334536937736783E-16, -2.220446049250315546E-16 ) ) ;
#10479=CARTESIAN_POINT ( 'NONE',  ( 104.9470444944719532, -1.248719657643215575, -1.538360625296347095 ) ) ;
#10482=PRODUCT_DEFINITION ( 'UNKNOWN', '', #14906, #5097 ) ;
#10483=CARTESIAN_POINT ( 'NONE',  ( 114.8747167782375840, -5.551115123125782702E-14, 1.849990392679523588 ) ) ;
#10489=CARTESIAN_POINT ( 'NONE',  ( 112.5624999999998010, -2.499999999999994671, -1.035533905932689347 ) ) ;
#10499=DIRECTION ( 'NONE',  ( -1.000000000000000000, -1.665334536937736783E-16, -2.220446049250315546E-16 ) ) ;
#10503=CARTESIAN_POINT ( 'NONE',  ( 104.7401757384973280, -1.849990392679412565, 2.220446049250313081E-13 ) ) ;
#10516=CARTESIAN_POINT ( 'NONE',  ( 112.3747167782374703, -5.551115123125782702E-14, -1.849990392679523588 ) ) ;
#10520=ORIENTED_EDGE ( 'NONE', *, *, #27812, .T. ) ;
#10535=FILL_AREA_STYLE_COLOUR ( '', #18326 ) ;
#10555=CARTESIAN_POINT ( 'NONE',  ( 120.0627832217621602, -0.7662911109077388261, -1.849990392679291551 ) ) ;
#10566=CARTESIAN_POINT ( 'NONE',  ( 105.8749999999999574, 1.767766952966320915, -1.767766952966320915 ) ) ;
#10567=EDGE_CURVE ( 'NONE', #29332, #23925, #17431, .T. ) ;
#10570=ADVANCED_FACE ( 'NONE', ( #15447 ), #27365, .F. ) ;
#10576=CARTESIAN_POINT ( 'NONE',  ( 118.8363248654051176, 1.414213562373034527, 1.414213562373256572 ) ) ;
#10578=CARTESIAN_POINT ( 'NONE',  ( 119.6249999999999716, -1.767766952966404181, -1.767766952966320915 ) ) ;
#10592=CARTESIAN_POINT ( 'NONE',  ( 120.2499999999998721, -2.775557561562891351E-14, 2.500000000000168754 ) ) ;
#10593=CARTESIAN_POINT ( 'NONE',  ( 107.8363248654051034, 1.414213562373117794, 1.414213562373256572 ) ) ;
#10595=ORIENTED_EDGE ( 'NONE', *, *, #27230, .F. ) ;
#10600=CARTESIAN_POINT ( 'NONE',  ( 107.1488248654049897, -1.999999999999911626, 0.8284271247464157772 ) ) ;
#10604=ORIENTED_EDGE ( 'NONE', *, *, #2118, .T. ) ;
#10608=CARTESIAN_POINT ( 'NONE',  ( 107.2886751345947118, 2.000000000000085265, 1.110223024625156540E-13 ) ) ;
#10616=LINE ( 'NONE', #27458, #18752 ) ;
#10618=CARTESIAN_POINT ( 'NONE',  ( 114.0627832217621602, -0.7662911109077388261, -1.849990392679231599 ) ) ;
#10622=CARTESIAN_POINT ( 'NONE',  ( 119.7113248654050750, 2.000000000000001776, 1.110223024625156540E-13 ) ) ;
#10624=CARTESIAN_POINT ( 'NONE',  ( 119.9999999999999574, 2.481996037643088293, -0.1722232477815017759 ) ) ;
#10629=CARTESIAN_POINT ( 'NONE',  ( 108.3363248654050182, -1.414213562373201061, -1.414213562373034527 ) ) ;
#10630=CARTESIAN_POINT ( 'NONE',  ( 104.7401757384973280, -1.849990392679412565, 2.220446049250313081E-13 ) ) ;
#10637=CARTESIAN_POINT ( 'NONE',  ( 114.3747167782375556, -1.665334536937734811E-13, -1.849990392679523588 ) ) ;
#10642=CARTESIAN_POINT ( 'NONE',  ( 115.6249999999998295, -1.767766952966376426, -1.767766952966320915 ) ) ;
#10666=CARTESIAN_POINT ( 'NONE',  ( 105.4136751345947260, 1.414213562372979016, 1.414213562373256572 ) ) ;
#10667=CIRCLE ( 'NONE', #4280, 2.000000000000012879 ) ;
#10669=ORIENTED_EDGE ( 'NONE', *, *, #13440, .F. ) ;
#10675=CARTESIAN_POINT ( 'NONE',  ( 107.9374999999997726, 2.500000000000144773, -1.035533905932508825 ) ) ;
#10682=CARTESIAN_POINT ( 'NONE',  ( 112.3122167782374987, -0.7662911109076785410, -1.849990392679291551 ) ) ;
#10684=ORIENTED_EDGE ( 'NONE', *, *, #11178, .T. ) ;
#10726=CARTESIAN_POINT ( 'NONE',  ( 118.8752832217621460, -1.849990392679384810, 2.220446049250313081E-13 ) ) ;
#10733=ORIENTED_EDGE ( 'NONE', *, *, #25964, .T. ) ;
#10735=DIRECTION ( 'NONE',  ( -1.000000000000000000, -1.665334536937736783E-16, -2.220446049250315546E-16 ) ) ;
#10740=CARTESIAN_POINT ( 'NONE',  ( 1.110223024625164183E-16, -2.000000000000012879, -1.776356839400262692E-15 ) ) ;
#10745=CARTESIAN_POINT ( 'NONE',  ( 117.8749999999998010, 1.767766952966320915, -1.767766952966209892 ) ) ;
#10757=CARTESIAN_POINT ( 'NONE',  ( 109.2502832217621602, 1.308140751793751555, -1.308140751793640533 ) ) ;
#10761=CARTESIAN_POINT ( 'NONE',  ( 108.4997167782375982, 1.308140751793668288, -1.308140751793418488 ) ) ;
#10778=CARTESIAN_POINT ( 'NONE',  ( 107.4136751345947545, 1.414213562373201061, 1.414213562373256572 ) ) ;
#10785=CARTESIAN_POINT ( 'NONE',  ( 114.7502832217623592, -1.308140751793640533, 1.308140751793640533 ) ) ;
#10787=CARTESIAN_POINT ( 'NONE',  ( 119.4613248654050182, 5.551115123125782702E-14, -2.000000000000001776 ) ) ;
#10789=CARTESIAN_POINT ( 'NONE',  ( 107.7113248654050892, 2.000000000000057288, 0.000000000000000000 ) ) ;
#10799=CARTESIAN_POINT ( 'NONE',  ( 115.4997167782375129, 1.308140751793640533, -1.308140751793640533 ) ) ;
#10805=CARTESIAN_POINT ( 'NONE',  ( 114.8749999999998295, 1.767766952966320915, -1.767766952966209892 ) ) ;
#10816=DIRECTION ( 'NONE',  ( -1.000000000000000000, -1.665334536937736783E-16, -2.220446049250315546E-16 ) ) ;
#10818=CARTESIAN_POINT ( 'NONE',  ( 116.7113248654051318, 2.000000000000057288, 0.000000000000000000 ) ) ;
#10831=DIRECTION ( 'NONE',  ( 5.551115123125785167E-17, -1.000000000000000000, -8.881784197001256268E-16 ) ) ;
#10833=CARTESIAN_POINT ( 'NONE',  ( 110.3124999999998863, -1.035533905932659149, 2.500000000000144773 ) ) ;
#10835=CARTESIAN_POINT ( 'NONE',  ( 0.000000000000000000, 0.000000000000000000, 0.000000000000000000 ) ) ;
#10840=AXIS2_PLACEMENT_3D ( 'NONE', #20740, #27613, #7456 ) ;
#10843=EDGE_LOOP ( 'NONE', ( #440, #9413, #6572, #18053 ) ) ;
#10844=ADVANCED_FACE ( 'NONE', ( #922 ), #12495, .F. ) ;
#10857=PRODUCT_CONTEXT ( 'NONE', #27314, 'mechanical' ) ;
#10878=CARTESIAN_POINT ( 'NONE',  ( 117.6252832217623165, 0.000000000000000000, 1.849990392679523588 ) ) ;
#10879=DIRECTION ( 'NONE',  ( 1.000000000000000000, 1.665334536937736783E-16, 2.220446049250315546E-16 ) ) ;
#10896=CARTESIAN_POINT ( 'NONE',  ( 114.4374999999998010, -2.499999999999964473, 1.035533905932929599 ) ) ;
#10907=CARTESIAN_POINT ( 'NONE',  ( 115.6249999999998295, -1.767766952966376426, -1.767766952966320915 ) ) ;
#10908=CARTESIAN_POINT ( 'NONE',  ( 109.8127832217621034, -1.849990392679501827, 0.7662911109077686911 ) ) ;
#10941=CARTESIAN_POINT ( 'NONE',  ( 119.9999999999997158, 1.183822024845517351, -1.888846423996454860 ) ) ;
#10952=CARTESIAN_POINT ( 'NONE',  ( 113.9372167782373566, -0.7662911109077388261, 1.849990392679652151 ) ) ;
#10960=CARTESIAN_POINT ( 'NONE',  ( 104.9999999999999432, 2.775557561562891351E-14, 1.110223024625156540E-13 ) ) ;
#10962=ORIENTED_EDGE ( 'NONE', *, *, #19965, .F. ) ;
#10986=CARTESIAN_POINT ( 'NONE',  ( 107.5624999999998153, -2.499999999999874767, -1.035533905932629173 ) ) ;
#10990=VERTEX_POINT ( 'NONE', #22452 ) ;
#11002=CARTESIAN_POINT ( 'NONE',  ( 104.9999999999999005, -0.4876318259229017738, -1.939643060551943243 ) ) ;
#11007=CARTESIAN_POINT ( 'NONE',  ( 121.3752832217622881, 1.849990392679579099, 0.000000000000000000 ) ) ;
#11026=( BOUNDED_CURVE ( )  B_SPLINE_CURVE ( 2, ( #6478, #22772, #11270, #13427, #27654 ),
 .UNSPECIFIED., .F., .F. ) 
 B_SPLINE_CURVE_WITH_KNOTS ( ( 3, 2, 3 ),
 ( 0.9117647058823529216, 0.9191176470588234837, 0.9241494898189103191 ),
 .UNSPECIFIED. ) 
 CURVE ( )  GEOMETRIC_REPRESENTATION_ITEM ( )  RATIONAL_B_SPLINE_CURVE ( ( 1.000000000000000000, 0.9238795325112867385, 1.000000000000000000, 0.9479084336410595890, 0.9671125746063085060 ) ) 
 REPRESENTATION_ITEM ( '' )  );
#11038=DIRECTION ( 'NONE',  ( 0.000000000000000000, 0.000000000000000000, 1.000000000000000000 ) ) ;
#11041=CARTESIAN_POINT ( 'NONE',  ( 116.7499999999997584, 1.665334536937734811E-13, -2.499999999999724665 ) ) ;
#11044=DIRECTION ( 'NONE',  ( 5.551115123125785167E-17, -1.000000000000000000, -8.881784197001256268E-16 ) ) ;
#11045=FACE_OUTER_BOUND ( 'NONE', #679, .T. ) ;
#11051=CARTESIAN_POINT ( 'NONE',  ( 116.3749999999998579, -1.767766952966209892, 1.767766952966542959 ) ) ;
#11052=CARTESIAN_POINT ( 'NONE',  ( 108.8127832217621176, -1.849990392679501827, 0.7662911109078287542 ) ) ;
#11055=CARTESIAN_POINT ( 'NONE',  ( 109.2497167782375413, -1.308140751793585022, -1.308140751793640533 ) ) ;
#11082=CARTESIAN_POINT ( 'NONE',  ( 110.6252832217622029, 5.551115123125782702E-14, 1.849990392679523588 ) ) ;
#11097=CARTESIAN_POINT ( 'NONE',  ( 108.9997167782375698, -1.308140751793612777, 1.308140751793640533 ) ) ;
#11129=CARTESIAN_POINT ( 'NONE',  ( 109.7499999999999147, 5.551115123125782702E-14, -2.499999999999835687 ) ) ;
#11134=CARTESIAN_POINT ( 'NONE',  ( 0.000000000000000000, 0.000000000000000000, 0.000000000000000000 ) ) ;
#11140=AXIS2_PLACEMENT_3D ( 'NONE', #1319, #20077, #22691 ) ;
#11165=CARTESIAN_POINT ( 'NONE',  ( 104.8544169799067731, -1.915947604159734308, -0.2177314441303023207 ) ) ;
#11168=CARTESIAN_POINT ( 'NONE',  ( 114.4613248654051603, 5.551115123125782702E-14, -2.000000000000001776 ) ) ;
#11171=( BOUNDED_CURVE ( )  B_SPLINE_CURVE ( 2, ( #4962, #2663, #25563, #28006, #6823, #16248, #25871, #7127, #13945 ),
 .UNSPECIFIED., .F., .F. ) 
 B_SPLINE_CURVE_WITH_KNOTS ( ( 3, 2, 2, 2, 3 ),
 ( 0.8823529411764705621, 0.8897058823529411242, 0.8970588235294117974, 0.9044117647058823595, 0.9117647058823529216 ),
 .UNSPECIFIED. ) 
 CURVE ( )  GEOMETRIC_REPRESENTATION_ITEM ( )  RATIONAL_B_SPLINE_CURVE ( ( 1.000000000000000000, 0.9238795325112867385, 1.000000000000000000, 0.9238795325112867385, 1.000000000000000000, 0.9238795325112867385, 1.000000000000000000, 0.9238795325112867385, 1.000000000000000000 ) ) 
 REPRESENTATION_ITEM ( '' )  );
#11178=EDGE_CURVE ( 'NONE', #24742, #18130, #5597, .T. ) ;
#11198=CARTESIAN_POINT ( 'NONE',  ( 117.6874999999997726, -1.035533905932719101, -2.499999999999844569 ) ) ;
#11201=CARTESIAN_POINT ( 'NONE',  ( 104.9999999999998863, -0.4876318259229017738, -1.939643060551943243 ) ) ;
#11208=CARTESIAN_POINT ( 'NONE',  ( 115.8749999999998579, 1.767766952966431937, -1.767766952966320915 ) ) ;
#11209=CARTESIAN_POINT ( 'NONE',  ( 110.3752832217623592, 1.849990392679495832, 0.000000000000000000 ) ) ;
#11210=CARTESIAN_POINT ( 'NONE',  ( 107.9613248654050892, 1.110223024625156540E-13, 2.000000000000001776 ) ) ;
#11212=VERTEX_POINT ( 'NONE', #21214 ) ;
#11213=CARTESIAN_POINT ( 'NONE',  ( 108.8122167782374703, 0.7662911109077987781, 1.849990392679712103 ) ) ;
#11238=CARTESIAN_POINT ( 'NONE',  ( 113.2502832217622455, 1.308140751793612777, -1.308140751793640533 ) ) ;
#11253=CARTESIAN_POINT ( 'NONE',  ( 111.7497167782375129, 1.308140751793751555, 1.308140751793973600 ) ) ;
#11255=CARTESIAN_POINT ( 'NONE',  ( 111.9372167782374703, -0.7662911109077388261, 1.849990392679652151 ) ) ;
#11262=VERTEX_POINT ( 'NONE', #7067 ) ;
#11267=ORIENTED_EDGE ( 'NONE', *, *, #16161, .T. ) ;
#11270=CARTESIAN_POINT ( 'NONE',  ( 105.0863248654051318, -1.414213562373034527, 1.414213562373145550 ) ) ;
#11274=CARTESIAN_POINT ( 'NONE',  ( 112.2886751345947118, 2.000000000000112799, 3.330669073875469621E-13 ) ) ;
#11279=CARTESIAN_POINT ( 'NONE',  ( 108.8124999999997442, 1.035533905932839227, -2.499999999999964473 ) ) ;
#11280=CARTESIAN_POINT ( 'NONE',  ( 106.6636751345947829, -1.414213562373090038, 1.414213562373145550 ) ) ;
#11291=CARTESIAN_POINT ( 'NONE',  ( 106.6249999999999289, -1.767766952966376426, -1.767766952966320915 ) ) ;
#11298=CARTESIAN_POINT ( 'NONE',  ( 119.6249999999999716, -1.767766952966404181, -1.767766952966320915 ) ) ;
#11310=CARTESIAN_POINT ( 'NONE',  ( 105.0386751345947971, 2.775557561562891351E-14, -2.000000000000001776 ) ) ;
#11314=CARTESIAN_POINT ( 'NONE',  ( 118.8752832217621460, -1.849990392679384810, 2.220446049250313081E-13 ) ) ;
#11333=CARTESIAN_POINT ( 'NONE',  ( 116.3747167782375840, 5.551115123125782702E-14, -1.849990392679190521 ) ) ;
#11335=EDGE_CURVE ( 'NONE', #1220, #28323, #15902, .T. ) ;
#11339=CARTESIAN_POINT ( 'NONE',  ( 117.9377832217621744, -1.849990392679441875, -0.7662911109075883909 ) ) ;
#11358=CARTESIAN_POINT ( 'NONE',  ( 114.3124999999997726, -1.035533905932719101, 2.500000000000205169 ) ) ;
#11359=ADVANCED_FACE ( 'NONE', ( #8210 ), #6526, .F. ) ;
#11367=ORIENTED_EDGE ( 'NONE', *, *, #23697, .F. ) ;
#11368=CARTESIAN_POINT ( 'NONE',  ( 115.9999999999998153, 2.500000000000002220, 2.220446049250313081E-13 ) ) ;
#11371=CARTESIAN_POINT ( 'NONE',  ( 105.7502832217622597, -1.308140751793557266, 1.308140751793751555 ) ) ;
#11377=CARTESIAN_POINT ( 'NONE',  ( 108.9997167782375698, -1.308140751793612777, 1.308140751793640533 ) ) ;
#11394=CYLINDRICAL_SURFACE ( 'NONE', #10840, 2.000000000000012879 ) ;
#11397=CARTESIAN_POINT ( 'NONE',  ( 111.1252832217622597, -5.551115123125782702E-14, -1.849990392679523588 ) ) ;
#11413=DIRECTION ( 'NONE',  ( -1.000000000000000000, -1.665334536937736783E-16, -2.220446049250315546E-16 ) ) ;
#11418=CARTESIAN_POINT ( 'NONE',  ( 111.2497167782375982, -1.308140751793640533, -1.308140751793640533 ) ) ;
#11420=CARTESIAN_POINT ( 'NONE',  ( 111.9997167782376550, -1.308140751793640533, 1.308140751793640533 ) ) ;
#11443=CARTESIAN_POINT ( 'NONE',  ( 108.7499999999998579, 8.326672684688674053E-14, -2.499999999999835687 ) ) ;
#11457=CARTESIAN_POINT ( 'NONE',  ( 107.3124999999996589, -1.035533905932598975, 2.500000000000205169 ) ) ;
#11476=CARTESIAN_POINT ( 'NONE',  ( 120.6877832217621176, -0.7662911109077388261, 1.849990392679652151 ) ) ;
#11478=ADVANCED_FACE ( 'NONE', ( #16405 ), #20677, .F. ) ;
#11499=CARTESIAN_POINT ( 'NONE',  ( 114.2502832217621602, 1.308140751793640533, -1.308140751793640533 ) ) ;
#11517=CARTESIAN_POINT ( 'NONE',  ( 111.4999999999998863, -2.499999999999946709, 1.110223024625156540E-13 ) ) ;
#11526=CARTESIAN_POINT ( 'NONE',  ( 117.1874999999997726, 1.035533905932659149, 2.500000000000205169 ) ) ;
#11527=CARTESIAN_POINT ( 'NONE',  ( 105.5002832217622313, 1.308140751793696044, 1.308140751793640533 ) ) ;
#11529=CARTESIAN_POINT ( 'NONE',  ( 110.2113248654050608, -1.999999999999946265, 0.000000000000000000 ) ) ;
#11530=CARTESIAN_POINT ( 'NONE',  ( 105.9997167782375982, -1.308140751793612777, 1.308140751793640533 ) ) ;
#11532=CARTESIAN_POINT ( 'NONE',  ( 106.9613248654050039, 1.110223024625156540E-13, 2.000000000000001776 ) ) ;
#11547=ORIENTED_EDGE ( 'NONE', *, *, #15605, .F. ) ;
#11568=CARTESIAN_POINT ( 'NONE',  ( 109.0622167782374561, -1.849990392679501827, 0.7662911109077686911 ) ) ;
#11570=CARTESIAN_POINT ( 'NONE',  ( 112.6247167782375271, 1.849990392679523588, 0.000000000000000000 ) ) ;
#11573=CARTESIAN_POINT ( 'NONE',  ( 110.4613248654051176, 5.551115123125782702E-14, -2.000000000000001776 ) ) ;
#11587=( BOUNDED_CURVE ( )  B_SPLINE_CURVE ( 2, ( #24574, #10014, #29171, #17096, #17247, #19392, #10629, #17396, #14640 ),
 .UNSPECIFIED., .F., .F. ) 
 B_SPLINE_CURVE_WITH_KNOTS ( ( 3, 2, 2, 2, 3 ),
 ( 0.7058823529411765163, 0.7132352941176470784, 0.7205882352941176405, 0.7279411764705882026, 0.7352941176470588758 ),
 .UNSPECIFIED. ) 
 CURVE ( )  GEOMETRIC_REPRESENTATION_ITEM ( )  RATIONAL_B_SPLINE_CURVE ( ( 1.000000000000000000, 0.9238795325112867385, 1.000000000000000000, 0.9238795325112867385, 1.000000000000000000, 0.9238795325112867385, 1.000000000000000000, 0.9238795325112867385, 1.000000000000000000 ) ) 
 REPRESENTATION_ITEM ( '' )  );
#11596=CARTESIAN_POINT ( 'NONE',  ( 109.3750000000000142, -1.767766952966320915, 1.767766952966431937 ) ) ;
#11597=DIRECTION ( 'NONE',  ( -1.000000000000000000, -1.665334536937736783E-16, -2.220446049250315546E-16 ) ) ;
#11608=CARTESIAN_POINT ( 'NONE',  ( 119.7497167782375556, 1.308140751793696044, 1.308140751793862577 ) ) ;
#11625=CARTESIAN_POINT ( 'NONE',  ( 106.1872167782374703, -1.849990392679381701, -0.7662911109075283278 ) ) ;
#11626=CARTESIAN_POINT ( 'NONE',  ( 113.2886751345947118, 1.999999999999946265, 1.110223024625156540E-13 ) ) ;
#11628=CARTESIAN_POINT ( 'NONE',  ( 117.6252832217623165, 0.000000000000000000, 1.849990392679523588 ) ) ;
#11647=CARTESIAN_POINT ( 'NONE',  ( 117.6247167782375840, 1.849990392679551343, 0.000000000000000000 ) ) ;
#11651=CARTESIAN_POINT ( 'NONE',  ( 113.3127832217621176, 1.849990392679501827, -0.7662911109077087390 ) ) ;
#11673=CARTESIAN_POINT ( 'NONE',  ( 114.1250000000000142, 1.767766952966293159, 1.767766952966320915 ) ) ;
#11680=CARTESIAN_POINT ( 'NONE',  ( 111.6249999999998153, -1.767766952966376426, -1.767766952966431937 ) ) ;
#11682=CARTESIAN_POINT ( 'NONE',  ( 105.0627832217622455, -0.7662911109076785410, -1.849990392679411677 ) ) ;
#11687=CARTESIAN_POINT ( 'NONE',  ( 113.9136751345947260, -1.414213562373256572, -1.414213562373034527 ) ) ;
#11689=CARTESIAN_POINT ( 'NONE',  ( 105.3747167782376550, -5.551115123125782702E-14, -1.849990392679523588 ) ) ;
#11691=ADVANCED_FACE ( 'NONE', ( #29684 ), #8030, .F. ) ;
#11701=CARTESIAN_POINT ( 'NONE',  ( 109.8749999999998437, 1.767766952966320915, -1.767766952966209892 ) ) ;
#11705=CARTESIAN_POINT ( 'NONE',  ( 107.9377832217621886, -1.849990392679472073, -0.7662911109075283278 ) ) ;
#11721=CARTESIAN_POINT ( 'NONE',  ( 111.0622167782374845, -1.849990392679501827, 0.7662911109078888172 ) ) ;
#11729=ORIENTED_EDGE ( 'NONE', *, *, #18026, .T. ) ;
#11746=CARTESIAN_POINT ( 'NONE',  ( 111.6249999999998153, -1.767766952966376426, -1.767766952966431937 ) ) ;
#11758=CARTESIAN_POINT ( 'NONE',  ( 106.0624999999998295, 2.500000000000114575, 1.035533905933049725 ) ) ;
#11762=ADVANCED_FACE ( 'NONE', ( #22332 ), #3873, .F. ) ;
#11765=CARTESIAN_POINT ( 'NONE',  ( 118.5624999999997016, -2.499999999999874767, -1.035533905932568999 ) ) ;
#11769=CARTESIAN_POINT ( 'NONE',  ( 3.330669073875473566E-16, -6.000000000000005329, -5.329070518200757705E-15 ) ) ;
#11776=CARTESIAN_POINT ( 'NONE',  ( 107.4997167782375982, 1.308140751793723799, -1.308140751793640533 ) ) ;
#11779=CARTESIAN_POINT ( 'NONE',  ( 120.4377832217621176, 1.849990392679562001, 0.7662911109080692285 ) ) ;
#11797=FACE_OUTER_BOUND ( 'NONE', #11852, .T. ) ;
#11798=CARTESIAN_POINT ( 'NONE',  ( 116.6872167782373708, 1.849990392679501827, 0.7662911109079489913 ) ) ;
#11805=CARTESIAN_POINT ( 'NONE',  ( 114.6252832217623450, 0.000000000000000000, 1.849990392679523588 ) ) ;
#11826=CARTESIAN_POINT ( 'NONE',  ( 113.4374999999998863, -2.499999999999994671, 1.035533905932869425 ) ) ;
#11837=CARTESIAN_POINT ( 'NONE',  ( 113.2499999999998437, 2.775557561562891351E-14, 2.500000000000168754 ) ) ;
#11839=CARTESIAN_POINT ( 'NONE',  ( 107.0627832217620892, -0.7662911109076184779, -1.849990392679351725 ) ) ;
#11852=EDGE_LOOP ( 'NONE', ( #25690, #23308, #4833, #17191 ) ) ;
#11855=CARTESIAN_POINT ( 'NONE',  ( 109.0624999999997868, 2.500000000000055067, 1.035533905932809473 ) ) ;
#11860=CARTESIAN_POINT ( 'NONE',  ( 109.5386751345946834, 5.551115123125782702E-14, 2.000000000000001776 ) ) ;
#11863=CARTESIAN_POINT ( 'NONE',  ( 106.3127832217621318, 1.849990392679501827, -0.7662911109075883909 ) ) ;
#11900=CARTESIAN_POINT ( 'NONE',  ( 119.9999999999997868, 1.387778780781445676E-13, 1.110223024625156540E-13 ) ) ;
#11905=CARTESIAN_POINT ( 'NONE',  ( 109.0238248654049045, -0.8284271247461453269, 2.000000000000271783 ) ) ;
#11906=CARTESIAN_POINT ( 'NONE',  ( 110.9374999999997158, 2.500000000000054623, -1.035533905932388699 ) ) ;
#11911=( BOUNDED_CURVE ( )  B_SPLINE_CURVE ( 2, ( #27843, #4512, #18823, #16239, #4810, #23572, #13936 ),
 .UNSPECIFIED., .F., .F. ) 
 B_SPLINE_CURVE_WITH_KNOTS ( ( 3, 2, 2, 3 ),
 ( 0.04179654864244304602, 0.04411764705882353227, 0.05147058823529411520, 0.05882352941176470507 ),
 .UNSPECIFIED. ) 
 CURVE ( )  GEOMETRIC_REPRESENTATION_ITEM ( )  RATIONAL_B_SPLINE_CURVE ( ( 0.9671125746063340411, 0.9759710988702614554, 1.000000000000000000, 0.9238795325112867385, 1.000000000000000000, 0.9238795325112867385, 1.000000000000000000 ) ) 
 REPRESENTATION_ITEM ( '' )  );
#11918=CARTESIAN_POINT ( 'NONE',  ( 118.9997167782376266, -1.308140751793529510, 1.308140751793973600 ) ) ;
#11923=CARTESIAN_POINT ( 'NONE',  ( 117.8749999999998010, 1.767766952966320915, -1.767766952966209892 ) ) ;
#11928=CARTESIAN_POINT ( 'NONE',  ( 115.6488248654049187, 2.000000000000151879, -0.8284271247459350507 ) ) ;
#11933=CARTESIAN_POINT ( 'NONE',  ( 108.7886751345946834, -1.999999999999946265, 1.110223024625156540E-13 ) ) ;
#11937=CARTESIAN_POINT ( 'NONE',  ( 104.8747167782376550, -2.775557561562891351E-14, 1.849990392679523588 ) ) ;
#11940=CARTESIAN_POINT ( 'NONE',  ( 119.1252832217622597, -5.551115123125782702E-14, -1.849990392679412565 ) ) ;
#11956=DIRECTION ( 'NONE',  ( -1.000000000000000000, -1.665334536937736783E-16, -2.220446049250315546E-16 ) ) ;
#11957=CARTESIAN_POINT ( 'NONE',  ( 117.5622167782373992, 1.849990392679562001, -0.7662911109076485650 ) ) ;
#11959=( BOUNDED_CURVE ( )  B_SPLINE_CURVE ( 2, ( #12864, #22051, #29086, #15151, #22519, #24643, #1291, #13182, #13019 ),
 .UNSPECIFIED., .F., .F. ) 
 B_SPLINE_CURVE_WITH_KNOTS ( ( 3, 2, 2, 2, 3 ),
 ( 0.1470588235294117696, 0.1544117647058823595, 0.1617647058823529493, 0.1691176470588235392, 0.1764705882352941291 ),
 .UNSPECIFIED. ) 
 CURVE ( )  GEOMETRIC_REPRESENTATION_ITEM ( )  RATIONAL_B_SPLINE_CURVE ( ( 1.000000000000000000, 0.9238795325112867385, 1.000000000000000000, 0.9238795325112867385, 1.000000000000000000, 0.9238795325112867385, 1.000000000000000000, 0.9238795325112867385, 1.000000000000000000 ) ) 
 REPRESENTATION_ITEM ( '' )  );
#11960=ORIENTED_EDGE ( 'NONE', *, *, #11999, .T. ) ;
#11962=CARTESIAN_POINT ( 'NONE',  ( 115.5002832217623308, 1.308140751793640533, 1.308140751793640533 ) ) ;
#11964=STYLED_ITEM ( 'NONE', ( #24330 ), #24617 ) ;
#11981=LINE ( 'NONE', #7754, #9372 ) ;
#11985=CARTESIAN_POINT ( 'NONE',  ( 107.1636751345947545, 1.414213562373062283, -1.414213562372812483 ) ) ;
#11988=CARTESIAN_POINT ( 'NONE',  ( 112.8124999999998579, 1.035533905932779275, -2.499999999999904521 ) ) ;
#11990=CARTESIAN_POINT ( 'NONE',  ( 108.3127832217620181, 1.849990392679562001, -0.7662911109076485650 ) ) ;
#11999=EDGE_CURVE ( 'NONE', #30347, #23965, #26246, .T. ) ;
#12006=CARTESIAN_POINT ( 'NONE',  ( 109.3124999999999147, -1.035533905932598975, 2.500000000000265121 ) ) ;
#12011=CARTESIAN_POINT ( 'NONE',  ( 108.3752832217622739, 1.849990392679523588, 0.000000000000000000 ) ) ;
#12032=CARTESIAN_POINT ( 'NONE',  ( 106.1011751345946266, 0.8284271247462955401, -1.999999999999731104 ) ) ;
#12036=EDGE_CURVE ( 'NONE', #4573, #20271, #28215, .T. ) ;
#12050=CARTESIAN_POINT ( 'NONE',  ( 106.5624999999998295, -2.499999999999874767, -1.035533905932629173 ) ) ;
#12058=CARTESIAN_POINT ( 'NONE',  ( 116.9372167782374845, -0.7662911109078588412, 1.849990392679652151 ) ) ;
#12064=CARTESIAN_POINT ( 'NONE',  ( 116.8124999999998010, 1.035533905932719101, -2.499999999999784173 ) ) ;
#12065=CIRCLE ( 'NONE', #24284, 2.000000000000012879 ) ;
#12068=VERTEX_POINT ( 'NONE', #19208 ) ;
#12071=CARTESIAN_POINT ( 'NONE',  ( 115.7113248654050466, 2.000000000000112799, 0.000000000000000000 ) ) ;
#12079=CARTESIAN_POINT ( 'NONE',  ( 106.1247167782374987, -1.849990392679412565, 2.220446049250313081E-13 ) ) ;
#12081=CARTESIAN_POINT ( 'NONE',  ( 116.5002832217622171, 1.308140751793696044, 1.308140751793640533 ) ) ;
#12097=CARTESIAN_POINT ( 'NONE',  ( 115.8122167782375982, 0.7662911109078588412, 1.849990392679712103 ) ) ;
#12110=VERTEX_POINT ( 'NONE', #14611 ) ;
#12116=CARTESIAN_POINT ( 'NONE',  ( 107.7886751345947403, -1.999999999999835243, 1.110223024625156540E-13 ) ) ;
#12122=CARTESIAN_POINT ( 'NONE',  ( 112.4999999999999147, -2.499999999999835687, 0.000000000000000000 ) ) ;
#12131=CARTESIAN_POINT ( 'NONE',  ( 113.9374999999997300, 2.500000000000114575, -1.035533905932629173 ) ) ;
#12137=CARTESIAN_POINT ( 'NONE',  ( 118.2886751345946976, 2.000000000000085265, 0.000000000000000000 ) ) ;
#12139=CARTESIAN_POINT ( 'NONE',  ( 110.7738248654050608, 2.000000000000061728, 0.8284271247464157772 ) ) ;
#12149=CARTESIAN_POINT ( 'NONE',  ( 114.0863248654051603, -1.414213562373034527, 1.414213562373145550 ) ) ;
#12151=CARTESIAN_POINT ( 'NONE',  ( 109.1874999999997584, 1.035533905932839449, 2.500000000000205169 ) ) ;
#12153=VECTOR ( 'NONE', #23693, 1000.000000000000000 ) ;
#12158=CARTESIAN_POINT ( 'NONE',  ( 107.4377832217621744, 1.849990392679562001, 0.7662911109080692285 ) ) ;
#12159=CARTESIAN_POINT ( 'NONE',  ( -9.992007221626473945E-16, 6.000000000000000888, 1.170861610602040338E-13 ) ) ;
#12161=CARTESIAN_POINT ( 'NONE',  ( 119.2886751345947260, 1.999999999999946265, 1.110223024625156540E-13 ) ) ;
#12187=CARTESIAN_POINT ( 'NONE',  ( 105.9761751345945839, -0.8284271247461453269, -1.999999999999791278 ) ) ;
#12189=ORIENTED_EDGE ( 'NONE', *, *, #29631, .F. ) ;
#12203=CARTESIAN_POINT ( 'NONE',  ( 107.0624999999998153, 2.500000000000115019, 1.035533905932989551 ) ) ;
#12213=CARTESIAN_POINT ( 'NONE',  ( 118.3747167782375129, 0.000000000000000000, -1.849990392679301543 ) ) ;
#12219=CARTESIAN_POINT ( 'NONE',  ( 117.1874999999997584, 1.035533905932659149, 2.500000000000205169 ) ) ;
#12221=ORIENTED_EDGE ( 'NONE', *, *, #4249, .T. ) ;
#12230=CARTESIAN_POINT ( 'NONE',  ( -1.110223024625164676E-16, 2.000000000000012879, 2.021286199229734960E-15 ) ) ;
#12231=CARTESIAN_POINT ( 'NONE',  ( 106.8122167782374277, 0.7662911109079189043, 1.849990392679712103 ) ) ;
#12233=CARTESIAN_POINT ( 'NONE',  ( 115.1252832217622881, -2.220446049250313081E-13, -1.849990392679523588 ) ) ;
#12235=PLANE ( 'NONE',  #7925 ) ;
#12248=CARTESIAN_POINT ( 'NONE',  ( 115.7497167782375698, 1.308140751793751555, 1.308140751793973600 ) ) ;
#12252=CARTESIAN_POINT ( 'NONE',  ( 119.9999999999997868, 1.387778780781445676E-13, 1.110223024625156540E-13 ) ) ;
#12254=CARTESIAN_POINT ( 'NONE',  ( 104.4999999999998863, -2.499999999999919176, 0.000000000000000000 ) ) ;
#12264=CARTESIAN_POINT ( 'NONE',  ( 111.5238248654049329, 0.8284271247462955401, -1.999999999999791278 ) ) ;
#12278=CARTESIAN_POINT ( 'NONE',  ( 109.3988248654050039, -0.8284271247461453269, -1.999999999999731104 ) ) ;
#12279=CARTESIAN_POINT ( 'NONE',  ( 114.2499999999999147, -1.110223024625156540E-13, 2.500000000000057732 ) ) ;
#12286=CARTESIAN_POINT ( 'NONE',  ( 121.0002832217622739, -1.308140751793557266, -1.308140751793529510 ) ) ;
#12296=CARTESIAN_POINT ( 'NONE',  ( 108.5000000000000000, -2.500000000000002220, 2.220446049250313081E-13 ) ) ;
#12297=AXIS2_PLACEMENT_3D ( 'NONE', #17016, #14703, #24049 ) ;
#12307=CARTESIAN_POINT ( 'NONE',  ( 107.3752832217621886, 1.849990392679523588, 0.000000000000000000 ) ) ;
#12340=CARTESIAN_POINT ( 'NONE',  ( 104.8749999999998437, 1.767766952966320915, -1.767766952966431937 ) ) ;
#12352=CARTESIAN_POINT ( 'NONE',  ( 117.6872167782374845, 1.849990392679621953, 0.7662911109078287542 ) ) ;
#12353=CARTESIAN_POINT ( 'NONE',  ( 109.2113248654051745, -1.999999999999946265, 0.000000000000000000 ) ) ;
#12357=CARTESIAN_POINT ( 'NONE',  ( 117.6874999999997726, -1.035533905932719101, -2.499999999999844569 ) ) ;
#12364=EDGE_CURVE ( 'NONE', #14656, #15734, #27223, .T. ) ;
#12375=CARTESIAN_POINT ( 'NONE',  ( 115.6877832217621744, -0.7662911109077087390, 1.849990392679712103 ) ) ;
#12393=CARTESIAN_POINT ( 'NONE',  ( 115.9997167782376266, -1.308140751793668288, 1.308140751793751555 ) ) ;
#12409=CARTESIAN_POINT ( 'NONE',  ( 0.000000000000000000, 0.000000000000000000, 0.000000000000000000 ) ) ;
#12411=CARTESIAN_POINT ( 'NONE',  ( 111.7113248654050892, 2.000000000000057288, 0.000000000000000000 ) ) ;
#12416=CARTESIAN_POINT ( 'NONE',  ( 104.4999999999998863, -2.499999999999919176, 0.000000000000000000 ) ) ;
#12424=CARTESIAN_POINT ( 'NONE',  ( 110.6874999999997868, -1.035533905932689347, -2.499999999999844569 ) ) ;
#12430=CARTESIAN_POINT ( 'NONE',  ( 120.1877832217620750, 0.7662911109077987781, -1.849990392679532247 ) ) ;
#12438=EDGE_LOOP ( 'NONE', ( #22138, #21035, #4413, #16001 ) ) ;
#12440=CARTESIAN_POINT ( 'NONE',  ( 114.2113248654050750, -1.999999999999890754, 0.000000000000000000 ) ) ;
#12442=CARTESIAN_POINT ( 'NONE',  ( 105.1249999999999005, 1.767766952966265404, 1.767766952966431937 ) ) ;
#12445=ORIENTED_EDGE ( 'NONE', *, *, #17139, .T. ) ;
#12451=CARTESIAN_POINT ( 'NONE',  ( 105.7502832217622597, -1.308140751793557266, 1.308140751793751555 ) ) ;
#12464=CARTESIAN_POINT ( 'NONE',  ( 120.4999999999998437, -2.499999999999891198, 3.330669073875469621E-13 ) ) ;
#12469=CARTESIAN_POINT ( 'NONE',  ( 111.3511751345947829, 2.000000000000061728, 0.8284271247462955401 ) ) ;
#12495=CONICAL_SURFACE ( 'NONE', #25697, 577.3502691896271699, 0.5235987755982998149 ) ;
#12505=CARTESIAN_POINT ( 'NONE',  ( 119.1872167782375271, -1.849990392679562001, -0.7662911109077087390 ) ) ;
#12511=CARTESIAN_POINT ( 'NONE',  ( 112.3124999999997726, -1.035533905932598975, 2.500000000000265121 ) ) ;
#12526=CARTESIAN_POINT ( 'NONE',  ( 1101.535898384862321, 1.665334536937736830E-13, 2.220446049250315605E-13 ) ) ;
#12528=CARTESIAN_POINT ( 'NONE',  ( 116.3127832217621034, 1.849990392679532247, -0.7662911109075883909 ) ) ;
#12541=FACE_OUTER_BOUND ( 'NONE', #29471, .T. ) ;
#12544=AXIS2_PLACEMENT_3D ( 'NONE', #2280, #4864, #23633 ) ;
#12553=AXIS2_PLACEMENT_3D ( 'NONE', #14945, #19698, #29040 ) ;
#12562=CARTESIAN_POINT ( 'NONE',  ( 116.9761751345948113, -0.8284271247460250898, -1.999999999999851674 ) ) ;
#12571=CARTESIAN_POINT ( 'NONE',  ( 108.5000000000000000, -2.500000000000002220, 2.220446049250313081E-13 ) ) ;
#12575=CARTESIAN_POINT ( 'NONE',  ( 113.2113248654051034, -1.999999999999918510, 1.110223024625156540E-13 ) ) ;
#12582=ORIENTED_EDGE ( 'NONE', *, *, #30050, .T. ) ;
#12584=ORIENTED_EDGE ( 'NONE', *, *, #16311, .T. ) ;
#12591=CARTESIAN_POINT ( 'NONE',  ( 10.00000000000002309, 8.326672684688674053E-14, 1.110223024625156540E-13 ) ) ;
#12598=CARTESIAN_POINT ( 'NONE',  ( 120.2499999999998721, -2.775557561562891351E-14, 2.500000000000168754 ) ) ;
#12602=CARTESIAN_POINT ( 'NONE',  ( 113.7261751345946124, -1.999999999999941602, 0.8284271247462955401 ) ) ;
#12612=CARTESIAN_POINT ( 'NONE',  ( 120.3750000000000284, -1.767766952966376426, 1.767766952966320915 ) ) ;
#12621=ORIENTED_EDGE ( 'NONE', *, *, #7956, .T. ) ;
#12636=CARTESIAN_POINT ( 'NONE',  ( 106.0624999999998295, 2.500000000000115019, 1.035533905933049725 ) ) ;
#12645=DIRECTION ( 'NONE',  ( 1.000000000000000000, 1.665334536937736783E-16, 2.220446049250315546E-16 ) ) ;
#12650=CARTESIAN_POINT ( 'NONE',  ( 113.0622167782374561, -1.849990392679532247, 0.7662911109078888172 ) ) ;
#12656=CARTESIAN_POINT ( 'NONE',  ( 112.6874999999997726, -1.035533905932659149, -2.499999999999604317 ) ) ;
#12669=CARTESIAN_POINT ( 'NONE',  ( 116.2113248654050750, -2.000000000000029310, 0.000000000000000000 ) ) ;
#12673=EDGE_CURVE ( 'NONE', #23965, #11212, #26072, .T. ) ;
#12684=CIRCLE ( 'NONE', #4296, 2.000000000000012879 ) ;
#12692=CARTESIAN_POINT ( 'NONE',  ( 114.7113248654050750, 2.000000000000057288, 0.000000000000000000 ) ) ;
#12693=CARTESIAN_POINT ( 'NONE',  ( 114.1247167782374987, -1.849990392679440321, 0.000000000000000000 ) ) ;
#12732=CARTESIAN_POINT ( 'NONE',  ( 104.7497167782376408, 1.308140751793640533, 1.308140751793640533 ) ) ;
#12741=CARTESIAN_POINT ( 'NONE',  ( 105.5624999999997726, -2.499999999999874767, -1.035533905932568777 ) ) ;
#12752=CARTESIAN_POINT ( 'NONE',  ( 118.7499999999997868, -1.665334536937734811E-13, -2.500000000000057732 ) ) ;
#12762=ORIENTED_EDGE ( 'NONE', *, *, #16971, .F. ) ;
#12778=CARTESIAN_POINT ( 'NONE',  ( 5.000000000000018652, 8.326672684688674053E-14, 1.110223024625156540E-13 ) ) ;
#12793=CARTESIAN_POINT ( 'NONE',  ( 107.6488248654049897, 2.000000000000061728, -0.8284271247460553989 ) ) ;
#12802=EDGE_LOOP ( 'NONE', ( #19371, #21492, #11367, #24506 ) ) ;
#12803=CARTESIAN_POINT ( 'NONE',  ( 114.6872167782375982, 1.849990392679621953, 0.7662911109080090544 ) ) ;
#12809=CARTESIAN_POINT ( 'NONE',  ( 115.5624999999998863, -2.499999999999934719, -1.035533905932568999 ) ) ;
#12832=( BOUNDED_CURVE ( )  B_SPLINE_CURVE ( 2, ( #16815, #640, #7547, #5386, #10023, #26719, #21845, #15093, #19548 ),
 .UNSPECIFIED., .F., .T. ) 
 B_SPLINE_CURVE_WITH_KNOTS ( ( 3, 2, 2, 2, 3 ),
 ( 0.7941176470588234837, 0.8014705882352941568, 0.8088235294117647189, 0.8161764705882352811, 0.8235294117647058432 ),
 .UNSPECIFIED. ) 
 CURVE ( )  GEOMETRIC_REPRESENTATION_ITEM ( )  RATIONAL_B_SPLINE_CURVE ( ( 1.000000000000000000, 0.9238795325112867385, 1.000000000000000000, 0.9238795325112867385, 1.000000000000000000, 0.9238795325112867385, 1.000000000000000000, 0.9238795325112867385, 1.000000000000000000 ) ) 
 REPRESENTATION_ITEM ( '' )  );
#12839=CARTESIAN_POINT ( 'NONE',  ( 112.2497167782374561, -1.308140751793585022, -1.308140751793640533 ) ) ;
#12858=DIRECTION ( 'NONE',  ( -1.000000000000000000, -1.665334536937736783E-16, -2.220446049250315546E-16 ) ) ;
#12864=CARTESIAN_POINT ( 'NONE',  ( 118.2113248654050466, -1.999999999999946265, 2.220446049250313081E-13 ) ) ;
#12885=CARTESIAN_POINT ( 'NONE',  ( 104.2497167782374845, -1.308140751793640533, -1.308140751793640533 ) ) ;
#12895=ORIENTED_EDGE ( 'NONE', *, *, #23697, .T. ) ;
#12897=CARTESIAN_POINT ( 'NONE',  ( 104.9374999999997726, 2.500000000000114575, -1.035533905932448873 ) ) ;
#12906=CARTESIAN_POINT ( 'NONE',  ( 120.1249999999998295, 1.767766952966348670, 1.767766952966431937 ) ) ;
#12921=CARTESIAN_POINT ( 'NONE',  ( 109.8747167782376124, -2.775557561562891351E-14, 1.849990392679523588 ) ) ;
#12941=DIRECTION ( 'NONE',  ( -1.000000000000000000, -1.665334536937736783E-16, -2.220446049250315546E-16 ) ) ;
#12950=CARTESIAN_POINT ( 'NONE',  ( 119.9999999999997868, 2.090674230935563926, -1.116850201269817600 ) ) ;
#12961=CARTESIAN_POINT ( 'NONE',  ( 111.8747167782376408, 0.000000000000000000, 1.849990392679523588 ) ) ;
#12967=CARTESIAN_POINT ( 'NONE',  ( 115.9999999999998153, 2.500000000000002220, 2.220446049250313081E-13 ) ) ;
#12997=CARTESIAN_POINT ( 'NONE',  ( 111.0622167782374845, -1.849990392679501827, 0.7662911109078888172 ) ) ;
#13005=ORIENTED_EDGE ( 'NONE', *, *, #14400, .T. ) ;
#13012=CARTESIAN_POINT ( 'NONE',  ( 106.5863248654051034, 1.414213562373145550, -1.414213562373145550 ) ) ;
#13017=( BOUNDED_CURVE ( )  B_SPLINE_CURVE ( 2, ( #10818, #27051, #5550, #6017, #3241, #21863, #944, #24443, #12669 ),
 .UNSPECIFIED., .F., .T. ) 
 B_SPLINE_CURVE_WITH_KNOTS ( ( 3, 2, 2, 2, 3 ),
 ( 0.2352941176470588203, 0.2426470588235294101, 0.2500000000000000000, 0.2573529411764705621, 0.2647058823529411797 ),
 .UNSPECIFIED. ) 
 CURVE ( )  GEOMETRIC_REPRESENTATION_ITEM ( )  RATIONAL_B_SPLINE_CURVE ( ( 1.000000000000000000, 0.9238795325112867385, 1.000000000000000000, 0.9238795325112867385, 1.000000000000000000, 0.9238795325112867385, 1.000000000000000000, 0.9238795325112867385, 1.000000000000000000 ) ) 
 REPRESENTATION_ITEM ( '' )  );
#13019=CARTESIAN_POINT ( 'NONE',  ( 117.7113248654050466, 2.000000000000085265, 0.000000000000000000 ) ) ;
#13033=CARTESIAN_POINT ( 'NONE',  ( 120.3747167782374277, 0.000000000000000000, -1.849990392679301543 ) ) ;
#13035=ADVANCED_FACE ( 'NONE', ( #29137 ), #29375, .T. ) ;
#13040=CARTESIAN_POINT ( 'NONE',  ( 116.8752832217622313, -1.849990392679579099, 0.000000000000000000 ) ) ;
#13041=DIRECTION ( 'NONE',  ( -3.845925372767118265E-16, 1.000000000000000000, 8.881784197001258240E-16 ) ) ;
#13048=FACE_OUTER_BOUND ( 'NONE', #21547, .T. ) ;
#13062=CARTESIAN_POINT ( 'NONE',  ( 118.8124999999998579, 1.035533905932749299, -2.499999999999784173 ) ) ;
#13066=EDGE_CURVE ( 'NONE', #13876, #1067, #3011, .T. ) ;
#13070=VECTOR ( 'NONE', #18718, 1000.000000000000000 ) ;
#13076=CARTESIAN_POINT ( 'NONE',  ( 109.6877832217621318, -0.7662911109076485650, 1.849990392679652151 ) ) ;
#13082=CARTESIAN_POINT ( 'NONE',  ( 108.7497167782375982, 1.308140751793696044, 1.308140751793640533 ) ) ;
#13102=CARTESIAN_POINT ( 'NONE',  ( 117.2502832217622455, 1.308140751793612777, -1.308140751793307466 ) ) ;
#13106=CARTESIAN_POINT ( 'NONE',  ( 119.5238248654049897, 0.8284271247463257382, -1.999999999999731104 ) ) ;
#13119=CARTESIAN_POINT ( 'NONE',  ( 114.1247167782374987, -1.849990392679440321, 0.000000000000000000 ) ) ;
#13122=CARTESIAN_POINT ( 'NONE',  ( 115.2499999999998721, -5.551115123125782702E-14, 2.500000000000057732 ) ) ;
#13130=CARTESIAN_POINT ( 'NONE',  ( -1.110223024625164676E-16, 2.000000000000012879, 2.021286199229734960E-15 ) ) ;
#13148=DIRECTION ( 'NONE',  ( 5.551115123125785167E-17, -1.000000000000000000, -8.881784197001256268E-16 ) ) ;
#13152=CARTESIAN_POINT ( 'NONE',  ( 109.2499999999999147, 0.000000000000000000, 2.499999999999946709 ) ) ;
#13164=( BOUNDED_CURVE ( )  B_SPLINE_CURVE ( 2, ( #17612, #5891, #29559, #17924, #8195, #27538, #8514, #15472, #15315 ),
 .UNSPECIFIED., .F., .F. ) 
 B_SPLINE_CURVE_WITH_KNOTS ( ( 3, 2, 2, 2, 3 ),
 ( 0.3235294117647058432, 0.3308823529411765163, 0.3382352941176470784, 0.3455882352941176405, 0.3529411764705882026 ),
 .UNSPECIFIED. ) 
 CURVE ( )  GEOMETRIC_REPRESENTATION_ITEM ( )  RATIONAL_B_SPLINE_CURVE ( ( 1.000000000000000000, 0.9238795325112867385, 1.000000000000000000, 0.9238795325112867385, 1.000000000000000000, 0.9238795325112867385, 1.000000000000000000, 0.9238795325112867385, 1.000000000000000000 ) ) 
 REPRESENTATION_ITEM ( '' )  );
#13182=CARTESIAN_POINT ( 'NONE',  ( 117.7738248654051034, 2.000000000000001776, 0.8284271247464157772 ) ) ;
#13190=DIRECTION ( 'NONE',  ( -1.000000000000000000, -1.665334536937736783E-16, -2.220446049250315546E-16 ) ) ;
#13198=CARTESIAN_POINT ( 'NONE',  ( 117.2502832217622455, 1.308140751793612777, -1.308140751793307466 ) ) ;
#13215=DIRECTION ( 'NONE',  ( -1.000000000000000000, -1.665334536937736783E-16, -2.220446049250315546E-16 ) ) ;
#13217=CARTESIAN_POINT ( 'NONE',  ( 116.6249999999999716, -1.767766952966459693, -1.767766952966209892 ) ) ;
#13225=CARTESIAN_POINT ( 'NONE',  ( 116.2499999999998437, 5.551115123125782702E-14, 2.500000000000168754 ) ) ;
#13226=CARTESIAN_POINT ( 'NONE',  ( 110.1877832217620750, 0.7662911109078588412, -1.849990392679411677 ) ) ;
#13245=SURFACE_SIDE_STYLE ('',( #17845 ) ) ;
#13253=CARTESIAN_POINT ( 'NONE',  ( 113.1252832217622029, -1.110223024625156540E-13, -1.849990392679523588 ) ) ;
#13256=CARTESIAN_POINT ( 'NONE',  ( 119.2738248654049471, -1.999999999999941602, -0.8284271247459952248 ) ) ;
#13264=CYLINDRICAL_SURFACE ( 'NONE', #9190, 2.000000000000012879 ) ;
#13268=CARTESIAN_POINT ( 'NONE',  ( 113.2497167782375982, -1.308140751793585022, -1.308140751793640533 ) ) ;
#13298=ORIENTED_EDGE ( 'NONE', *, *, #20033, .T. ) ;
#13299=CARTESIAN_POINT ( 'NONE',  ( 108.6874999999998010, -1.035533905932749299, -2.499999999999844569 ) ) ;
#13301=DIRECTION ( 'NONE',  ( -1.000000000000000000, -1.665334536937736783E-16, -2.220446049250315546E-16 ) ) ;
#13320=CARTESIAN_POINT ( 'NONE',  ( 3.330669073875470114E-16, -5.999999999999999112, -5.329070518200752183E-15 ) ) ;
#13328=CARTESIAN_POINT ( 'NONE',  ( 104.1872167782373708, -1.849990392679351725, -0.7662911109074683758 ) ) ;
#13357=CARTESIAN_POINT ( 'NONE',  ( 115.1249999999998863, 1.767766952966376426, 1.767766952966320915 ) ) ;
#13369=CARTESIAN_POINT ( 'NONE',  ( 115.8124999999997584, 1.035533905932719101, -2.499999999999784173 ) ) ;
#13370=CARTESIAN_POINT ( 'NONE',  ( 111.4377832217621744, 1.849990392679532247, 0.7662911109078888172 ) ) ;
#13373=ORIENTED_EDGE ( 'NONE', *, *, #14294, .F. ) ;
#13375=CARTESIAN_POINT ( 'NONE',  ( 108.5622167782374277, 1.849990392679501827, -0.7662911109077087390 ) ) ;
#13392=PRESENTATION_STYLE_ASSIGNMENT (( #24409 ) ) ;
#13398=CARTESIAN_POINT ( 'NONE',  ( 110.1252832217622029, -1.665334536937734811E-13, -1.849990392679412565 ) ) ;
#13411=ORIENTED_EDGE ( 'NONE', *, *, #16710, .T. ) ;
#13412=CARTESIAN_POINT ( 'NONE',  ( 109.1247167782376124, -1.849990392679523588, 1.110223024625156540E-13 ) ) ;
#13417=CARTESIAN_POINT ( 'NONE',  ( 105.7113248654051461, 2.000000000000057288, 0.000000000000000000 ) ) ;
#13422=VERTEX_POINT ( 'NONE', #181 ) ;
#13427=CARTESIAN_POINT ( 'NONE',  ( 105.0446384121982675, -1.023503819632144651, 1.804923305114234156 ) ) ;
#13440=EDGE_CURVE ( 'NONE', #19914, #24100, #20, .T. ) ;
#13446=CARTESIAN_POINT ( 'NONE',  ( 108.1874999999998579, 1.035533905932719101, 2.500000000000205169 ) ) ;
#13465=CARTESIAN_POINT ( 'NONE',  ( 119.9999999999998437, -0.3289648646781667685, 2.003997983321501586 ) ) ;
#13478=CARTESIAN_POINT ( 'NONE',  ( 117.2113248654051034, -1.999999999999890754, 3.330669073875469621E-13 ) ) ;
#13494=CARTESIAN_POINT ( 'NONE',  ( 118.9377832217621460, -1.849990392679472073, -0.7662911109077087390 ) ) ;
#13509=LINE ( 'NONE', #4242, #24658 ) ;
#13512=CARTESIAN_POINT ( 'NONE',  ( 116.0624999999999005, 2.500000000000055067, 1.035533905932929599 ) ) ;
#13517=CARTESIAN_POINT ( 'NONE',  ( 105.7113248654051461, 2.000000000000057288, 0.000000000000000000 ) ) ;
#13525=CARTESIAN_POINT ( 'NONE',  ( 117.3750000000000142, -1.767766952966320915, 1.767766952966431937 ) ) ;
#13526=CARTESIAN_POINT ( 'NONE',  ( 111.9377832217620465, -1.849990392679441875, -0.7662911109075883909 ) ) ;
#13530=CARTESIAN_POINT ( 'NONE',  ( 109.3747167782375556, -1.665334536937734811E-13, -1.849990392679523588 ) ) ;
#13550=CARTESIAN_POINT ( 'NONE',  ( 119.9999999999997868, -1.999999999999875211, 2.320366121466830552E-14 ) ) ;
#13555=LINE ( 'NONE', #25171, #2803 ) ;
#13560=CARTESIAN_POINT ( 'NONE',  ( 117.2113248654051034, -1.999999999999890754, 3.330669073875469621E-13 ) ) ;
#13561=CARTESIAN_POINT ( 'NONE',  ( 104.7401757384974985, -0.1191742713688042632, -1.850113936623924538 ) ) ;
#13565=LINE ( 'NONE', #9070, #21458 ) ;
#13569=CARTESIAN_POINT ( 'NONE',  ( 111.6247167782376408, 1.849990392679523588, 0.000000000000000000 ) ) ;
#13574=CARTESIAN_POINT ( 'NONE',  ( 113.6488248654048618, 2.000000000000122125, -0.8284271247460553989 ) ) ;
#13582=AXIS2_PLACEMENT_3D ( 'NONE', #18048, #24914, #27510 ) ;
#13603=CARTESIAN_POINT ( 'NONE',  ( 104.9999999999998579, 2.500000000000002220, 0.000000000000000000 ) ) ;
#13606=CARTESIAN_POINT ( 'NONE',  ( 111.2886751345946834, 2.000000000000001776, 3.330669073875469621E-13 ) ) ;
#13609=VERTEX_POINT ( 'NONE', #27326 ) ;
#13621=CARTESIAN_POINT ( 'NONE',  ( 120.2502832217622739, 1.308140751793612777, -1.308140751793418488 ) ) ;
#13632=CARTESIAN_POINT ( 'NONE',  ( 116.9613248654049897, 5.551115123125782702E-14, 2.000000000000223821 ) ) ;
#13639=CARTESIAN_POINT ( 'NONE',  ( 0.000000000000000000, 0.000000000000000000, 0.000000000000000000 ) ) ;
#13640=CARTESIAN_POINT ( 'NONE',  ( 117.2497167782375129, -1.308140751793585022, -1.308140751793640533 ) ) ;
#13647=CARTESIAN_POINT ( 'NONE',  ( 118.0627832217622455, -0.7662911109076485650, -1.849990392679171425 ) ) ;
#13661=VERTEX_POINT ( 'NONE', #8451 ) ;
#13668=CARTESIAN_POINT ( 'NONE',  ( 115.6874999999997584, -1.035533905932719101, -2.499999999999844569 ) ) ;
#13677=CARTESIAN_POINT ( 'NONE',  ( 118.1249999999999147, 1.767766952966320915, 1.767766952966431937 ) ) ;
#13679=CARTESIAN_POINT ( 'NONE',  ( 112.4377832217622455, 1.849990392679621953, 0.7662911109081291805 ) ) ;
#13683=CARTESIAN_POINT ( 'NONE',  ( 109.3122167782373566, -0.7662911109077388261, -1.849990392679351725 ) ) ;
#13687=CARTESIAN_POINT ( 'NONE',  ( 106.8988248654050892, 0.8284271247462354770, 2.000000000000212275 ) ) ;
#13690=ORIENTED_EDGE ( 'NONE', *, *, #21327, .T. ) ;
#13691=EDGE_LOOP ( 'NONE', ( #10669, #11729, #4733, #7972 ) ) ;
#13709=CARTESIAN_POINT ( 'NONE',  ( 112.9377832217622171, -1.849990392679381701, -0.7662911109076485650 ) ) ;
#13726=CARTESIAN_POINT ( 'NONE',  ( 108.4997167782375982, 1.308140751793668288, -1.308140751793418488 ) ) ;
#13728=CARTESIAN_POINT ( 'NONE',  ( 113.0622167782374561, -1.849990392679532247, 0.7662911109078888172 ) ) ;
#13731=CARTESIAN_POINT ( 'NONE',  ( 113.4613248654050182, 0.000000000000000000, -2.000000000000001776 ) ) ;
#13749=CARTESIAN_POINT ( 'NONE',  ( 109.6874999999997868, -1.035533905932659149, -2.499999999999724221 ) ) ;
#13754=ORIENTED_EDGE ( 'NONE', *, *, #29061, .T. ) ;
#13759=CARTESIAN_POINT ( 'NONE',  ( 104.5624999999997442, -2.499999999999934719, -1.035533905932689347 ) ) ;
#13761=EDGE_CURVE ( 'NONE', #16234, #29267, #1116, .T. ) ;
#13781=CARTESIAN_POINT ( 'NONE',  ( 119.6877832217621176, -0.7662911109077686911, 1.849990392679532247 ) ) ;
#13790=CARTESIAN_POINT ( 'NONE',  ( 116.7738248654050892, 2.000000000000061728, 0.8284271247462955401 ) ) ;
#13805=CARTESIAN_POINT ( 'NONE',  ( 114.6877832217621318, -0.7662911109077987781, 1.849990392679591977 ) ) ;
#13815=FACE_OUTER_BOUND ( 'NONE', #5674, .T. ) ;
#13825=CARTESIAN_POINT ( 'NONE',  ( 117.9999999999997868, 2.500000000000002220, 2.220446049250313081E-13 ) ) ;
#13827=FACE_OUTER_BOUND ( 'NONE', #26135, .T. ) ;
#13828=( BOUNDED_CURVE ( )  B_SPLINE_CURVE ( 2, ( #12575, #24061, #851, #9947, #715, #9794, #28357, #7332, #26205 ),
 .UNSPECIFIED., .F., .T. ) 
 B_SPLINE_CURVE_WITH_KNOTS ( ( 3, 2, 2, 2, 3 ),
 ( 0.4411764705882352811, 0.4485294117647058987, 0.4558823529411764608, 0.4632352941176470784, 0.4705882352941176405 ),
 .UNSPECIFIED. ) 
 CURVE ( )  GEOMETRIC_REPRESENTATION_ITEM ( )  RATIONAL_B_SPLINE_CURVE ( ( 1.000000000000000000, 0.9238795325112867385, 1.000000000000000000, 0.9238795325112867385, 1.000000000000000000, 0.9238795325112867385, 1.000000000000000000, 0.9238795325112867385, 1.000000000000000000 ) ) 
 REPRESENTATION_ITEM ( '' )  );
#13834=CARTESIAN_POINT ( 'NONE',  ( 116.4374999999997726, -2.499999999999934719, 1.035533905932929599 ) ) ;
#13837=CONICAL_SURFACE ( 'NONE', #29470, 577.3502691896271699, 0.5235987755982998149 ) ;
#13838=CARTESIAN_POINT ( 'NONE',  ( 107.1252832217622455, 0.000000000000000000, -1.849990392679523588 ) ) ;
#13862=CARTESIAN_POINT ( 'NONE',  ( 109.2886751345947971, 2.000000000000057288, 1.110223024625156540E-13 ) ) ;
#13866=CARTESIAN_POINT ( 'NONE',  ( 111.6252832217622739, 0.000000000000000000, 1.849990392679523588 ) ) ;
#13876=VERTEX_POINT ( 'NONE', #12159 ) ;
#13883=CARTESIAN_POINT ( 'NONE',  ( 108.7497167782375982, 1.308140751793696044, 1.308140751793640533 ) ) ;
#13885=CARTESIAN_POINT ( 'NONE',  ( 112.0622167782374277, -1.849990392679472073, 0.7662911109078888172 ) ) ;
#13890=EDGE_CURVE ( 'NONE', #30108, #15655, #24084, .T. ) ;
#13898=PRODUCT_DEFINITION_SHAPE ( 'NONE', 'NONE',  #10482 ) ;
#13908=CARTESIAN_POINT ( 'NONE',  ( 108.6874999999998010, -1.035533905932749299, -2.499999999999844569 ) ) ;
#13919=CARTESIAN_POINT ( 'NONE',  ( 120.1247167782375698, -1.849990392679523588, 0.000000000000000000 ) ) ;
#13924=FACE_OUTER_BOUND ( 'NONE', #8666, .T. ) ;
#13936=CARTESIAN_POINT ( 'NONE',  ( 119.7113248654050750, 2.000000000000001776, 1.110223024625156540E-13 ) ) ;
#13937=CARTESIAN_POINT ( 'NONE',  ( 104.7497167782376408, 1.308140751793640533, 1.308140751793640533 ) ) ;
#13939=CARTESIAN_POINT ( 'NONE',  ( 117.6877832217621034, -0.7662911109077388261, 1.849990392679712103 ) ) ;
#13945=CARTESIAN_POINT ( 'NONE',  ( 105.2113248654051745, -1.999999999999974021, 0.000000000000000000 ) ) ;
#13964=CARTESIAN_POINT ( 'NONE',  ( 114.5627832217621602, 0.7662911109078588412, 1.849990392679712103 ) ) ;
#13966=VERTEX_POINT ( 'NONE', #5938 ) ;
#13968=ORIENTED_EDGE ( 'NONE', *, *, #10567, .F. ) ;
#13983=CARTESIAN_POINT ( 'NONE',  ( 112.3124999999997726, -1.035533905932598975, 2.500000000000265121 ) ) ;
#13994=CARTESIAN_POINT ( 'NONE',  ( 112.4999999999999147, -2.499999999999835687, 0.000000000000000000 ) ) ;
#13996=CARTESIAN_POINT ( 'NONE',  ( 107.8127832217621318, -1.849990392679472073, 0.7662911109079489913 ) ) ;
#13999=CYLINDRICAL_SURFACE ( 'NONE', #27837, 2.000000000000012879 ) ;
#14001=CARTESIAN_POINT ( 'NONE',  ( 105.9372167782374135, -0.7662911109076184779, 1.849990392679652151 ) ) ;
#14011=CARTESIAN_POINT ( 'NONE',  ( 109.2499999999999147, 0.000000000000000000, 2.499999999999946709 ) ) ;
#14018=CARTESIAN_POINT ( 'NONE',  ( 109.1877832217621034, 0.7662911109079489913, -1.849990392679291551 ) ) ;
#14036=CARTESIAN_POINT ( 'NONE',  ( 111.8122167782374419, 0.7662911109077987781, 1.849990392679772278 ) ) ;
#14041=CARTESIAN_POINT ( 'NONE',  ( 113.3988248654051745, -0.8284271247460852639, -1.999999999999791278 ) ) ;
#14055=CARTESIAN_POINT ( 'NONE',  ( 112.1636751345948113, 1.414213562373034527, -1.414213562373145550 ) ) ;
#14061=CARTESIAN_POINT ( 'NONE',  ( 108.3124999999997442, -1.035533905932629173, 2.500000000000205169 ) ) ;
#14074=CARTESIAN_POINT ( 'NONE',  ( 107.0624999999998010, 2.500000000000114575, 1.035533905932989551 ) ) ;
#14081=VECTOR ( 'NONE', #439, 1000.000000000000000 ) ;
#14089=EDGE_CURVE ( 'NONE', #25684, #29332, #8321, .T. ) ;
#14095=CARTESIAN_POINT ( 'NONE',  ( 118.5627832217621034, 0.7662911109077087390, 1.849990392679772278 ) ) ;
#14111=CARTESIAN_POINT ( 'NONE',  ( 119.4997167782375982, 1.308140751793723799, -1.308140751793640533 ) ) ;
#14117=CARTESIAN_POINT ( 'NONE',  ( 115.5627832217620892, 0.7662911109077987781, 1.849990392679772278 ) ) ;
#14137=CARTESIAN_POINT ( 'NONE',  ( 114.0624999999997300, 2.500000000000114575, 1.035533905932989551 ) ) ;
#14144=VERTEX_POINT ( 'NONE', #2041 ) ;
#14146=CARTESIAN_POINT ( 'NONE',  ( 113.4374999999998863, -2.499999999999994671, 1.035533905932869425 ) ) ;
#14148=CARTESIAN_POINT ( 'NONE',  ( 108.1252832217622455, 0.000000000000000000, -1.849990392679301543 ) ) ;
#14150=ORIENTED_EDGE ( 'NONE', *, *, #14400, .F. ) ;
#14160=EDGE_CURVE ( 'NONE', #15916, #13609, #4333, .T. ) ;
#14165=CARTESIAN_POINT ( 'NONE',  ( 106.7499999999999147, -8.326672684688674053E-14, -2.499999999999946709 ) ) ;
#14169=CARTESIAN_POINT ( 'NONE',  ( 119.2113248654050466, -1.999999999999946265, 2.220446049250313081E-13 ) ) ;
#14171=CARTESIAN_POINT ( 'NONE',  ( 108.1252832217622455, 0.000000000000000000, -1.849990392679301543 ) ) ;
#14174=CARTESIAN_POINT ( 'NONE',  ( 0.000000000000000000, 0.000000000000000000, 0.000000000000000000 ) ) ;
#14179=CARTESIAN_POINT ( 'NONE',  ( 114.7886751345947403, -1.999999999999946265, 0.000000000000000000 ) ) ;
#14186=CARTESIAN_POINT ( 'NONE',  ( 118.6488248654050324, 2.000000000000122125, -0.8284271247459952248 ) ) ;
#14190=CARTESIAN_POINT ( 'NONE',  ( 113.3363248654051176, -1.414213562373201061, -1.414213562373034527 ) ) ;
#14208=CARTESIAN_POINT ( 'NONE',  ( 111.7499999999998010, 0.000000000000000000, -2.499999999999946709 ) ) ;
#14217=CARTESIAN_POINT ( 'NONE',  ( 106.1874999999999289, 1.035533905932839449, 2.500000000000265121 ) ) ;
#14219=MANIFOLD_SOLID_BREP ( 'Cut-Sweep1', #3118 ) ;
#14224=CARTESIAN_POINT ( 'NONE',  ( 118.9999999999998437, 2.500000000000057732, 2.220446049250313081E-13 ) ) ;
#14225=ORIENTED_EDGE ( 'NONE', *, *, #24418, .T. ) ;
#14240=CARTESIAN_POINT ( 'NONE',  ( 105.6247167782375271, 1.849990392679495832, 0.000000000000000000 ) ) ;
#14241=CARTESIAN_POINT ( 'NONE',  ( 120.0627832217621602, -0.7662911109077388261, -1.849990392679291551 ) ) ;
#14257=CARTESIAN_POINT ( 'NONE',  ( 117.1247167782376408, -1.849990392679579099, 1.110223024625156540E-13 ) ) ;
#14267=ORIENTED_EDGE ( 'NONE', *, *, #20001, .T. ) ;
#14278=CARTESIAN_POINT ( 'NONE',  ( 110.4374999999997442, -2.500000000000024425, 1.035533905932809473 ) ) ;
#14281=CARTESIAN_POINT ( 'NONE',  ( 115.2886751345946550, 2.000000000000112799, 3.330669073875469621E-13 ) ) ;
#14289=CARTESIAN_POINT ( 'NONE',  ( 112.1249999999998437, 1.767766952966293159, 1.767766952966431937 ) ) ;
#14292=CARTESIAN_POINT ( 'NONE',  ( 106.8127832217621602, -1.849990392679441875, 0.7662911109078888172 ) ) ;
#14294=EDGE_CURVE ( 'NONE', #15655, #3485, #5245, .T. ) ;
#14298=CARTESIAN_POINT ( 'NONE',  ( 106.9997167782376550, -1.308140751793612777, 1.308140751793640533 ) ) ;
#14301=VECTOR ( 'NONE', #16342, 1000.000000000000000 ) ;
#14309=CARTESIAN_POINT ( 'NONE',  ( 109.7499999999999147, 5.551115123125782702E-14, -2.499999999999835687 ) ) ;
#14315=CARTESIAN_POINT ( 'NONE',  ( 109.8127832217621034, -1.849990392679501827, 0.7662911109077686911 ) ) ;
#14321=UNCERTAINTY_MEASURE_WITH_UNIT (LENGTH_MEASURE( 1.000000000000000082E-05 ), #24252, 'distance_accuracy_value', 'NONE');
#14348=CARTESIAN_POINT ( 'NONE',  ( 117.3363248654050892, -1.414213562373256572, -1.414213562372923505 ) ) ;
#14356=CARTESIAN_POINT ( 'NONE',  ( 107.5624999999998153, -2.499999999999874767, -1.035533905932629173 ) ) ;
#14367=CARTESIAN_POINT ( 'NONE',  ( 118.4997167782374135, 1.308140751793696044, -1.308140751793640533 ) ) ;
#14371=( BOUNDED_CURVE ( )  B_SPLINE_CURVE ( 2, ( #7304, #522, #9915, #9763, #21288, #16708, #4977, #28615, #19138 ),
 .UNSPECIFIED., .F., .T. ) 
 B_SPLINE_CURVE_WITH_KNOTS ( ( 3, 2, 2, 2, 3 ),
 ( 0.8235294117647058432, 0.8308823529411764053, 0.8382352941176470784, 0.8455882352941176405, 0.8529411764705882026 ),
 .UNSPECIFIED. ) 
 CURVE ( )  GEOMETRIC_REPRESENTATION_ITEM ( )  RATIONAL_B_SPLINE_CURVE ( ( 1.000000000000000000, 0.9238795325112867385, 1.000000000000000000, 0.9238795325112867385, 1.000000000000000000, 0.9238795325112867385, 1.000000000000000000, 0.9238795325112867385, 1.000000000000000000 ) ) 
 REPRESENTATION_ITEM ( '' )  );
#14373=CARTESIAN_POINT ( 'NONE',  ( 116.7499999999997584, 1.665334536937734811E-13, -2.499999999999724665 ) ) ;
#14377=EDGE_LOOP ( 'NONE', ( #22574, #28735, #1325 ) ) ;
#14381=CARTESIAN_POINT ( 'NONE',  ( 109.2261751345945697, 2.000000000000122125, -0.8284271247459952248 ) ) ;
#14387=CARTESIAN_POINT ( 'NONE',  ( 106.9372167782374703, -0.7662911109076785410, 1.849990392679772278 ) ) ;
#14389=CARTESIAN_POINT ( 'NONE',  ( 113.6252832217621460, 1.665334536937734811E-13, 1.849990392679745632 ) ) ;
#14400=EDGE_CURVE ( 'NONE', #14144, #2147, #11587, .T. ) ;
#14403=CARTESIAN_POINT ( 'NONE',  ( 104.9999999999998863, -0.4876318259229017738, -1.939643060551943243 ) ) ;
#14408=CARTESIAN_POINT ( 'NONE',  ( 115.5622167782373850, 1.849990392679532247, -0.7662911109075883909 ) ) ;
#14412=CARTESIAN_POINT ( 'NONE',  ( 114.8127832217620465, -1.849990392679591977, 0.7662911109078888172 ) ) ;
#14421=CARTESIAN_POINT ( 'NONE',  ( 110.7886751345946834, -1.999999999999946265, 0.000000000000000000 ) ) ;
#14429=CARTESIAN_POINT ( 'NONE',  ( 113.6249999999998721, -1.767766952966376426, -1.767766952966431937 ) ) ;
#14437=CARTESIAN_POINT ( 'NONE',  ( 109.5238248654049471, 0.8284271247463257382, -1.999999999999791278 ) ) ;
#14438=CARTESIAN_POINT ( 'NONE',  ( 112.5624999999998010, -2.499999999999994671, -1.035533905932689347 ) ) ;
#14440=CARTESIAN_POINT ( 'NONE',  ( 106.7502832217622597, -1.308140751793529510, 1.308140751793973600 ) ) ;
#14444=CARTESIAN_POINT ( 'NONE',  ( 107.2497167782375129, -1.308140751793585022, -1.308140751793640533 ) ) ;
#14453=CARTESIAN_POINT ( 'NONE',  ( 108.6249999999999289, -1.767766952966320915, -1.767766952966320915 ) ) ;
#14462=CARTESIAN_POINT ( 'NONE',  ( 106.1252832217622171, -5.551115123125782702E-14, -1.849990392679523588 ) ) ;
#14487=VERTEX_POINT ( 'NONE', #13560 ) ;
#14501=CARTESIAN_POINT ( 'NONE',  ( 106.3124999999997584, -1.035533905932659149, 2.500000000000205169 ) ) ;
#14507=CARTESIAN_POINT ( 'NONE',  ( 118.5622167782375698, 1.849990392679621953, -0.7662911109077087390 ) ) ;
#14512=CARTESIAN_POINT ( 'NONE',  ( 117.3750000000000142, -1.767766952966320915, 1.767766952966431937 ) ) ;
#14526=CARTESIAN_POINT ( 'NONE',  ( 105.3122167782374277, -0.7662911109076785410, -1.849990392679231599 ) ) ;
#14527=CARTESIAN_POINT ( 'NONE',  ( 113.7502832217623023, -1.308140751793585022, 1.308140751793640533 ) ) ;
#14536=CARTESIAN_POINT ( 'NONE',  ( 108.4136751345946692, 1.414213562373201061, 1.414213562373256572 ) ) ;
#14545=CARTESIAN_POINT ( 'NONE',  ( 112.8752832217622029, -1.849990392679384810, 0.000000000000000000 ) ) ;
#14551=VERTEX_POINT ( 'NONE', #292 ) ;
#14555=ORIENTED_EDGE ( 'NONE', *, *, #11178, .F. ) ;
#14556=CARTESIAN_POINT ( 'NONE',  ( 107.7261751345945839, -1.999999999999941602, 0.8284271247462955401 ) ) ;
#14559=DIRECTION ( 'NONE',  ( -1.000000000000000000, -5.551115123125765446E-17, -2.220446049250314560E-16 ) ) ;
#14569=CARTESIAN_POINT ( 'NONE',  ( 113.3124999999997300, -1.035533905932598975, 2.500000000000144773 ) ) ;
#14572=ORIENTED_EDGE ( 'NONE', *, *, #19622, .T. ) ;
#14575=CARTESIAN_POINT ( 'NONE',  ( 104.5622167782374703, 1.849990392679501827, -0.7662911109076485650 ) ) ;
#14588=CARTESIAN_POINT ( 'NONE',  ( 109.4999999999998579, -2.499999999999891198, 2.220446049250313081E-13 ) ) ;
#14592=ORIENTED_EDGE ( 'NONE', *, *, #647, .T. ) ;
#14596=CARTESIAN_POINT ( 'NONE',  ( 106.6877832217621602, -0.7662911109076785410, 1.849990392679712103 ) ) ;
#14609=AXIS2_PLACEMENT_3D ( 'NONE', #9758, #11956, #2671 ) ;
#14611=CARTESIAN_POINT ( 'NONE',  ( 119.9999999999997868, -5.999999999999873879, 1.056932319443148900E-13 ) ) ;
#14629=VECTOR ( 'NONE', #17473, 1000.000000000000000 ) ;
#14640=CARTESIAN_POINT ( 'NONE',  ( 108.2113248654050892, -1.999999999999946265, 0.000000000000000000 ) ) ;
#14643=CARTESIAN_POINT ( 'NONE',  ( 118.2886751345946976, 2.000000000000085265, 0.000000000000000000 ) ) ;
#14645=CARTESIAN_POINT ( 'NONE',  ( 118.3122167782374561, -0.7662911109076485650, -1.849990392679411677 ) ) ;
#14653=CARTESIAN_POINT ( 'NONE',  ( 118.7499999999997868, -1.665334536937734811E-13, -2.500000000000057732 ) ) ;
#14656=VERTEX_POINT ( 'NONE', #7652 ) ;
#14666=CARTESIAN_POINT ( 'NONE',  ( 116.0627832217622029, -0.7662911109076785410, -1.849990392679291551 ) ) ;
#14694=CARTESIAN_POINT ( 'NONE',  ( 119.9999999999998437, 0.8621349163126781345, 2.008502556958250640 ) ) ;
#14696=FACE_OUTER_BOUND ( 'NONE', #4265, .T. ) ;
#14703=DIRECTION ( 'NONE',  ( -1.000000000000000000, -1.665334536937736783E-16, -2.220446049250315546E-16 ) ) ;
#14715=CARTESIAN_POINT ( 'NONE',  ( 109.5624999999997158, -2.499999999999994671, -1.035533905932508825 ) ) ;
#14723=CARTESIAN_POINT ( 'NONE',  ( 104.1247167782375556, -1.849990392679468076, 0.000000000000000000 ) ) ;
#14724=EDGE_LOOP ( 'NONE', ( #8457, #15960, #30272, #28909, #20595 ) ) ;
#14739=CARTESIAN_POINT ( 'NONE',  ( 119.3749999999998863, -1.767766952966209892, 1.767766952966542959 ) ) ;
#14743=CARTESIAN_POINT ( 'NONE',  ( 113.6011751345946124, -0.8284271247461753029, 2.000000000000271783 ) ) ;
#14770=STYLED_ITEM ( 'NONE', ( #13392 ), #27710 ) ;
#14777=CARTESIAN_POINT ( 'NONE',  ( 101.5358983848621932, 0.000000000000000000, 0.000000000000000000 ) ) ;
#14780=CARTESIAN_POINT ( 'NONE',  ( 104.7499999999998295, 5.551115123125782702E-14, -2.499999999999835687 ) ) ;
#14787=CARTESIAN_POINT ( 'NONE',  ( 108.0386751345947687, 5.551115123125782702E-14, -2.000000000000001776 ) ) ;
#14789=CARTESIAN_POINT ( 'NONE',  ( 117.9761751345946408, -0.8284271247461453269, -1.999999999999851674 ) ) ;
#14792=CARTESIAN_POINT ( 'NONE',  ( 116.1247167782375556, -1.849990392679468076, 1.110223024625156540E-13 ) ) ;
#14800=CARTESIAN_POINT ( 'NONE',  ( 118.6874999999998295, -1.035533905932719101, -2.499999999999844569 ) ) ;
#14811=LINE ( 'NONE', #12230, #27998 ) ;
#14814=VECTOR ( 'NONE', #21689, 1000.000000000000000 ) ;
#14817=CARTESIAN_POINT ( 'NONE',  ( 116.6252832217622313, 0.000000000000000000, 1.849990392679523588 ) ) ;
#14835=CARTESIAN_POINT ( 'NONE',  ( 104.8954487758440877, 0.3872062312935020123, 1.908582334821284254 ) ) ;
#14852=B_SPLINE_CURVE_WITH_KNOTS ( 'NONE', 3,
 ( #6769, #18473, #4312, #18327, #22762, #20307, #8620, #27944 ),
 .UNSPECIFIED., .F., .F.,
 ( 4, 2, 2, 4 ),
 ( 0.000000000000000000, 0.0006652843935019894924, 0.0009979265902529841845, 0.001330568787003978985 ),
 .UNSPECIFIED. ) ;
#14865=CARTESIAN_POINT ( 'NONE',  ( 120.6252832217622881, 2.775557561562891351E-14, 1.849990392679523588 ) ) ;
#14885=CARTESIAN_POINT ( 'NONE',  ( 105.1252832217623023, -5.551115123125782702E-14, -1.849990392679523588 ) ) ;
#14896=CARTESIAN_POINT ( 'NONE',  ( 120.4374999999997442, -2.499999999999964473, 1.035533905932989551 ) ) ;
#14904=ORIENTED_EDGE ( 'NONE', *, *, #15605, .T. ) ;
#14906=PRODUCT_DEFINITION_FORMATION_WITH_SPECIFIED_SOURCE ( 'ANY', '', #6474, .NOT_KNOWN. ) ;
#14928=CARTESIAN_POINT ( 'NONE',  ( 107.7499999999998579, 5.551115123125782702E-14, -2.499999999999946709 ) ) ;
#14935=CARTESIAN_POINT ( 'NONE',  ( 112.6636751345946976, -1.414213562373062283, 1.414213562373034527 ) ) ;
#14938=CARTESIAN_POINT ( 'NONE',  ( 118.1872167782374845, -1.849990392679472073, -0.7662911109076485650 ) ) ;
#14943=CARTESIAN_POINT ( 'NONE',  ( 112.6249999999998437, -1.767766952966431937, -1.767766952966320915 ) ) ;
#14945=CARTESIAN_POINT ( 'NONE',  ( 0.000000000000000000, 0.000000000000000000, 0.000000000000000000 ) ) ;
#14971=CARTESIAN_POINT ( 'NONE',  ( 115.0238248654049329, -0.8284271247460852639, 2.000000000000212275 ) ) ;
#14972=CARTESIAN_POINT ( 'NONE',  ( 114.4997167782375413, 1.308140751793696044, -1.308140751793640533 ) ) ;
#14987=CARTESIAN_POINT ( 'NONE',  ( 119.9999999999998579, 1.752251084798616354, 1.505035388670107999 ) ) ;
#15015=CARTESIAN_POINT ( 'NONE',  ( 119.8127832217621460, -1.849990392679381701, 0.7662911109078287542 ) ) ;
#15020=ORIENTED_EDGE ( 'NONE', *, *, #24154, .F. ) ;
#15024=ORIENTED_EDGE ( 'NONE', *, *, #46, .F. ) ;
#15027=CARTESIAN_POINT ( 'NONE',  ( 106.2499999999999716, -2.775557561562891351E-14, 2.499999999999946709 ) ) ;
#15034=CARTESIAN_POINT ( 'NONE',  ( 119.4999999999999289, -2.499999999999919176, 0.000000000000000000 ) ) ;
#15040=CYLINDRICAL_SURFACE ( 'NONE', #24701, 2.000000000000012879 ) ;
#15047=CARTESIAN_POINT ( 'NONE',  ( 119.6874999999998010, -1.035533905932809473, -2.499999999999784173 ) ) ;
#15089=CARTESIAN_POINT ( 'NONE',  ( 108.6636751345948113, -1.414213562373062283, 1.414213562373256572 ) ) ;
#15092=CARTESIAN_POINT ( 'NONE',  ( 113.6247167782374987, 1.849990392679551343, 0.000000000000000000 ) ) ;
#15093=CARTESIAN_POINT ( 'NONE',  ( 118.7261751345945981, -1.999999999999941602, 0.8284271247463557142 ) ) ;
#15098=CARTESIAN_POINT ( 'NONE',  ( 113.6874999999998437, -1.035533905932749299, -2.499999999999904521 ) ) ;
#15115=CARTESIAN_POINT ( 'NONE',  ( 105.7886751345946550, -1.999999999999946265, 0.000000000000000000 ) ) ;
#15130=CARTESIAN_POINT ( 'NONE',  ( 113.5622167782373850, 1.849990392679621953, -0.7662911109075283278 ) ) ;
#15151=CARTESIAN_POINT ( 'NONE',  ( 118.0238248654050182, -0.8284271247461153509, 2.000000000000212275 ) ) ;
#15153=PRESENTATION_STYLE_ASSIGNMENT (( #27819 ) ) ;
#15154=EDGE_CURVE ( 'NONE', #4691, #6944, #11026, .T. ) ;
#15156=CARTESIAN_POINT ( 'NONE',  ( 104.1247167782375556, -1.849990392679468076, 0.000000000000000000 ) ) ;
#15171=CARTESIAN_POINT ( 'NONE',  ( 104.4372167782374419, 0.7662911109077987781, -1.849990392679231599 ) ) ;
#15179=CARTESIAN_POINT ( 'NONE',  ( 105.3124999999998437, -1.035533905932598975, 2.500000000000265121 ) ) ;
#15188=CARTESIAN_POINT ( 'NONE',  ( 119.1488248654049187, -1.999999999999941602, 0.8284271247464759513 ) ) ;
#15190=CARTESIAN_POINT ( 'NONE',  ( 105.1877832217621176, 0.7662911109078588412, -1.849990392679291551 ) ) ;
#15200=DIRECTION ( 'NONE',  ( 5.551115123125785167E-17, -1.000000000000000000, -8.881784197001256268E-16 ) ) ;
#15229=FACE_OUTER_BOUND ( 'NONE', #30087, .T. ) ;
#15251=CARTESIAN_POINT ( 'NONE',  ( 113.5622167782373850, 1.849990392679621953, -0.7662911109075283278 ) ) ;
#15256=CARTESIAN_POINT ( 'NONE',  ( 106.2113248654051745, -1.999999999999946265, 0.000000000000000000 ) ) ;
#15257=CARTESIAN_POINT ( 'NONE',  ( 112.3749999999999289, -1.767766952966320915, 1.767766952966431937 ) ) ;
#15262=ORIENTED_EDGE ( 'NONE', *, *, #29570, .F. ) ;
#15275=CARTESIAN_POINT ( 'NONE',  ( 109.7886751345948255, -2.000000000000001776, 0.000000000000000000 ) ) ;
#15293=CARTESIAN_POINT ( 'NONE',  ( 110.9372167782374277, -0.7662911109077686911, 1.849990392679591977 ) ) ;
#15305=EDGE_CURVE ( 'NONE', #7046, #14487, #24898, .T. ) ;
#15307=AXIS2_PLACEMENT_3D ( 'NONE', #25312, #9207, #18600 ) ;
#15315=CARTESIAN_POINT ( 'NONE',  ( 110.7886751345946834, -1.999999999999946265, 0.000000000000000000 ) ) ;
#15325=UNCERTAINTY_MEASURE_WITH_UNIT (LENGTH_MEASURE( 1.000000000000000082E-05 ), #20636, 'distance_accuracy_value', 'NONE');
#15340=CARTESIAN_POINT ( 'NONE',  ( 1.110223024625164183E-16, -2.000000000000012879, -1.776356839400262692E-15 ) ) ;
#15342=CARTESIAN_POINT ( 'NONE',  ( 117.1252832217621460, -5.551115123125782702E-14, -1.849990392679523588 ) ) ;
#15353=CARTESIAN_POINT ( 'NONE',  ( 104.5624999999997442, -2.499999999999934719, -1.035533905932689347 ) ) ;
#15361=CARTESIAN_POINT ( 'NONE',  ( 105.9377832217620323, -1.849990392679441875, -0.7662911109074682647 ) ) ;
#15374=CARTESIAN_POINT ( 'NONE',  ( 112.0002832217622739, -1.308140751793557266, -1.308140751793640533 ) ) ;
#15391=SURFACE_SIDE_STYLE ('',( #8268 ) ) ;
#15394=CARTESIAN_POINT ( 'NONE',  ( 107.3511751345946266, 2.000000000000061728, 0.8284271247462955401 ) ) ;
#15398=CARTESIAN_POINT ( 'NONE',  ( 104.7401757384973280, 1.387249626875697306, 1.223929297688219897 ) ) ;
#15402=CARTESIAN_POINT ( 'NONE',  ( 114.0002832217621602, -1.308140751793585022, -1.308140751793640533 ) ) ;
#15418=CARTESIAN_POINT ( 'NONE',  ( 113.1247167782375556, -1.849990392679523588, 1.110223024625156540E-13 ) ) ;
#15422=CARTESIAN_POINT ( 'NONE',  ( 116.1249999999999574, 1.767766952966265404, 1.767766952966431937 ) ) ;
#15445=ORIENTED_EDGE ( 'NONE', *, *, #8921, .F. ) ;
#15447=FACE_OUTER_BOUND ( 'NONE', #2130, .T. ) ;
#15450=VERTEX_POINT ( 'NONE', #5662 ) ;
#15451=CARTESIAN_POINT ( 'NONE',  ( 110.1874999999997584, 1.035533905932779275, 2.500000000000205169 ) ) ;
#15472=CARTESIAN_POINT ( 'NONE',  ( 110.7261751345945413, -1.999999999999971800, 0.8284271247464157772 ) ) ;
#15478=CARTESIAN_POINT ( 'NONE',  ( 104.4997167782375413, 1.308140751793668288, -1.308140751793640533 ) ) ;
#15495=CARTESIAN_POINT ( 'NONE',  ( 117.4377832217621602, 1.849990392679562001, 0.7662911109079489913 ) ) ;
#15506=AXIS2_PLACEMENT_3D ( 'NONE', #23444, #25727, #25407 ) ;
#15513=CARTESIAN_POINT ( 'NONE',  ( 114.7499999999999147, -5.551115123125782702E-14, -2.499999999999946709 ) ) ;
#15525=CARTESIAN_POINT ( 'NONE',  ( 117.9374999999998721, 2.500000000000114575, -1.035533905932448873 ) ) ;
#15527=CARTESIAN_POINT ( 'NONE',  ( 109.1252832217621744, -1.665334536937734811E-13, -1.849990392679523588 ) ) ;
#15538=CARTESIAN_POINT ( 'NONE',  ( 115.8988248654050750, 0.8284271247463257382, 2.000000000000271783 ) ) ;
#15550=ORIENTED_EDGE ( 'NONE', *, *, #30265, .T. ) ;
#15557=CARTESIAN_POINT ( 'NONE',  ( 110.8127832217621318, -1.849990392679381701, 0.7662911109078888172 ) ) ;
#15566=CARTESIAN_POINT ( 'NONE',  ( 104.7401757384973138, -0.5936465683476789268, -1.756393372907816719 ) ) ;
#15575=CARTESIAN_POINT ( 'NONE',  ( 113.6872167782373850, 1.849990392679532247, 0.7662911109078888172 ) ) ;
#15577=CARTESIAN_POINT ( 'NONE',  ( 114.1636751345947829, 1.414213562373145550, -1.414213562372812483 ) ) ;
#15581=VERTEX_POINT ( 'NONE', #15398 ) ;
#15594=DIRECTION ( 'NONE',  ( -1.000000000000000000, -1.665334536937736783E-16, -2.220446049250315546E-16 ) ) ;
#15605=EDGE_CURVE ( 'NONE', #14656, #23965, #18144, .T. ) ;
#15608=CARTESIAN_POINT ( 'NONE',  ( 109.6249999999999858, -1.767766952966376426, -1.767766952966320915 ) ) ;
#15613=VECTOR ( 'NONE', #5568, 1000.000000000000000 ) ;
#15636=LINE ( 'NONE', #24946, #5620 ) ;
#15644=CARTESIAN_POINT ( 'NONE',  ( 113.2113248654051034, -1.999999999999918510, 1.110223024625156540E-13 ) ) ;
#15645=CARTESIAN_POINT ( 'NONE',  ( 119.8122167782374277, 0.7662911109078588412, 1.849990392679712103 ) ) ;
#15652=CARTESIAN_POINT ( 'NONE',  ( 116.2502832217621886, 1.308140751793612777, -1.308140751793418488 ) ) ;
#15654=ORIENTED_EDGE ( 'NONE', *, *, #1550, .T. ) ;
#15655=VERTEX_POINT ( 'NONE', #24870 ) ;
#15669=CARTESIAN_POINT ( 'NONE',  ( 116.4374999999997726, -2.499999999999934719, 1.035533905932929599 ) ) ;
#15673=ADVANCED_FACE ( 'NONE', ( #15229 ), #22589, .F. ) ;
#15681=CARTESIAN_POINT ( 'NONE',  ( 115.4374999999997868, -2.499999999999934719, 1.035533905932929599 ) ) ;
#15682=CARTESIAN_POINT ( 'NONE',  ( 109.7502832217623734, -1.308140751793612777, 1.308140751793640533 ) ) ;
#15684=CARTESIAN_POINT ( 'NONE',  ( 109.0622167782374561, -1.849990392679501827, 0.7662911109077686911 ) ) ;
#15690=ORIENTED_EDGE ( 'NONE', *, *, #18609, .F. ) ;
#15709=CARTESIAN_POINT ( 'NONE',  ( 111.0627832217621602, -0.7662911109077987781, -1.849990392679291551 ) ) ;
#15714=CARTESIAN_POINT ( 'NONE',  ( 119.9999999999999289, 2.500000000000057732, 1.110223024625156540E-13 ) ) ;
#15723=CYLINDRICAL_SURFACE ( 'NONE', #9687, 2.000000000000012879 ) ;
#15727=CARTESIAN_POINT ( 'NONE',  ( 113.9997167782376266, -1.308140751793585022, 1.308140751793862577 ) ) ;
#15734=VERTEX_POINT ( 'NONE', #16721 ) ;
#15741=CARTESIAN_POINT ( 'NONE',  ( 117.2886751345947971, 2.000000000000140332, 2.220446049250313081E-13 ) ) ;
#15751=CARTESIAN_POINT ( 'NONE',  ( 106.3511751345947118, 2.000000000000091926, 0.8284271247462955401 ) ) ;
#15763=CARTESIAN_POINT ( 'NONE',  ( 108.7499999999998579, 8.326672684688674053E-14, -2.499999999999835687 ) ) ;
#15771=CARTESIAN_POINT ( 'NONE',  ( 119.9999999999999289, 2.500000000000057732, 1.110223024625156540E-13 ) ) ;
#15780=EDGE_CURVE ( 'NONE', #18409, #4573, #4717, .T. ) ;
#15812=VERTEX_POINT ( 'NONE', #12116 ) ;
#15815=ADVANCED_FACE ( 'NONE', ( #18448 ), #11394, .F. ) ;
#15827=CARTESIAN_POINT ( 'NONE',  ( 116.9999999999999005, 2.500000000000057732, 1.110223024625156540E-13 ) ) ;
#15829=CIRCLE ( 'NONE', #1058, 5.999999999999999112 ) ;
#15839=CARTESIAN_POINT ( 'NONE',  ( 117.7499999999998721, 1.387778780781445676E-13, -2.499999999999835687 ) ) ;
#15840=CARTESIAN_POINT ( 'NONE',  ( 108.6252832217621886, 5.551115123125782702E-14, 1.849990392679634610 ) ) ;
#15841=CARTESIAN_POINT ( 'NONE',  ( 108.0238248654050182, -0.8284271247461753029, 2.000000000000271783 ) ) ;
#15843=CARTESIAN_POINT ( 'NONE',  ( 109.9613248654051461, 5.551115123125782702E-14, 2.000000000000112799 ) ) ;
#15868=CARTESIAN_POINT ( 'NONE',  ( 112.8752832217622029, -1.849990392679384810, 0.000000000000000000 ) ) ;
#15877=CARTESIAN_POINT ( 'NONE',  ( 104.7401757384973564, 0.1229795387093424036, -1.849864891959644098 ) ) ;
#15878=ORIENTED_EDGE ( 'NONE', *, *, #5508, .F. ) ;
#15883=CARTESIAN_POINT ( 'NONE',  ( 108.1247167782375556, -1.849990392679468076, 2.220446049250313081E-13 ) ) ;
#15902=( BOUNDED_CURVE ( )  B_SPLINE_CURVE ( 2, ( #17935, #1458, #3906, #20225, #11168, #27550, #29405, #4061, #27401 ),
 .UNSPECIFIED., .F., .T. ) 
 B_SPLINE_CURVE_WITH_KNOTS ( ( 3, 2, 2, 2, 3 ),
 ( 0.3529411764705882582, 0.3602941176470588203, 0.3676470588235294379, 0.3750000000000000000, 0.3823529411764705621 ),
 .UNSPECIFIED. ) 
 CURVE ( )  GEOMETRIC_REPRESENTATION_ITEM ( )  RATIONAL_B_SPLINE_CURVE ( ( 1.000000000000000000, 0.9238795325112867385, 1.000000000000000000, 0.9238795325112867385, 1.000000000000000000, 0.9238795325112867385, 1.000000000000000000, 0.9238795325112867385, 1.000000000000000000 ) ) 
 REPRESENTATION_ITEM ( '' )  );
#15916=VERTEX_POINT ( 'NONE', #19303 ) ;
#15919=CARTESIAN_POINT ( 'NONE',  ( 120.3747167782374277, 0.000000000000000000, -1.849990392679301543 ) ) ;
#15926=EDGE_LOOP ( 'NONE', ( #29578, #1857, #15654, #21057 ) ) ;
#15943=DIRECTION ( 'NONE',  ( 0.8660254037844380415, -0.5000000000000008882, -1.905606012543395233E-16 ) ) ;
#15952=CARTESIAN_POINT ( 'NONE',  ( 119.3122167782375556, -0.7662911109076785410, -1.849990392679411677 ) ) ;
#15959=ORIENTED_EDGE ( 'NONE', *, *, #22928, .T. ) ;
#15960=ORIENTED_EDGE ( 'NONE', *, *, #8248, .T. ) ;
#15963=CARTESIAN_POINT ( 'NONE',  ( 115.5863248654050892, 1.414213562373201061, -1.414213562373145550 ) ) ;
#15975=CARTESIAN_POINT ( 'NONE',  ( 117.3750000000000142, -1.767766952966320915, 1.767766952966431937 ) ) ;
#15985=CARTESIAN_POINT ( 'NONE',  ( 117.3124999999997300, -1.035533905932689347, 2.500000000000265121 ) ) ;
#15988=CARTESIAN_POINT ( 'NONE',  ( 112.3127832217622455, 1.849990392679411677, -0.7662911109077087390 ) ) ;
#15990=ADVANCED_FACE ( 'NONE', ( #24478 ), #26626, .F. ) ;
#15994=CARTESIAN_POINT ( 'NONE',  ( 107.9997167782376835, -1.308140751793585022, 1.308140751793640533 ) ) ;
#16001=ORIENTED_EDGE ( 'NONE', *, *, #30402, .F. ) ;
#16015=CARTESIAN_POINT ( 'NONE',  ( 113.3127832217621176, 1.849990392679501827, -0.7662911109077087390 ) ) ;
#16035=CARTESIAN_POINT ( 'NONE',  ( 109.4372167782374845, 0.7662911109079189043, -1.849990392679231599 ) ) ;
#16037=CARTESIAN_POINT ( 'NONE',  ( 113.3747167782374987, -1.110223024625156540E-13, -1.849990392679523588 ) ) ;
#16040=CARTESIAN_POINT ( 'NONE',  ( 113.5238248654049471, 0.8284271247463257382, -1.999999999999791278 ) ) ;
#16042=ORIENTED_EDGE ( 'NONE', *, *, #18463, .T. ) ;
#16062=CARTESIAN_POINT ( 'NONE',  ( 111.3749999999999289, -1.767766952966320915, 1.767766952966431937 ) ) ;
#16073=CARTESIAN_POINT ( 'NONE',  ( 106.3124999999997584, -1.035533905932659149, 2.500000000000205169 ) ) ;
#16089=CARTESIAN_POINT ( 'NONE',  ( 118.6877832217621460, -0.7662911109076785410, 1.849990392679712103 ) ) ;
#16098=CARTESIAN_POINT ( 'NONE',  ( 117.0863248654050892, -1.414213562373090038, 1.414213562373256572 ) ) ;
#16108=DIRECTION ( 'NONE',  ( -1.000000000000000000, -1.665334536937736783E-16, -2.220446049250315546E-16 ) ) ;
#16109=CARTESIAN_POINT ( 'NONE',  ( 116.9997167782375698, -1.308140751793557266, 1.308140751793862577 ) ) ;
#16130=CARTESIAN_POINT ( 'NONE',  ( 117.3124999999997300, -1.035533905932689347, 2.500000000000265121 ) ) ;
#16140=CARTESIAN_POINT ( 'NONE',  ( 118.7499999999997868, -1.665334536937734811E-13, -2.500000000000057732 ) ) ;
#16142=CARTESIAN_POINT ( 'NONE',  ( 107.6877832217621744, -0.7662911109077987781, 1.849990392679652151 ) ) ;
#16147=VERTEX_POINT ( 'NONE', #25338 ) ;
#16151=B_SPLINE_CURVE_WITH_KNOTS ( 'NONE', 3,
 ( #15714, #10624, #24878, #5670, #17858, #12950, #27176, #26861, #1077, #3828, #10941, #5821, #22748, #8285, #10467, #3979, #20289, #6147 ),
 .UNSPECIFIED., .F., .F.,
 ( 4, 2, 2, 2, 2, 2, 2, 2, 4 ),
 ( 0.000000000000000000, 0.0005121067916115667898, 0.001024213583223133580, 0.001536320374834700695, 0.002048427166446268027, 0.002560533958057835575, 0.003072640749669401823, 0.003584747541280968938, 0.004096854332892535186 ),
 .UNSPECIFIED. ) ;
#16161=EDGE_CURVE ( 'NONE', #9582, #14656, #2736, .T. ) ;
#16170=CARTESIAN_POINT ( 'NONE',  ( 112.5627832217621886, 0.7662911109078588412, 1.849990392679712103 ) ) ;
#16185=CARTESIAN_POINT ( 'NONE',  ( 109.7497167782375698, 1.308140751793640533, 1.308140751793862577 ) ) ;
#16202=EDGE_CURVE ( 'NONE', #15581, #30081, #14852, .T. ) ;
#16209=CARTESIAN_POINT ( 'NONE',  ( 109.9999999999999432, 2.500000000000030198, 0.000000000000000000 ) ) ;
#16221=CARTESIAN_POINT ( 'NONE',  ( 107.2499999999999147, 0.000000000000000000, 2.499999999999946709 ) ) ;
#16227=CARTESIAN_POINT ( 'NONE',  ( 119.9374999999996874, 2.499999999999852118, -1.035533905932651377 ) ) ;
#16234=VERTEX_POINT ( 'NONE', #6307 ) ;
#16235=VECTOR ( 'NONE', #25209, 1000.000000000000227 ) ;
#16239=CARTESIAN_POINT ( 'NONE',  ( 119.8988248654050324, 0.8284271247462654530, 2.000000000000151879 ) ) ;
#16241=DIRECTION ( 'NONE',  ( 5.551115123125785167E-17, -1.000000000000000000, -8.881784197001256268E-16 ) ) ;
#16242=CARTESIAN_POINT ( 'NONE',  ( 119.5002832217621886, 1.308140751793640533, 1.308140751793751555 ) ) ;
#16248=CARTESIAN_POINT ( 'NONE',  ( 105.3988248654049471, -0.8284271247460852639, -1.999999999999851674 ) ) ;
#16260=CARTESIAN_POINT ( 'NONE',  ( 117.4372167782373566, 0.7662911109078888172, -1.849990392679411677 ) ) ;
#16266=CARTESIAN_POINT ( 'NONE',  ( 113.4377832217621460, 1.849990392679591977, 0.7662911109080692285 ) ) ;
#16270=VERTEX_POINT ( 'NONE', #13417 ) ;
#16274=EDGE_CURVE ( 'NONE', #27307, #22257, #19448, .T. ) ;
#16279=DIRECTION ( 'NONE',  ( 5.551115123125785167E-17, -1.000000000000000000, -8.881784197001256268E-16 ) ) ;
#16295=CARTESIAN_POINT ( 'NONE',  ( 112.7499999999998579, -5.551115123125782702E-14, -2.499999999999946709 ) ) ;
#16298=CARTESIAN_POINT ( 'NONE',  ( 107.6252832217623308, -2.775557561562891351E-14, 1.849990392679523588 ) ) ;
#16311=EDGE_CURVE ( 'NONE', #19788, #16147, #9543, .T. ) ;
#16322=CARTESIAN_POINT ( 'NONE',  ( 108.3127832217620181, 1.849990392679562001, -0.7662911109076485650 ) ) ;
#16335=CARTESIAN_POINT ( 'NONE',  ( 111.3747167782376692, -5.551115123125782702E-14, -1.849990392679523588 ) ) ;
#16342=DIRECTION ( 'NONE',  ( -1.000000000000000000, -1.665334536937736783E-16, -2.220446049250315546E-16 ) ) ;
#16359=CARTESIAN_POINT ( 'NONE',  ( 108.8749999999999574, 1.767766952966265404, -1.767766952966320915 ) ) ;
#16361=CARTESIAN_POINT ( 'NONE',  ( 115.2261751345946266, 2.000000000000091926, -0.8284271247459952248 ) ) ;
#16368=CARTESIAN_POINT ( 'NONE',  ( 120.6247167782375413, 1.849990392679579099, 0.000000000000000000 ) ) ;
#16386=CARTESIAN_POINT ( 'NONE',  ( 106.3122167782376124, -0.7662911109076184779, -1.849990392679351725 ) ) ;
#16388=CARTESIAN_POINT ( 'NONE',  ( 120.3752832217621460, 1.849990392679579099, 0.000000000000000000 ) ) ;
#16405=FACE_OUTER_BOUND ( 'NONE', #4343, .T. ) ;
#16409=CARTESIAN_POINT ( 'NONE',  ( 117.6872167782374845, 1.849990392679621953, 0.7662911109078287542 ) ) ;
#16415=CARTESIAN_POINT ( 'NONE',  ( 113.5002832217622455, 1.308140751793696044, 1.308140751793640533 ) ) ;
#16417=EDGE_LOOP ( 'NONE', ( #9690, #25765, #14592, #14555 ) ) ;
#16431=CARTESIAN_POINT ( 'NONE',  ( 110.8124999999999432, 1.035533905932719101, -2.499999999999904521 ) ) ;
#16437=( BOUNDED_SURFACE ( )  B_SPLINE_SURFACE ( 1, 2, ( 
 ( #26949, #29408, #17789, #3603, #13033, #22370, #1306, #8378, #27107, #24813, #22529, #1461, #17938, #15645, #24954, #28169, #2089, #25412, #14111, #18695, #23145, #15952, #7139, #20835, #16559, #6836, #18999, #25732, #4679, #23594, #20993, #28321, #30184, #25877, #23449, #2532, #2387, #25250, #18542, #21139, #27868, #23301, #18846, #4223, #4373, #30340, #2245, #16409, #11647, #11957, #9609, #16260, #4831, #9461, #13640, #9303, #14257, #22986, #16109, #25580, #28017, #18390, #21284, #11798, #30031, #76, #1927, #224, #11333, #6990, #20679, #9002, #27708, #6688, #12393, #9911, #4973, #12097, #12248, #369, #16993, #14408, #23743, #7580, #3120, #26316, #19134, #7732, #2672, #10063, #5273, #10218, #16704, #19579, #16846, #19440, #28915, #7881, #14972, #22026, #24313, #962, #3262, #26171, #12693, #25334, #25184, #4309, #20765, #2011, #18323, #22910, #5872, #15130, #22183, #8177, #16037, #27481, #4150, #6615, #6459, #13728, #18468, #23225, #8933, #25494, #2170, #6766, #11570, #27790, #24461, #23070, #10516, #10682, #12839, #4459, #1851, #13885, #11420, #11255, #20606, #8033, #17439, #29215, #29953, #30111, #26753, #17594, #27636, #9075, #5720, #1115, #19869, #12997, #26908, #15293, #24618, #3567, #1270, #22335, #20027, #8339, #25811, #18928, #7226, #5049, #19212, #23376, #28544, #22238, #1048, #5795, #12921, #29299, #19949, #28687, #8255, #3644, #29758, #25291, #13530, #13683, #11055, #18279, #6265, #15684, #11377, #3946, #1808, #11213, #13082, #22414, #20401, #13375, #10761, #20561, #29451, #1661, #29912, #17830, #27592, #6570, #15994, #4263, #20720, #23023, #30069, #25623, #27903, #409, #5013, #7337, #26070, #9798, #14444, #23186, #28212, #21032, #14298, #2129, #19044, #18889, #7478, #30378, #23778, #23637, #21483, #21326, #28509, #9346, #2711, #18738, #2432, #19177, #11530, #14001, #16598, #23490, #25920, #25451, #4415, #23341, #28059, #2284, #11689, #7032, #4721, #8063, #16890, #26360, #5309, #19614, #19329, #5758, #12732, #564, #22071, #14575, #17479, #15171, #26504, #28956, #12885, #3155, #14723 ),
 ( #2865, #21773, #24356, #7766, #9951, #17333, #12286, #26648, #5458, #19760, #19912, #24504, #14865, #5608, #7621, #3450, #28650, #1003, #29105, #12430, #22222, #10555, #1153, #10406, #3012, #15015, #26209, #24208, #24064, #28804, #720, #23924, #29258, #5162, #10104, #21629, #19475, #17180, #21924, #13494, #10726, #29877, #4228, #29415, #8385, #5913, #4072, #24819, #1466, #17794, #27112, #8857, #6080, #13647, #18240, #11339, #20684, #20525, #22833, #25255, #10878, #8220, #3767, #15495, #6375, #20371, #13198, #17634, #15342, #22534, #24663, #29582, #13040, #18094, #27409, #20235, #8539, #17945, #27259, #6231, #29721, #8701, #15652, #22686, #1774, #4539, #9007, #2392, #18396, #20999, #81, #4378, #25882, #14117, #11962, #4835, #7305, #7145, #21143, #30189, #23151, #4978, #19003, #21289, #228, #14412, #16709, #13805, #11805, #13964, #18851, #2094, #23600, #28175, #11499, #18700, #23306, #2538, #28022, #2676, #26031, #20840, #9155, #18548, #4683, #27873, #16415, #16266, #2249, #11651, #30345, #9309, #6995, #25737, #9764, #19140, #14545, #16851, #26175, #2830, #5121, #373, #28473, #13679, #29754, #15988, #23020, #27588, #19945, #8887, #15374, #13526, #1347, #1497, #5953, #25287, #6261, #4259, #1804, #13370, #27289, #29295, #8251, #20103, #3941, #4104, #17664, #29446, #18119, #22866, #26988, #8734, #17975, #3797, #24696, #3640, #11209, #20398, #22566, #13226, #20557, #18275, #6113, #17825, #8420, #10908, #15682, #13076, #29907, #6566, #24990, #24847, #25139, #22409, #10757, #27145, #15527, #20263, #22713, #29609, #1656, #11052, #27436, #6405, #15840, #7181, #25447, #16593, #9035, #11990, #9646, #21026, #14148, #7331, #28054, #30220, #7027, #13996, #18423, #16142, #16298, #4411, #30373, #30065, #27744, #25618, #18884, #2279, #13838, #11839, #6724, #25771, #9341, #14292, #14440, #263, #18732, #118, #2125, #28356, #23181, #25915, #23632, #6874, #19038, #5008, #16739, #4863, #27900, #21176, #11371, #16444, #9185, #23335, #11527, #20869, #9499, #28204, #18580, #26064, #4570, #11682, #2567, #21321, #4715 ) ),
 .UNSPECIFIED., .F., .F., .F. ) 
 B_SPLINE_SURFACE_WITH_KNOTS ( ( 2, 2 ),
 ( 3, 2, 2, 2, 2, 2, 2, 2, 2, 2, 2, 2, 2, 2, 2, 2, 2, 2, 2, 2, 2, 2, 2, 2, 2, 2, 2, 2, 2, 2, 2, 2, 2, 2, 2, 2, 2, 2, 2, 2, 2, 2, 2, 2, 2, 2, 2, 2, 2, 2, 2, 2, 2, 2, 2, 2, 2, 2, 2, 2, 2, 2, 2, 2, 2, 2, 2, 2, 2, 2, 2, 2, 2, 2, 2, 2, 2, 2, 2, 2, 2, 2, 2, 2, 2, 2, 2, 2, 2, 2, 2, 2, 2, 2, 2, 2, 2, 2, 2, 2, 2, 2, 2, 2, 2, 2, 2, 2, 2, 2, 2, 2, 2, 2, 2, 2, 2, 2, 2, 2, 2, 2, 2, 2, 2, 2, 2, 2, 2, 2, 2, 2, 3 ),
 ( 0.000000000000000000, 1.000000000000000000 ),
 ( 0.000000000000000000, 0.007352941176470588133, 0.01470588235294117627, 0.02205882352941176613, 0.02941176470588235253, 0.03676470588235294240, 0.04411764705882353227, 0.05147058823529411520, 0.05882352941176470507, 0.06617647058823529493, 0.07352941176470588480, 0.08088235294117647467, 0.08823529411764706454, 0.09558823529411764053, 0.1029411764705882304, 0.1102941176470588203, 0.1176470588235294101, 0.1250000000000000000, 0.1323529411764705899, 0.1397058823529411797, 0.1470588235294117696, 0.1544117647058823595, 0.1617647058823529493, 0.1691176470588235392, 0.1764705882352941291, 0.1838235294117647189, 0.1911764705882352811, 0.1985294117647058709, 0.2058823529411764608, 0.2132352941176470507, 0.2205882352941176405, 0.2279411764705882304, 0.2352941176470588203, 0.2426470588235294101, 0.2500000000000000000, 0.2573529411764705621, 0.2647058823529411797, 0.2720588235294117418, 0.2794117647058823595, 0.2867647058823529216, 0.2941176470588235392, 0.3014705882352941013, 0.3088235294117647189, 0.3161764705882352811, 0.3235294117647058987, 0.3308823529411764608, 0.3382352941176470784, 0.3455882352941176405, 0.3529411764705882582, 0.3602941176470588203, 0.3676470588235294379, 0.3750000000000000000, 0.3823529411764705621, 0.3897058823529411797, 0.3970588235294117418, 0.4044117647058823595, 0.4117647058823529216, 0.4191176470588235392, 0.4264705882352941013, 0.4338235294117647189, 0.4411764705882352811, 0.4485294117647058987, 0.4558823529411764608, 0.4632352941176470784, 0.4705882352941176405, 0.4779411764705882582, 0.4852941176470588203, 0.4926470588235294379, 0.5000000000000000000, 0.5073529411764705621, 0.5147058823529411242, 0.5220588235294117974, 0.5294117647058823595, 0.5367647058823529216, 0.5441176470588234837, 0.5514705882352941568, 0.5588235294117647189, 0.5661764705882352811, 0.5735294117647058432, 0.5808823529411765163, 0.5882352941176470784, 0.5955882352941176405, 0.6029411764705882026, 0.6102941176470588758, 0.6176470588235294379, 0.6250000000000000000, 0.6323529411764705621, 0.6397058823529411242, 0.6470588235294117974, 0.6544117647058823595, 0.6617647058823529216, 0.6691176470588234837, 0.6764705882352941568, 0.6838235294117647189, 0.6911764705882352811, 0.6985294117647058432, 0.7058823529411765163, 0.7132352941176470784, 0.7205882352941176405, 0.7279411764705882026, 0.7352941176470588758, 0.7426470588235294379, 0.7500000000000000000, 0.7573529411764705621, 0.7647058823529411242, 0.7720588235294117974, 0.7794117647058823595, 0.7867647058823529216, 0.7941176470588234837, 0.8014705882352941568, 0.8088235294117647189, 0.8161764705882352811, 0.8235294117647058432, 0.8308823529411765163, 0.8382352941176470784, 0.8455882352941176405, 0.8529411764705882026, 0.8602941176470588758, 0.8676470588235294379, 0.8750000000000000000, 0.8823529411764705621, 0.8897058823529411242, 0.8970588235294117974, 0.9044117647058823595, 0.9117647058823529216, 0.9191176470588234837, 0.9264705882352941568, 0.9338235294117647189, 0.9411764705882352811, 0.9485294117647058432, 0.9558823529411765163, 0.9632352941176470784, 0.9705882352941176405 ),
 .UNSPECIFIED. ) 
 GEOMETRIC_REPRESENTATION_ITEM ( )  RATIONAL_B_SPLINE_SURFACE ( (
 ( 1.000000000000000000, 0.9238795325112867385, 1.000000000000000000, 0.9238795325112867385, 1.000000000000000000, 0.9238795325112867385, 1.000000000000000000, 0.9238795325112867385, 1.000000000000000000, 0.9238795325112867385, 1.000000000000000000, 0.9238795325112867385, 1.000000000000000000, 0.9238795325112867385, 1.000000000000000000, 0.9238795325112867385, 1.000000000000000000, 0.9238795325112867385, 1.000000000000000000, 0.9238795325112867385, 1.000000000000000000, 0.9238795325112867385, 1.000000000000000000, 0.9238795325112867385, 1.000000000000000000, 0.9238795325112867385, 1.000000000000000000, 0.9238795325112867385, 1.000000000000000000, 0.9238795325112867385, 1.000000000000000000, 0.9238795325112867385, 1.000000000000000000, 0.9238795325112867385, 1.000000000000000000, 0.9238795325112867385, 1.000000000000000000, 0.9238795325112867385, 1.000000000000000000, 0.9238795325112867385, 1.000000000000000000, 0.9238795325112867385, 1.000000000000000000, 0.9238795325112867385, 1.000000000000000000, 0.9238795325112867385, 1.000000000000000000, 0.9238795325112867385, 1.000000000000000000, 0.9238795325112867385, 1.000000000000000000, 0.9238795325112867385, 1.000000000000000000, 0.9238795325112867385, 1.000000000000000000, 0.9238795325112867385, 1.000000000000000000, 0.9238795325112867385, 1.000000000000000000, 0.9238795325112867385, 1.000000000000000000, 0.9238795325112867385, 1.000000000000000000, 0.9238795325112867385, 1.000000000000000000, 0.9238795325112867385, 1.000000000000000000, 0.9238795325112867385, 1.000000000000000000, 0.9238795325112867385, 1.000000000000000000, 0.9238795325112867385, 1.000000000000000000, 0.9238795325112867385, 1.000000000000000000, 0.9238795325112867385, 1.000000000000000000, 0.9238795325112867385, 1.000000000000000000, 0.9238795325112867385, 1.000000000000000000, 0.9238795325112867385, 1.000000000000000000, 0.9238795325112867385, 1.000000000000000000, 0.9238795325112867385, 1.000000000000000000, 0.9238795325112867385, 1.000000000000000000, 0.9238795325112867385, 1.000000000000000000, 0.9238795325112867385, 1.000000000000000000, 0.9238795325112867385, 1.000000000000000000, 0.9238795325112867385, 1.000000000000000000, 0.9238795325112867385, 1.000000000000000000, 0.9238795325112867385, 1.000000000000000000, 0.9238795325112867385, 1.000000000000000000, 0.9238795325112867385, 1.000000000000000000, 0.9238795325112867385, 1.000000000000000000, 0.9238795325112867385, 1.000000000000000000, 0.9238795325112867385, 1.000000000000000000, 0.9238795325112867385, 1.000000000000000000, 0.9238795325112867385, 1.000000000000000000, 0.9238795325112867385, 1.000000000000000000, 0.9238795325112867385, 1.000000000000000000, 0.9238795325112867385, 1.000000000000000000, 0.9238795325112867385, 1.000000000000000000, 0.9238795325112867385, 1.000000000000000000, 0.9238795325112867385, 1.000000000000000000, 0.9238795325112867385, 1.000000000000000000, 0.9238795325112867385, 1.000000000000000000, 0.9238795325112867385, 1.000000000000000000, 0.9238795325112867385, 1.000000000000000000, 0.9238795325112867385, 1.000000000000000000, 0.9238795325112867385, 1.000000000000000000, 0.9238795325112867385, 1.000000000000000000, 0.9238795325112867385, 1.000000000000000000, 0.9238795325112867385, 1.000000000000000000, 0.9238795325112867385, 1.000000000000000000, 0.9238795325112867385, 1.000000000000000000, 0.9238795325112867385, 1.000000000000000000, 0.9238795325112867385, 1.000000000000000000, 0.9238795325112867385, 1.000000000000000000, 0.9238795325112867385, 1.000000000000000000, 0.9238795325112867385, 1.000000000000000000, 0.9238795325112867385, 1.000000000000000000, 0.9238795325112867385, 1.000000000000000000, 0.9238795325112867385, 1.000000000000000000, 0.9238795325112867385, 1.000000000000000000, 0.9238795325112867385, 1.000000000000000000, 0.9238795325112867385, 1.000000000000000000, 0.9238795325112867385, 1.000000000000000000, 0.9238795325112867385, 1.000000000000000000, 0.9238795325112867385, 1.000000000000000000, 0.9238795325112867385, 1.000000000000000000, 0.9238795325112867385, 1.000000000000000000, 0.9238795325112867385, 1.000000000000000000, 0.9238795325112867385, 1.000000000000000000, 0.9238795325112867385, 1.000000000000000000, 0.9238795325112867385, 1.000000000000000000, 0.9238795325112867385, 1.000000000000000000, 0.9238795325112867385, 1.000000000000000000, 0.9238795325112867385, 1.000000000000000000, 0.9238795325112867385, 1.000000000000000000, 0.9238795325112867385, 1.000000000000000000, 0.9238795325112867385, 1.000000000000000000, 0.9238795325112867385, 1.000000000000000000, 0.9238795325112867385, 1.000000000000000000, 0.9238795325112867385, 1.000000000000000000, 0.9238795325112867385, 1.000000000000000000, 0.9238795325112867385, 1.000000000000000000, 0.9238795325112867385, 1.000000000000000000, 0.9238795325112867385, 1.000000000000000000, 0.9238795325112867385, 1.000000000000000000, 0.9238795325112867385, 1.000000000000000000, 0.9238795325112867385, 1.000000000000000000, 0.9238795325112867385, 1.000000000000000000, 0.9238795325112867385, 1.000000000000000000, 0.9238795325112867385, 1.000000000000000000, 0.9238795325112867385, 1.000000000000000000, 0.9238795325112867385, 1.000000000000000000, 0.9238795325112867385, 1.000000000000000000, 0.9238795325112867385, 1.000000000000000000, 0.9238795325112867385, 1.000000000000000000, 0.9238795325112867385, 1.000000000000000000, 0.9238795325112867385, 1.000000000000000000, 0.9238795325112867385, 1.000000000000000000, 0.9238795325112867385, 1.000000000000000000, 0.9238795325112867385, 1.000000000000000000, 0.9238795325112867385, 1.000000000000000000, 0.9238795325112867385, 1.000000000000000000, 0.9238795325112867385, 1.000000000000000000, 0.9238795325112867385, 1.000000000000000000, 0.9238795325112867385, 1.000000000000000000, 0.9238795325112867385, 1.000000000000000000, 0.9238795325112867385, 1.000000000000000000, 0.9238795325112867385, 1.000000000000000000, 0.9238795325112867385, 1.000000000000000000),
 ( 1.000000000000000000, 0.9238795325112867385, 1.000000000000000000, 0.9238795325112867385, 1.000000000000000000, 0.9238795325112867385, 1.000000000000000000, 0.9238795325112867385, 1.000000000000000000, 0.9238795325112867385, 1.000000000000000000, 0.9238795325112867385, 1.000000000000000000, 0.9238795325112867385, 1.000000000000000000, 0.9238795325112867385, 1.000000000000000000, 0.9238795325112867385, 1.000000000000000000, 0.9238795325112867385, 1.000000000000000000, 0.9238795325112867385, 1.000000000000000000, 0.9238795325112867385, 1.000000000000000000, 0.9238795325112867385, 1.000000000000000000, 0.9238795325112867385, 1.000000000000000000, 0.9238795325112867385, 1.000000000000000000, 0.9238795325112867385, 1.000000000000000000, 0.9238795325112867385, 1.000000000000000000, 0.9238795325112867385, 1.000000000000000000, 0.9238795325112867385, 1.000000000000000000, 0.9238795325112867385, 1.000000000000000000, 0.9238795325112867385, 1.000000000000000000, 0.9238795325112867385, 1.000000000000000000, 0.9238795325112867385, 1.000000000000000000, 0.9238795325112867385, 1.000000000000000000, 0.9238795325112867385, 1.000000000000000000, 0.9238795325112867385, 1.000000000000000000, 0.9238795325112867385, 1.000000000000000000, 0.9238795325112867385, 1.000000000000000000, 0.9238795325112867385, 1.000000000000000000, 0.9238795325112867385, 1.000000000000000000, 0.9238795325112867385, 1.000000000000000000, 0.9238795325112867385, 1.000000000000000000, 0.9238795325112867385, 1.000000000000000000, 0.9238795325112867385, 1.000000000000000000, 0.9238795325112867385, 1.000000000000000000, 0.9238795325112867385, 1.000000000000000000, 0.9238795325112867385, 1.000000000000000000, 0.9238795325112867385, 1.000000000000000000, 0.9238795325112867385, 1.000000000000000000, 0.9238795325112867385, 1.000000000000000000, 0.9238795325112867385, 1.000000000000000000, 0.9238795325112867385, 1.000000000000000000, 0.9238795325112867385, 1.000000000000000000, 0.9238795325112867385, 1.000000000000000000, 0.9238795325112867385, 1.000000000000000000, 0.9238795325112867385, 1.000000000000000000, 0.9238795325112867385, 1.000000000000000000, 0.9238795325112867385, 1.000000000000000000, 0.9238795325112867385, 1.000000000000000000, 0.9238795325112867385, 1.000000000000000000, 0.9238795325112867385, 1.000000000000000000, 0.9238795325112867385, 1.000000000000000000, 0.9238795325112867385, 1.000000000000000000, 0.9238795325112867385, 1.000000000000000000, 0.9238795325112867385, 1.000000000000000000, 0.9238795325112867385, 1.000000000000000000, 0.9238795325112867385, 1.000000000000000000, 0.9238795325112867385, 1.000000000000000000, 0.9238795325112867385, 1.000000000000000000, 0.9238795325112867385, 1.000000000000000000, 0.9238795325112867385, 1.000000000000000000, 0.9238795325112867385, 1.000000000000000000, 0.9238795325112867385, 1.000000000000000000, 0.9238795325112867385, 1.000000000000000000, 0.9238795325112867385, 1.000000000000000000, 0.9238795325112867385, 1.000000000000000000, 0.9238795325112867385, 1.000000000000000000, 0.9238795325112867385, 1.000000000000000000, 0.9238795325112867385, 1.000000000000000000, 0.9238795325112867385, 1.000000000000000000, 0.9238795325112867385, 1.000000000000000000, 0.9238795325112867385, 1.000000000000000000, 0.9238795325112867385, 1.000000000000000000, 0.9238795325112867385, 1.000000000000000000, 0.9238795325112867385, 1.000000000000000000, 0.9238795325112867385, 1.000000000000000000, 0.9238795325112867385, 1.000000000000000000, 0.9238795325112867385, 1.000000000000000000, 0.9238795325112867385, 1.000000000000000000, 0.9238795325112867385, 1.000000000000000000, 0.9238795325112867385, 1.000000000000000000, 0.9238795325112867385, 1.000000000000000000, 0.9238795325112867385, 1.000000000000000000, 0.9238795325112867385, 1.000000000000000000, 0.9238795325112867385, 1.000000000000000000, 0.9238795325112867385, 1.000000000000000000, 0.9238795325112867385, 1.000000000000000000, 0.9238795325112867385, 1.000000000000000000, 0.9238795325112867385, 1.000000000000000000, 0.9238795325112867385, 1.000000000000000000, 0.9238795325112867385, 1.000000000000000000, 0.9238795325112867385, 1.000000000000000000, 0.9238795325112867385, 1.000000000000000000, 0.9238795325112867385, 1.000000000000000000, 0.9238795325112867385, 1.000000000000000000, 0.9238795325112867385, 1.000000000000000000, 0.9238795325112867385, 1.000000000000000000, 0.9238795325112867385, 1.000000000000000000, 0.9238795325112867385, 1.000000000000000000, 0.9238795325112867385, 1.000000000000000000, 0.9238795325112867385, 1.000000000000000000, 0.9238795325112867385, 1.000000000000000000, 0.9238795325112867385, 1.000000000000000000, 0.9238795325112867385, 1.000000000000000000, 0.9238795325112867385, 1.000000000000000000, 0.9238795325112867385, 1.000000000000000000, 0.9238795325112867385, 1.000000000000000000, 0.9238795325112867385, 1.000000000000000000, 0.9238795325112867385, 1.000000000000000000, 0.9238795325112867385, 1.000000000000000000, 0.9238795325112867385, 1.000000000000000000, 0.9238795325112867385, 1.000000000000000000, 0.9238795325112867385, 1.000000000000000000, 0.9238795325112867385, 1.000000000000000000, 0.9238795325112867385, 1.000000000000000000, 0.9238795325112867385, 1.000000000000000000, 0.9238795325112867385, 1.000000000000000000, 0.9238795325112867385, 1.000000000000000000, 0.9238795325112867385, 1.000000000000000000, 0.9238795325112867385, 1.000000000000000000, 0.9238795325112867385, 1.000000000000000000, 0.9238795325112867385, 1.000000000000000000, 0.9238795325112867385, 1.000000000000000000, 0.9238795325112867385, 1.000000000000000000, 0.9238795325112867385, 1.000000000000000000, 0.9238795325112867385, 1.000000000000000000, 0.9238795325112867385, 1.000000000000000000, 0.9238795325112867385, 1.000000000000000000, 0.9238795325112867385, 1.000000000000000000, 0.9238795325112867385, 1.000000000000000000, 0.9238795325112867385, 1.000000000000000000, 0.9238795325112867385, 1.000000000000000000) ) ) 
 REPRESENTATION_ITEM ( '' )  SURFACE ( )  );
#16442=CARTESIAN_POINT ( 'NONE',  ( 113.6249999999998721, -1.767766952966376426, -1.767766952966431937 ) ) ;
#16444=CARTESIAN_POINT ( 'NONE',  ( 105.6877832217623023, -0.7662911109077987781, 1.849990392679532247 ) ) ;
#16447=ORIENTED_EDGE ( 'NONE', *, *, #6574, .F. ) ;
#16448=CARTESIAN_POINT ( 'NONE',  ( 114.2886751345947971, 2.000000000000029310, 1.110223024625156540E-13 ) ) ;
#16461=CARTESIAN_POINT ( 'NONE',  ( 106.9374999999997868, 2.500000000000055067, -1.035533905932568777 ) ) ;
#16466=CARTESIAN_POINT ( 'NONE',  ( 110.0002832217622597, -1.308140751793585022, -1.308140751793640533 ) ) ;
#16480=ADVANCED_FACE ( 'NONE', ( #11045 ), #25609, .T. ) ;
#16492=CARTESIAN_POINT ( 'NONE',  ( 106.1636751345947260, 1.414213562373034527, -1.414213562373034527 ) ) ;
#16503=DIRECTION ( 'NONE',  ( -1.000000000000000000, -1.665334536937736783E-16, -2.220446049250315546E-16 ) ) ;
#16509=CARTESIAN_POINT ( 'NONE',  ( 111.1249999999999289, 1.767766952966320915, 1.767766952966431937 ) ) ;
#16519=B_SPLINE_CURVE_WITH_KNOTS ( 'NONE', 3,
 ( #10223, #26618, #19293, #10070, #14835, #21889, #28921, #524, #5124, #7444 ),
 .UNSPECIFIED., .F., .F.,
 ( 4, 2, 2, 2, 4 ),
 ( 6.138082936578478530E-16, 0.0005289548070271558140, 0.001057909614053697970, 0.001586864421080240450, 0.002115819228106782714 ),
 .UNSPECIFIED. ) ;
#16522=CARTESIAN_POINT ( 'NONE',  ( 105.3124999999998437, -1.035533905932598975, 2.500000000000265121 ) ) ;
#16528=CARTESIAN_POINT ( 'NONE',  ( 116.9999999999999005, 2.500000000000057732, 1.110223024625156540E-13 ) ) ;
#16538=CARTESIAN_POINT ( 'NONE',  ( 105.2497167782374845, -1.308140751793585022, -1.308140751793640533 ) ) ;
#16542=CARTESIAN_POINT ( 'NONE',  ( 118.9377832217621460, -1.849990392679472073, -0.7662911109077087390 ) ) ;
#16544=ADVANCED_FACE ( 'NONE', ( #13827 ), #23174, .T. ) ;
#16546=FACE_OUTER_BOUND ( 'NONE', #29606, .T. ) ;
#16559=CARTESIAN_POINT ( 'NONE',  ( 119.1247167782375698, -1.849990392679412565, 1.110223024625156540E-13 ) ) ;
#16566=ORIENTED_EDGE ( 'NONE', *, *, #10409, .T. ) ;
#16577=EDGE_CURVE ( 'NONE', #2721, #30412, #11981, .T. ) ;
#16582=CARTESIAN_POINT ( 'NONE',  ( 110.4999999999999432, -2.499999999999891198, 3.330669073875469621E-13 ) ) ;
#16591=CARTESIAN_POINT ( 'NONE',  ( 112.1874999999998295, 1.035533905932719101, 2.500000000000205169 ) ) ;
#16593=CARTESIAN_POINT ( 'NONE',  ( 108.4377832217621318, 1.849990392679532247, 0.7662911109080692285 ) ) ;
#16598=CARTESIAN_POINT ( 'NONE',  ( 105.8747167782375271, -2.775557561562891351E-14, 1.849990392679523588 ) ) ;
#16611=CARTESIAN_POINT ( 'NONE',  ( 106.8749999999998437, 1.767766952966320915, -1.767766952966320915 ) ) ;
#16615=CARTESIAN_POINT ( 'NONE',  ( 109.7886751345948255, -2.000000000000001776, 0.000000000000000000 ) ) ;
#16617=CARTESIAN_POINT ( 'NONE',  ( 107.1252832217622455, 0.000000000000000000, -1.849990392679523588 ) ) ;
#16630=DIRECTION ( 'NONE',  ( -1.000000000000000000, -1.665334536937736783E-16, -2.220446049250315546E-16 ) ) ;
#16634=CARTESIAN_POINT ( 'NONE',  ( 111.7261751345945555, -1.999999999999971800, 0.8284271247464759513 ) ) ;
#16658=CARTESIAN_POINT ( 'NONE',  ( 110.8749999999998721, 1.767766952966431937, -1.767766952966209892 ) ) ;
#16659=CARTESIAN_POINT ( 'NONE',  ( 115.2886751345946550, 2.000000000000112799, 3.330669073875469621E-13 ) ) ;
#16668=CARTESIAN_POINT ( 'NONE',  ( 116.7497167782375413, 1.308140751793585022, 1.308140751793751555 ) ) ;
#16673=CARTESIAN_POINT ( 'NONE',  ( 116.9374999999998295, 2.500000000000024425, -1.035533905932629173 ) ) ;
#16676=ORIENTED_EDGE ( 'NONE', *, *, #17393, .T. ) ;
#16685=CARTESIAN_POINT ( 'NONE',  ( 104.3122167782373992, -0.7662911109076785410, -1.849990392679291551 ) ) ;
#16687=CARTESIAN_POINT ( 'NONE',  ( 119.9377832217623023, -1.849990392679501827, -0.7662911109076485650 ) ) ;
#16704=CARTESIAN_POINT ( 'NONE',  ( 114.8747167782375840, -5.551115123125782702E-14, 1.849990392679523588 ) ) ;
#16708=CARTESIAN_POINT ( 'NONE',  ( 119.1011751345947260, 0.8284271247463257382, -1.999999999999851674 ) ) ;
#16709=CARTESIAN_POINT ( 'NONE',  ( 114.7502832217623592, -1.308140751793640533, 1.308140751793640533 ) ) ;
#16710=EDGE_CURVE ( 'NONE', #3485, #3730, #4890, .T. ) ;
#16721=CARTESIAN_POINT ( 'NONE',  ( 109.7113248654051176, 2.000000000000057288, 0.000000000000000000 ) ) ;
#16734=CARTESIAN_POINT ( 'NONE',  ( 109.7113248654051176, 2.000000000000057288, 0.000000000000000000 ) ) ;
#16737=CARTESIAN_POINT ( 'NONE',  ( 112.9999999999998579, 2.500000000000057732, 0.000000000000000000 ) ) ;
#16738=CARTESIAN_POINT ( 'NONE',  ( 112.0863248654050324, -1.414213562373117794, 1.414213562373256572 ) ) ;
#16739=CARTESIAN_POINT ( 'NONE',  ( 106.0002832217622029, -1.308140751793585022, -1.308140751793640533 ) ) ;
#16745=CARTESIAN_POINT ( 'NONE',  ( 110.7113248654050182, 2.000000000000057288, 0.000000000000000000 ) ) ;
#16748=ORIENTED_EDGE ( 'NONE', *, *, #15154, .T. ) ;
#16757=CARTESIAN_POINT ( 'NONE',  ( 108.3749999999998437, -1.767766952966209892, 1.767766952966431937 ) ) ;
#16763=CARTESIAN_POINT ( 'NONE',  ( 106.8127832217621602, -1.849990392679441875, 0.7662911109078888172 ) ) ;
#16765=CARTESIAN_POINT ( 'NONE',  ( 119.7886751345947829, -1.999999999999946265, 3.330669073875469621E-13 ) ) ;
#16807=CARTESIAN_POINT ( 'NONE',  ( 104.9374999999997726, 2.500000000000115019, -1.035533905932448873 ) ) ;
#16814=CARTESIAN_POINT ( 'NONE',  ( 119.3747167782375413, -5.551115123125782702E-14, -1.849990392679523588 ) ) ;
#16815=CARTESIAN_POINT ( 'NONE',  ( 118.2886751345946976, 2.000000000000085265, 0.000000000000000000 ) ) ;
#16820=CARTESIAN_POINT ( 'NONE',  ( 119.2499999999999574, -5.551115123125782702E-14, 2.500000000000168754 ) ) ;
#16831=CARTESIAN_POINT ( 'NONE',  ( 106.4372167782374419, 0.7662911109078588412, -1.849990392679231599 ) ) ;
#16833=CARTESIAN_POINT ( 'NONE',  ( 115.4377832217621744, 1.849990392679591977, 0.7662911109078888172 ) ) ;
#16846=CARTESIAN_POINT ( 'NONE',  ( 114.7497167782374561, 1.308140751793751555, 1.308140751793973600 ) ) ;
#16851=CARTESIAN_POINT ( 'NONE',  ( 112.8127832217621886, -1.849990392679441875, 0.7662911109079489913 ) ) ;
#16858=ORIENTED_EDGE ( 'NONE', *, *, #5271, .F. ) ;
#16866=FACE_OUTER_BOUND ( 'NONE', #6576, .T. ) ;
#16869=CIRCLE ( 'NONE', #28568, 5.999999999999998224 ) ;
#16873=CARTESIAN_POINT ( 'NONE',  ( 111.8749999999998437, 1.767766952966348670, -1.767766952966209892 ) ) ;
#16884=CARTESIAN_POINT ( 'NONE',  ( 114.1874999999998295, 1.035533905932779275, 2.500000000000445421 ) ) ;
#16890=CARTESIAN_POINT ( 'NONE',  ( 105.1247167782375840, -1.849990392679468076, 0.000000000000000000 ) ) ;
#16896=ORIENTED_EDGE ( 'NONE', *, *, #21885, .T. ) ;
#16899=CARTESIAN_POINT ( 'NONE',  ( 109.6249999999999858, -1.767766952966376426, -1.767766952966320915 ) ) ;
#16906=CARTESIAN_POINT ( 'NONE',  ( 106.9377832217621318, -1.849990392679441875, -0.7662911109075883909 ) ) ;
#16912=EDGE_CURVE ( 'NONE', #14487, #1738, #25710, .T. ) ;
#16918=( BOUNDED_SURFACE ( )  B_SPLINE_SURFACE ( 1, 2, ( 
 ( #11007, #20351, #29705, #8676, #20662, #2224, #23284, #18982, #25866, #18826, #23575, #11476, #30011, #20972, #22967, #11779, #16388, #20819, #13621, #4814, #18523, #14241, #4517, #16687, #23430, #2375, #21267, #13781, #25709, #4355, #16242, #21120, #206, #55, #1907, #9131, #11940, #18375, #30167, #16542, #11314, #2073, #28000, #16089, #4662, #14095, #8984, #7284, #27847, #2512, #7121, #27690, #9282, #9593, #25393, #6816, #23125, #9444, #25556, #13939, #11628, #30321, #18676, #6970, #28152, #28304, #13102, #663, #2658, #17126, #8447, #19121, #27019, #7719, #5984, #24012, #14817, #23866, #12081, #21420, #9898, #12528, #26304, #16979, #5404, #14666, #19968, #2957, #8280, #17854, #24726, #12375, #24160, #26154, #22438, #16833, #29322, #21723, #28453, #2808, #12233, #19423, #1375, #3667, #7563, #10045, #10785, #5103, #28749, #26453, #19273, #20132, #1210, #352, #3102, #503, #21868, #10618, #15402, #28595, #17693, #29479, #14527, #4956, #14389, #23723, #9745, #21572, #5259, #16015, #11238, #3974, #13253, #29633, #6286, #13709, #15868, #1526, #24874, #1834, #27460, #16170, #20898, #6593, #23206, #30244, #4441, #9210, #25475, #22594, #20744, #8599, #8762, #8914, #6438, #27171, #13866, #9059, #20586, #4130, #6143, #2152, #27323, #29934, #11397, #15709, #3823, #18148, #27618, #15557, #25314, #25166, #11082, #4290, #18005, #25019, #18452, #23050, #1989, #30094, #13398, #22742, #16466, #7054, #21203, #14315, #584, #9819, #430, #23656, #18602, #4592, #6897, #19195, #2885, #14018, #27924, #25938, #2592, #5183, #21648, #4885, #2729, #144, #21050, #23361, #2305, #28232, #12011, #16322, #23948, #21346, #14171, #25641, #287, #11705, #9525, #9671, #28378, #21503, #30398, #26089, #9365, #12158, #12307, #19061, #7206, #28524, #16617, #7493, #18757, #16906, #7358, #16763, #28079, #14596, #25795, #26231, #4745, #23509, #2452, #11863, #18912, #5029, #14462, #23795, #8238, #15361, #7786, #21941, #12451, #7642, #8085, #19777, #10124, #26972, #26526, #17052, #3472, #15190, #14885, #877, #10425, #22242, #21794 ),
 ( #28825, #26382, #10275, #3324, #9971, #29125, #7943, #24227, #19639, #5329, #17650, #1170, #12598, #3177, #12906, #29278, #5479, #17202, #28976, #17353, #5628, #22394, #10578, #19932, #15034, #19349, #14739, #28668, #5937, #24684, #24083, #3034, #26668, #24381, #3626, #13062, #12752, #24524, #22092, #741, #19495, #1027, #17499, #26815, #5778, #6713, #18108, #27277, #13825, #4092, #10745, #22703, #22853, #11198, #4246, #20090, #8876, #29433, #15975, #16130, #8720, #24835, #20250, #29599, #15827, #9024, #30054, #3930, #11041, #18414, #13217, #25127, #20387, #15669, #27734, #27575, #27132, #29744, #6250, #13512, #27428, #24978, #25436, #6101, #8559, #13668, #8404, #17964, #1791, #3785, #20545, #29895, #17812, #4399, #13357, #1955, #25273, #1333, #6394, #23010, #15513, #1642, #22554, #18264, #1487, #10896, #6556, #11358, #20705, #26194, #11673, #14137, #394, #18869, #20857, #4850, #5145, #6862, #14429, #25901, #23766, #11826, #2553, #21014, #30210, #9172, #28044, #248, #23476, #4703, #23619, #2413, #7319, #21164, #26053, #23169, #12122, #104, #21308, #13983, #9784, #4559, #4996, #2697, #18720, #21465, #16873, #19162, #28497, #2113, #7014, #7462, #11517, #30361, #9486, #25607, #18566, #9631, #19025, #23323, #27890, #9329, #2267, #16431, #28344, #25755, #28190, #7166, #16582, #14278, #2297, #21495, #21193, #28225, #28073, #18751, #5174, #2724, #11701, #23650, #14309, #9963, #16899, #9811, #14588, #2446, #21045, #12006, #14011, #12151, #7351, #11855, #4586, #26219, #9519, #23939, #25932, #7632, #14453, #23788, #12296, #4736, #16757, #25788, #7199, #422, #21640, #19190, #17042, #23356, #4879, #26081, #28518, #7489, #30392, #2877, #9359, #575, #19341, #21340, #7049, #23502, #135, #19054, #28660, #16461, #16611, #2583, #14165, #18906, #28371, #281, #9664, #5023, #22232, #21787, #15027, #21932, #19769, #5619, #26965, #10266, #10566, #3462, #10115, #1017, #1162, #12741, #19923, #17642, #29269, #15179, #10417, #3167, #12442, #19485, #5468, #12897, #24370, #730, #24075, #29115, #26658, #15353, #20081 ) ),
 .UNSPECIFIED., .F., .F., .F. ) 
 B_SPLINE_SURFACE_WITH_KNOTS ( ( 2, 2 ),
 ( 3, 2, 2, 2, 2, 2, 2, 2, 2, 2, 2, 2, 2, 2, 2, 2, 2, 2, 2, 2, 2, 2, 2, 2, 2, 2, 2, 2, 2, 2, 2, 2, 2, 2, 2, 2, 2, 2, 2, 2, 2, 2, 2, 2, 2, 2, 2, 2, 2, 2, 2, 2, 2, 2, 2, 2, 2, 2, 2, 2, 2, 2, 2, 2, 2, 2, 2, 2, 2, 2, 2, 2, 2, 2, 2, 2, 2, 2, 2, 2, 2, 2, 2, 2, 2, 2, 2, 2, 2, 2, 2, 2, 2, 2, 2, 2, 2, 2, 2, 2, 2, 2, 2, 2, 2, 2, 2, 2, 2, 2, 2, 2, 2, 2, 2, 2, 2, 2, 2, 2, 2, 2, 2, 2, 2, 2, 2, 2, 2, 2, 2, 2, 3 ),
 ( 0.000000000000000000, 1.000000000000000000 ),
 ( 0.000000000000000000, 0.007352941176470588133, 0.01470588235294117627, 0.02205882352941176613, 0.02941176470588235253, 0.03676470588235294240, 0.04411764705882353227, 0.05147058823529411520, 0.05882352941176470507, 0.06617647058823529493, 0.07352941176470588480, 0.08088235294117647467, 0.08823529411764706454, 0.09558823529411764053, 0.1029411764705882304, 0.1102941176470588203, 0.1176470588235294101, 0.1250000000000000000, 0.1323529411764705899, 0.1397058823529411797, 0.1470588235294117696, 0.1544117647058823595, 0.1617647058823529493, 0.1691176470588235392, 0.1764705882352941291, 0.1838235294117647189, 0.1911764705882352811, 0.1985294117647058709, 0.2058823529411764608, 0.2132352941176470507, 0.2205882352941176405, 0.2279411764705882304, 0.2352941176470588203, 0.2426470588235294101, 0.2500000000000000000, 0.2573529411764705621, 0.2647058823529411797, 0.2720588235294117418, 0.2794117647058823595, 0.2867647058823529216, 0.2941176470588235392, 0.3014705882352941013, 0.3088235294117647189, 0.3161764705882352811, 0.3235294117647058987, 0.3308823529411764608, 0.3382352941176470784, 0.3455882352941176405, 0.3529411764705882582, 0.3602941176470588203, 0.3676470588235294379, 0.3750000000000000000, 0.3823529411764705621, 0.3897058823529411797, 0.3970588235294117418, 0.4044117647058823595, 0.4117647058823529216, 0.4191176470588235392, 0.4264705882352941013, 0.4338235294117647189, 0.4411764705882352811, 0.4485294117647058987, 0.4558823529411764608, 0.4632352941176470784, 0.4705882352941176405, 0.4779411764705882582, 0.4852941176470588203, 0.4926470588235294379, 0.5000000000000000000, 0.5073529411764705621, 0.5147058823529411242, 0.5220588235294117974, 0.5294117647058823595, 0.5367647058823529216, 0.5441176470588234837, 0.5514705882352941568, 0.5588235294117647189, 0.5661764705882352811, 0.5735294117647058432, 0.5808823529411765163, 0.5882352941176470784, 0.5955882352941176405, 0.6029411764705882026, 0.6102941176470588758, 0.6176470588235294379, 0.6250000000000000000, 0.6323529411764705621, 0.6397058823529411242, 0.6470588235294117974, 0.6544117647058823595, 0.6617647058823529216, 0.6691176470588234837, 0.6764705882352941568, 0.6838235294117647189, 0.6911764705882352811, 0.6985294117647058432, 0.7058823529411765163, 0.7132352941176470784, 0.7205882352941176405, 0.7279411764705882026, 0.7352941176470588758, 0.7426470588235294379, 0.7500000000000000000, 0.7573529411764705621, 0.7647058823529411242, 0.7720588235294117974, 0.7794117647058823595, 0.7867647058823529216, 0.7941176470588234837, 0.8014705882352941568, 0.8088235294117647189, 0.8161764705882352811, 0.8235294117647058432, 0.8308823529411765163, 0.8382352941176470784, 0.8455882352941176405, 0.8529411764705882026, 0.8602941176470588758, 0.8676470588235294379, 0.8750000000000000000, 0.8823529411764705621, 0.8897058823529411242, 0.8970588235294117974, 0.9044117647058823595, 0.9117647058823529216, 0.9191176470588234837, 0.9264705882352941568, 0.9338235294117647189, 0.9411764705882352811, 0.9485294117647058432, 0.9558823529411765163, 0.9632352941176470784, 0.9705882352941176405 ),
 .UNSPECIFIED. ) 
 GEOMETRIC_REPRESENTATION_ITEM ( )  RATIONAL_B_SPLINE_SURFACE ( (
 ( 1.000000000000000000, 0.9238795325112867385, 1.000000000000000000, 0.9238795325112867385, 1.000000000000000000, 0.9238795325112867385, 1.000000000000000000, 0.9238795325112867385, 1.000000000000000000, 0.9238795325112867385, 1.000000000000000000, 0.9238795325112867385, 1.000000000000000000, 0.9238795325112867385, 1.000000000000000000, 0.9238795325112867385, 1.000000000000000000, 0.9238795325112867385, 1.000000000000000000, 0.9238795325112867385, 1.000000000000000000, 0.9238795325112867385, 1.000000000000000000, 0.9238795325112867385, 1.000000000000000000, 0.9238795325112867385, 1.000000000000000000, 0.9238795325112867385, 1.000000000000000000, 0.9238795325112867385, 1.000000000000000000, 0.9238795325112867385, 1.000000000000000000, 0.9238795325112867385, 1.000000000000000000, 0.9238795325112867385, 1.000000000000000000, 0.9238795325112867385, 1.000000000000000000, 0.9238795325112867385, 1.000000000000000000, 0.9238795325112867385, 1.000000000000000000, 0.9238795325112867385, 1.000000000000000000, 0.9238795325112867385, 1.000000000000000000, 0.9238795325112867385, 1.000000000000000000, 0.9238795325112867385, 1.000000000000000000, 0.9238795325112867385, 1.000000000000000000, 0.9238795325112867385, 1.000000000000000000, 0.9238795325112867385, 1.000000000000000000, 0.9238795325112867385, 1.000000000000000000, 0.9238795325112867385, 1.000000000000000000, 0.9238795325112867385, 1.000000000000000000, 0.9238795325112867385, 1.000000000000000000, 0.9238795325112867385, 1.000000000000000000, 0.9238795325112867385, 1.000000000000000000, 0.9238795325112867385, 1.000000000000000000, 0.9238795325112867385, 1.000000000000000000, 0.9238795325112867385, 1.000000000000000000, 0.9238795325112867385, 1.000000000000000000, 0.9238795325112867385, 1.000000000000000000, 0.9238795325112867385, 1.000000000000000000, 0.9238795325112867385, 1.000000000000000000, 0.9238795325112867385, 1.000000000000000000, 0.9238795325112867385, 1.000000000000000000, 0.9238795325112867385, 1.000000000000000000, 0.9238795325112867385, 1.000000000000000000, 0.9238795325112867385, 1.000000000000000000, 0.9238795325112867385, 1.000000000000000000, 0.9238795325112867385, 1.000000000000000000, 0.9238795325112867385, 1.000000000000000000, 0.9238795325112867385, 1.000000000000000000, 0.9238795325112867385, 1.000000000000000000, 0.9238795325112867385, 1.000000000000000000, 0.9238795325112867385, 1.000000000000000000, 0.9238795325112867385, 1.000000000000000000, 0.9238795325112867385, 1.000000000000000000, 0.9238795325112867385, 1.000000000000000000, 0.9238795325112867385, 1.000000000000000000, 0.9238795325112867385, 1.000000000000000000, 0.9238795325112867385, 1.000000000000000000, 0.9238795325112867385, 1.000000000000000000, 0.9238795325112867385, 1.000000000000000000, 0.9238795325112867385, 1.000000000000000000, 0.9238795325112867385, 1.000000000000000000, 0.9238795325112867385, 1.000000000000000000, 0.9238795325112867385, 1.000000000000000000, 0.9238795325112867385, 1.000000000000000000, 0.9238795325112867385, 1.000000000000000000, 0.9238795325112867385, 1.000000000000000000, 0.9238795325112867385, 1.000000000000000000, 0.9238795325112867385, 1.000000000000000000, 0.9238795325112867385, 1.000000000000000000, 0.9238795325112867385, 1.000000000000000000, 0.9238795325112867385, 1.000000000000000000, 0.9238795325112867385, 1.000000000000000000, 0.9238795325112867385, 1.000000000000000000, 0.9238795325112867385, 1.000000000000000000, 0.9238795325112867385, 1.000000000000000000, 0.9238795325112867385, 1.000000000000000000, 0.9238795325112867385, 1.000000000000000000, 0.9238795325112867385, 1.000000000000000000, 0.9238795325112867385, 1.000000000000000000, 0.9238795325112867385, 1.000000000000000000, 0.9238795325112867385, 1.000000000000000000, 0.9238795325112867385, 1.000000000000000000, 0.9238795325112867385, 1.000000000000000000, 0.9238795325112867385, 1.000000000000000000, 0.9238795325112867385, 1.000000000000000000, 0.9238795325112867385, 1.000000000000000000, 0.9238795325112867385, 1.000000000000000000, 0.9238795325112867385, 1.000000000000000000, 0.9238795325112867385, 1.000000000000000000, 0.9238795325112867385, 1.000000000000000000, 0.9238795325112867385, 1.000000000000000000, 0.9238795325112867385, 1.000000000000000000, 0.9238795325112867385, 1.000000000000000000, 0.9238795325112867385, 1.000000000000000000, 0.9238795325112867385, 1.000000000000000000, 0.9238795325112867385, 1.000000000000000000, 0.9238795325112867385, 1.000000000000000000, 0.9238795325112867385, 1.000000000000000000, 0.9238795325112867385, 1.000000000000000000, 0.9238795325112867385, 1.000000000000000000, 0.9238795325112867385, 1.000000000000000000, 0.9238795325112867385, 1.000000000000000000, 0.9238795325112867385, 1.000000000000000000, 0.9238795325112867385, 1.000000000000000000, 0.9238795325112867385, 1.000000000000000000, 0.9238795325112867385, 1.000000000000000000, 0.9238795325112867385, 1.000000000000000000, 0.9238795325112867385, 1.000000000000000000, 0.9238795325112867385, 1.000000000000000000, 0.9238795325112867385, 1.000000000000000000, 0.9238795325112867385, 1.000000000000000000, 0.9238795325112867385, 1.000000000000000000, 0.9238795325112867385, 1.000000000000000000, 0.9238795325112867385, 1.000000000000000000, 0.9238795325112867385, 1.000000000000000000, 0.9238795325112867385, 1.000000000000000000, 0.9238795325112867385, 1.000000000000000000, 0.9238795325112867385, 1.000000000000000000, 0.9238795325112867385, 1.000000000000000000, 0.9238795325112867385, 1.000000000000000000, 0.9238795325112867385, 1.000000000000000000, 0.9238795325112867385, 1.000000000000000000, 0.9238795325112867385, 1.000000000000000000, 0.9238795325112867385, 1.000000000000000000, 0.9238795325112867385, 1.000000000000000000, 0.9238795325112867385, 1.000000000000000000, 0.9238795325112867385, 1.000000000000000000, 0.9238795325112867385, 1.000000000000000000, 0.9238795325112867385, 1.000000000000000000, 0.9238795325112867385, 1.000000000000000000),
 ( 1.000000000000000000, 0.9238795325112867385, 1.000000000000000000, 0.9238795325112867385, 1.000000000000000000, 0.9238795325112867385, 1.000000000000000000, 0.9238795325112867385, 1.000000000000000000, 0.9238795325112867385, 1.000000000000000000, 0.9238795325112867385, 1.000000000000000000, 0.9238795325112867385, 1.000000000000000000, 0.9238795325112867385, 1.000000000000000000, 0.9238795325112867385, 1.000000000000000000, 0.9238795325112867385, 1.000000000000000000, 0.9238795325112867385, 1.000000000000000000, 0.9238795325112867385, 1.000000000000000000, 0.9238795325112867385, 1.000000000000000000, 0.9238795325112867385, 1.000000000000000000, 0.9238795325112867385, 1.000000000000000000, 0.9238795325112867385, 1.000000000000000000, 0.9238795325112867385, 1.000000000000000000, 0.9238795325112867385, 1.000000000000000000, 0.9238795325112867385, 1.000000000000000000, 0.9238795325112867385, 1.000000000000000000, 0.9238795325112867385, 1.000000000000000000, 0.9238795325112867385, 1.000000000000000000, 0.9238795325112867385, 1.000000000000000000, 0.9238795325112867385, 1.000000000000000000, 0.9238795325112867385, 1.000000000000000000, 0.9238795325112867385, 1.000000000000000000, 0.9238795325112867385, 1.000000000000000000, 0.9238795325112867385, 1.000000000000000000, 0.9238795325112867385, 1.000000000000000000, 0.9238795325112867385, 1.000000000000000000, 0.9238795325112867385, 1.000000000000000000, 0.9238795325112867385, 1.000000000000000000, 0.9238795325112867385, 1.000000000000000000, 0.9238795325112867385, 1.000000000000000000, 0.9238795325112867385, 1.000000000000000000, 0.9238795325112867385, 1.000000000000000000, 0.9238795325112867385, 1.000000000000000000, 0.9238795325112867385, 1.000000000000000000, 0.9238795325112867385, 1.000000000000000000, 0.9238795325112867385, 1.000000000000000000, 0.9238795325112867385, 1.000000000000000000, 0.9238795325112867385, 1.000000000000000000, 0.9238795325112867385, 1.000000000000000000, 0.9238795325112867385, 1.000000000000000000, 0.9238795325112867385, 1.000000000000000000, 0.9238795325112867385, 1.000000000000000000, 0.9238795325112867385, 1.000000000000000000, 0.9238795325112867385, 1.000000000000000000, 0.9238795325112867385, 1.000000000000000000, 0.9238795325112867385, 1.000000000000000000, 0.9238795325112867385, 1.000000000000000000, 0.9238795325112867385, 1.000000000000000000, 0.9238795325112867385, 1.000000000000000000, 0.9238795325112867385, 1.000000000000000000, 0.9238795325112867385, 1.000000000000000000, 0.9238795325112867385, 1.000000000000000000, 0.9238795325112867385, 1.000000000000000000, 0.9238795325112867385, 1.000000000000000000, 0.9238795325112867385, 1.000000000000000000, 0.9238795325112867385, 1.000000000000000000, 0.9238795325112867385, 1.000000000000000000, 0.9238795325112867385, 1.000000000000000000, 0.9238795325112867385, 1.000000000000000000, 0.9238795325112867385, 1.000000000000000000, 0.9238795325112867385, 1.000000000000000000, 0.9238795325112867385, 1.000000000000000000, 0.9238795325112867385, 1.000000000000000000, 0.9238795325112867385, 1.000000000000000000, 0.9238795325112867385, 1.000000000000000000, 0.9238795325112867385, 1.000000000000000000, 0.9238795325112867385, 1.000000000000000000, 0.9238795325112867385, 1.000000000000000000, 0.9238795325112867385, 1.000000000000000000, 0.9238795325112867385, 1.000000000000000000, 0.9238795325112867385, 1.000000000000000000, 0.9238795325112867385, 1.000000000000000000, 0.9238795325112867385, 1.000000000000000000, 0.9238795325112867385, 1.000000000000000000, 0.9238795325112867385, 1.000000000000000000, 0.9238795325112867385, 1.000000000000000000, 0.9238795325112867385, 1.000000000000000000, 0.9238795325112867385, 1.000000000000000000, 0.9238795325112867385, 1.000000000000000000, 0.9238795325112867385, 1.000000000000000000, 0.9238795325112867385, 1.000000000000000000, 0.9238795325112867385, 1.000000000000000000, 0.9238795325112867385, 1.000000000000000000, 0.9238795325112867385, 1.000000000000000000, 0.9238795325112867385, 1.000000000000000000, 0.9238795325112867385, 1.000000000000000000, 0.9238795325112867385, 1.000000000000000000, 0.9238795325112867385, 1.000000000000000000, 0.9238795325112867385, 1.000000000000000000, 0.9238795325112867385, 1.000000000000000000, 0.9238795325112867385, 1.000000000000000000, 0.9238795325112867385, 1.000000000000000000, 0.9238795325112867385, 1.000000000000000000, 0.9238795325112867385, 1.000000000000000000, 0.9238795325112867385, 1.000000000000000000, 0.9238795325112867385, 1.000000000000000000, 0.9238795325112867385, 1.000000000000000000, 0.9238795325112867385, 1.000000000000000000, 0.9238795325112867385, 1.000000000000000000, 0.9238795325112867385, 1.000000000000000000, 0.9238795325112867385, 1.000000000000000000, 0.9238795325112867385, 1.000000000000000000, 0.9238795325112867385, 1.000000000000000000, 0.9238795325112867385, 1.000000000000000000, 0.9238795325112867385, 1.000000000000000000, 0.9238795325112867385, 1.000000000000000000, 0.9238795325112867385, 1.000000000000000000, 0.9238795325112867385, 1.000000000000000000, 0.9238795325112867385, 1.000000000000000000, 0.9238795325112867385, 1.000000000000000000, 0.9238795325112867385, 1.000000000000000000, 0.9238795325112867385, 1.000000000000000000, 0.9238795325112867385, 1.000000000000000000, 0.9238795325112867385, 1.000000000000000000, 0.9238795325112867385, 1.000000000000000000, 0.9238795325112867385, 1.000000000000000000, 0.9238795325112867385, 1.000000000000000000, 0.9238795325112867385, 1.000000000000000000, 0.9238795325112867385, 1.000000000000000000, 0.9238795325112867385, 1.000000000000000000, 0.9238795325112867385, 1.000000000000000000, 0.9238795325112867385, 1.000000000000000000, 0.9238795325112867385, 1.000000000000000000, 0.9238795325112867385, 1.000000000000000000, 0.9238795325112867385, 1.000000000000000000, 0.9238795325112867385, 1.000000000000000000, 0.9238795325112867385, 1.000000000000000000, 0.9238795325112867385, 1.000000000000000000) ) ) 
 REPRESENTATION_ITEM ( '' )  SURFACE ( )  );
#16944=CARTESIAN_POINT ( 'NONE',  ( 108.7113248654051176, 2.000000000000057288, 0.000000000000000000 ) ) ;
#16945=CARTESIAN_POINT ( 'NONE',  ( 104.6874999999998437, -1.035533905932689347, -2.499999999999724221 ) ) ;
#16951=CARTESIAN_POINT ( 'NONE',  ( 107.8511751345945129, -1.999999999999941602, -0.8284271247460553989 ) ) ;
#16953=CARTESIAN_POINT ( 'NONE',  ( 117.9136751345946266, -1.414213562373201061, -1.414213562373034527 ) ) ;
#16956=CARTESIAN_POINT ( 'NONE',  ( 118.0622167782374277, -1.849990392679381701, 0.7662911109079489913 ) ) ;
#16961=CARTESIAN_POINT ( 'NONE',  ( 116.5624999999998721, -2.499999999999844569, -1.035533905932629173 ) ) ;
#16971=EDGE_CURVE ( 'NONE', #19218, #10990, #15636, .T. ) ;
#16979=CARTESIAN_POINT ( 'NONE',  ( 116.1877832217621886, 0.7662911109078888172, -1.849990392679291551 ) ) ;
#16993=CARTESIAN_POINT ( 'NONE',  ( 115.6247167782374561, 1.849990392679523588, 0.000000000000000000 ) ) ;
#17015=CARTESIAN_POINT ( 'NONE',  ( 116.9136751345947260, -1.414213562373034527, -1.414213562372812483 ) ) ;
#17016=CARTESIAN_POINT ( 'NONE',  ( 119.9999999999997868, 1.387778780781445676E-13, 1.110223024625156540E-13 ) ) ;
#17024=CARTESIAN_POINT ( 'NONE',  ( 109.1874999999997584, 1.035533905932839449, 2.500000000000205169 ) ) ;
#17042=CARTESIAN_POINT ( 'NONE',  ( 107.9999999999998863, 2.500000000000002220, 0.000000000000000000 ) ) ;
#17052=CARTESIAN_POINT ( 'NONE',  ( 105.3127832217621034, 1.849990392679562001, -0.7662911109076485650 ) ) ;
#17055=DIRECTION ( 'NONE',  ( -1.000000000000000000, -1.665334536937736783E-16, -2.220446049250315546E-16 ) ) ;
#17071=DIRECTION ( 'NONE',  ( -1.000000000000000000, -1.665334536937736783E-16, -2.220446049250315546E-16 ) ) ;
#17075=LINE ( 'NONE', #24107, #17949 ) ;
#17094=CARTESIAN_POINT ( 'NONE',  ( 106.1249999999999858, 1.767766952966320915, 1.767766952966431937 ) ) ;
#17096=CARTESIAN_POINT ( 'NONE',  ( 108.5238248654049755, 0.8284271247463257382, -1.999999999999731104 ) ) ;
#17100=CARTESIAN_POINT ( 'NONE',  ( 118.1011751345946124, 0.8284271247463257382, -1.999999999999851674 ) ) ;
#17103=CARTESIAN_POINT ( 'NONE',  ( 119.3122167782375556, -0.7662911109076785410, -1.849990392679411677 ) ) ;
#17109=CARTESIAN_POINT ( 'NONE',  ( 117.4999999999999574, -2.499999999999891198, 0.000000000000000000 ) ) ;
#17126=CARTESIAN_POINT ( 'NONE',  ( 117.0627832217621318, -0.7662911109077686911, -1.849990392679231599 ) ) ;
#17139=EDGE_CURVE ( 'NONE', #7046, #22143, #21274, .T. ) ;
#17155=CARTESIAN_POINT ( 'NONE',  ( 119.9999999999998721, 2.445790564474887852, 0.3393521411448525704 ) ) ;
#17157=FACE_OUTER_BOUND ( 'NONE', #14724, .T. ) ;
#17171=CARTESIAN_POINT ( 'NONE',  ( 110.1249999999998437, 1.767766952966265404, 1.767766952966431937 ) ) ;
#17178=DIRECTION ( 'NONE',  ( -1.000000000000000000, -1.665334536937736783E-16, -2.220446049250315546E-16 ) ) ;
#17180=CARTESIAN_POINT ( 'NONE',  ( 119.0627832217622739, -0.7662911109077388261, -1.849990392679291551 ) ) ;
#17191=ORIENTED_EDGE ( 'NONE', *, *, #26464, .F. ) ;
#17202=CARTESIAN_POINT ( 'NONE',  ( 119.9374999999996874, 2.500000000000114575, -1.035533905932388699 ) ) ;
#17244=CARTESIAN_POINT ( 'NONE',  ( 107.3124999999996589, -1.035533905932598975, 2.500000000000205169 ) ) ;
#17247=CARTESIAN_POINT ( 'NONE',  ( 108.4613248654050892, 5.551115123125782702E-14, -2.000000000000001776 ) ) ;
#17256=CARTESIAN_POINT ( 'NONE',  ( 118.1247167782376408, -1.849990392679523588, 0.000000000000000000 ) ) ;
#17262=CARTESIAN_POINT ( 'NONE',  ( 115.7499999999998153, -1.110223024625156540E-13, -2.499999999999946709 ) ) ;
#17264=AXIS2_PLACEMENT_3D ( 'NONE', #14174, #23512, #2454 ) ;
#17283=CARTESIAN_POINT ( 'NONE',  ( 106.7113248654050324, 2.000000000000001776, 1.110223024625156540E-13 ) ) ;
#17333=CARTESIAN_POINT ( 'NONE',  ( 121.0627832217620750, -0.7662911109076785410, -1.849990392679291551 ) ) ;
#17353=CARTESIAN_POINT ( 'NONE',  ( 119.8124999999998863, 1.035533905932839449, -2.499999999999844569 ) ) ;
#17362=LINE ( 'NONE', #19646, #14081 ) ;
#17365=CARTESIAN_POINT ( 'NONE',  ( 120.1874999999997016, 1.035533905932809473, 2.500000000000205169 ) ) ;
#17385=DIRECTION ( 'NONE',  ( 5.551115123125783935E-17, -1.000000000000000000, -8.881784197001254296E-16 ) ) ;
#17386=CARTESIAN_POINT ( 'NONE',  ( 10.00000000000002309, 8.326672684688674053E-14, 1.110223024625156540E-13 ) ) ;
#17391=CARTESIAN_POINT ( 'NONE',  ( 105.4999999999999147, -2.499999999999919176, 1.110223024625156540E-13 ) ) ;
#17393=EDGE_CURVE ( 'NONE', #1437, #13422, #29010, .T. ) ;
#17396=CARTESIAN_POINT ( 'NONE',  ( 108.2738248654049471, -1.999999999999941602, -0.8284271247459952248 ) ) ;
#17399=DIRECTION ( 'NONE',  ( 5.551115123125785167E-17, -1.000000000000000000, -8.881784197001256268E-16 ) ) ;
#17405=CARTESIAN_POINT ( 'NONE',  ( 115.4372167782374561, 0.7662911109078287542, -1.849990392679231599 ) ) ;
#17410=CARTESIAN_POINT ( 'NONE',  ( 114.0624999999997300, 2.500000000000115019, 1.035533905932989551 ) ) ;
#17418=ADVANCED_FACE ( 'NONE', ( #4574 ), #13999, .F. ) ;
#17431=LINE ( 'NONE', #8647, #28120 ) ;
#17436=DIRECTION ( 'NONE',  ( -1.000000000000000000, -1.665334536937736783E-16, -2.220446049250315546E-16 ) ) ;
#17438=CARTESIAN_POINT ( 'NONE',  ( 115.0863248654050608, -1.414213562373090038, 1.414213562373256572 ) ) ;
#17439=CARTESIAN_POINT ( 'NONE',  ( 111.7497167782375129, 1.308140751793751555, 1.308140751793973600 ) ) ;
#17448=VERTEX_POINT ( 'NONE', #12137 ) ;
#17463=SURFACE_SIDE_STYLE ('',( #17617 ) ) ;
#17465=CARTESIAN_POINT ( 'NONE',  ( 104.3747167782376124, -5.551115123125782702E-14, -1.849990392679523588 ) ) ;
#17473=DIRECTION ( 'NONE',  ( -1.000000000000000000, -1.665334536937736783E-16, -2.220446049250315546E-16 ) ) ;
#17479=CARTESIAN_POINT ( 'NONE',  ( 104.4997167782375413, 1.308140751793668288, -1.308140751793640533 ) ) ;
#17490=CARTESIAN_POINT ( 'NONE',  ( 113.7113248654051034, 2.000000000000057288, 0.000000000000000000 ) ) ;
#17499=CARTESIAN_POINT ( 'NONE',  ( 118.3749999999999147, -1.767766952966293159, 1.767766952966431937 ) ) ;
#17513=CARTESIAN_POINT ( 'NONE',  ( 119.2499999999999574, -5.551115123125782702E-14, 2.500000000000168754 ) ) ;
#17531=CARTESIAN_POINT ( 'NONE',  ( 113.7113248654051034, 2.000000000000057288, 0.000000000000000000 ) ) ;
#17544=AXIS2_PLACEMENT_3D ( 'NONE', #21883, #821, #7880 ) ;
#17545=VECTOR ( 'NONE', #27335, 1000.000000000000000 ) ;
#17553=CARTESIAN_POINT ( 'NONE',  ( 112.6011751345947545, -0.8284271247462053900, 2.000000000000151879 ) ) ;
#17557=CARTESIAN_POINT ( 'NONE',  ( 112.3122167782374987, -0.7662911109076785410, -1.849990392679291551 ) ) ;
#17563=CARTESIAN_POINT ( 'NONE',  ( 113.6249999999998721, -1.767766952966376426, -1.767766952966431937 ) ) ;
#17594=CARTESIAN_POINT ( 'NONE',  ( 111.4372167782375271, 0.7662911109078888172, -1.849990392679231599 ) ) ;
#17612=CARTESIAN_POINT ( 'NONE',  ( 110.2886751345946834, 2.000000000000085265, 1.110223024625156540E-13 ) ) ;
#17617=SURFACE_STYLE_FILL_AREA ( #29238 ) ;
#17630=EDGE_CURVE ( 'NONE', #2147, #15812, #3606, .T. ) ;
#17633=CARTESIAN_POINT ( 'NONE',  ( 109.9136751345947260, -1.414213562373090038, -1.414213562373145550 ) ) ;
#17634=CARTESIAN_POINT ( 'NONE',  ( 117.1877832217620892, 0.7662911109078287542, -1.849990392679472073 ) ) ;
#17642=CARTESIAN_POINT ( 'NONE',  ( 105.4374999999998153, -2.499999999999994671, 1.035533905932929599 ) ) ;
#17650=CARTESIAN_POINT ( 'NONE',  ( 120.3750000000000284, -1.767766952966376426, 1.767766952966320915 ) ) ;
#17654=CARTESIAN_POINT ( 'NONE',  ( 0.000000000000000000, 0.000000000000000000, 0.000000000000000000 ) ) ;
#17664=CARTESIAN_POINT ( 'NONE',  ( 111.0002832217622597, -1.308140751793557266, -1.308140751793640533 ) ) ;
#17693=CARTESIAN_POINT ( 'NONE',  ( 113.8752832217622313, -1.849990392679523588, 0.000000000000000000 ) ) ;
#17704=CARTESIAN_POINT ( 'NONE',  ( 0.000000000000000000, 0.000000000000000000, 0.000000000000000000 ) ) ;
#17709=CARTESIAN_POINT ( 'NONE',  ( 114.9372167782374135, -0.7662911109077987781, 1.849990392679591977 ) ) ;
#17715=CARTESIAN_POINT ( 'NONE',  ( 114.6874999999997158, -1.035533905932689347, -2.499999999999784173 ) ) ;
#17734=CARTESIAN_POINT ( 'NONE',  ( 105.6636751345948113, -1.414213562373117794, 1.414213562373145550 ) ) ;
#17743=CARTESIAN_POINT ( 'NONE',  ( 108.3124999999997442, -1.035533905932629173, 2.500000000000205169 ) ) ;
#17765=CARTESIAN_POINT ( 'NONE',  ( 105.1011751345946124, 0.8284271247462955401, -1.999999999999731104 ) ) ;
#17769=CARTESIAN_POINT ( 'NONE',  ( 106.4613248654051176, 5.551115123125782702E-14, -1.999999999999890754 ) ) ;
#17788=AXIS2_PLACEMENT_3D ( 'NONE', #11900, #16503, #23244 ) ;
#17789=CARTESIAN_POINT ( 'NONE',  ( 120.4997167782374703, 1.308140751793723799, -1.308140751793640533 ) ) ;
#17793=CARTESIAN_POINT ( 'NONE',  ( 110.2886751345946834, 2.000000000000085265, 1.110223024625156540E-13 ) ) ;
#17794=CARTESIAN_POINT ( 'NONE',  ( 118.3127832217620750, 1.849990392679532247, -0.7662911109075883909 ) ) ;
#17809=LINE ( 'NONE', #25898, #13070 ) ;
#17812=CARTESIAN_POINT ( 'NONE',  ( 115.2499999999998721, -5.551115123125782702E-14, 2.500000000000057732 ) ) ;
#17824=CARTESIAN_POINT ( 'NONE',  ( 120.7499999999998721, 1.110223024625156540E-13, -2.499999999999946709 ) ) ;
#17825=CARTESIAN_POINT ( 'NONE',  ( 109.9377832217622029, -1.849990392679472073, -0.7662911109076485650 ) ) ;
#17830=CARTESIAN_POINT ( 'NONE',  ( 108.1872167782373850, -1.849990392679472073, -0.7662911109077087390 ) ) ;
#17845=SURFACE_STYLE_FILL_AREA ( #29314 ) ;
#17854=CARTESIAN_POINT ( 'NONE',  ( 115.8127832217621460, -1.849990392679472073, 0.7662911109078888172 ) ) ;
#17858=CARTESIAN_POINT ( 'NONE',  ( 119.9999999999998437, 2.265773637424566278, -0.8226836970581136166 ) ) ;
#17870=CARTESIAN_POINT ( 'NONE',  ( 114.4372167782375271, 0.7662911109078588412, -1.849990392679351725 ) ) ;
#17872=CARTESIAN_POINT ( 'NONE',  ( 113.7886751345947687, -1.999999999999918510, 0.000000000000000000 ) ) ;
#17875=CARTESIAN_POINT ( 'NONE',  ( 115.1874999999998579, 1.035533905932719101, 2.500000000000265121 ) ) ;
#17876=ORIENTED_EDGE ( 'NONE', *, *, #7607, .T. ) ;
#17878=EDGE_CURVE ( 'NONE', #29332, #13966, #10667, .T. ) ;
#17901=CARTESIAN_POINT ( 'NONE',  ( 107.6874999999997726, -1.035533905932659149, -2.499999999999724221 ) ) ;
#17918=EDGE_CURVE ( 'NONE', #20178, #26967, #14371, .T. ) ;
#17924=CARTESIAN_POINT ( 'NONE',  ( 110.4761751345946976, 0.8284271247462354770, 2.000000000000212275 ) ) ;
#17935=CARTESIAN_POINT ( 'NONE',  ( 114.7113248654050750, 2.000000000000057288, 0.000000000000000000 ) ) ;
#17938=CARTESIAN_POINT ( 'NONE',  ( 119.8747167782375982, 0.000000000000000000, 1.849990392679523588 ) ) ;
#17940=( BOUNDED_CURVE ( )  B_SPLINE_CURVE ( 2, ( #25474, #3973, #25313, #6592, #2304, #9208, #2151, #6896, #25165 ),
 .UNSPECIFIED., .F., .F. ) 
 B_SPLINE_CURVE_WITH_KNOTS ( ( 3, 2, 2, 2, 3 ),
 ( 0.4705882352941176405, 0.4779411764705882582, 0.4852941176470588203, 0.4926470588235294379, 0.5000000000000000000 ),
 .UNSPECIFIED. ) 
 CURVE ( )  GEOMETRIC_REPRESENTATION_ITEM ( )  RATIONAL_B_SPLINE_CURVE ( ( 1.000000000000000000, 0.9238795325112867385, 1.000000000000000000, 0.9238795325112867385, 1.000000000000000000, 0.9238795325112867385, 1.000000000000000000, 0.9238795325112867385, 1.000000000000000000 ) ) 
 REPRESENTATION_ITEM ( '' )  );
#17945=CARTESIAN_POINT ( 'NONE',  ( 116.5627832217621034, 0.7662911109078888172, 1.849990392679652151 ) ) ;
#17949=VECTOR ( 'NONE', #28852, 1000.000000000000000 ) ;
#17964=CARTESIAN_POINT ( 'NONE',  ( 115.5624999999999005, -2.499999999999934719, -1.035533905932568777 ) ) ;
#17967=CYLINDRICAL_SURFACE ( 'NONE', #27626, 2.000000000000012879 ) ;
#17974=CARTESIAN_POINT ( 'NONE',  ( 115.6874999999997584, -1.035533905932719101, -2.499999999999844569 ) ) ;
#17975=CARTESIAN_POINT ( 'NONE',  ( 110.6252832217622029, 5.551115123125782702E-14, 1.849990392679523588 ) ) ;
#17976=CARTESIAN_POINT ( 'NONE',  ( 108.2113248654050892, -1.999999999999946265, 0.000000000000000000 ) ) ;
#18005=CARTESIAN_POINT ( 'NONE',  ( 110.5002832217622881, 1.308140751793668288, 1.308140751793640533 ) ) ;
#18015=CARTESIAN_POINT ( 'NONE',  ( 104.7401757384973138, -1.135388960144151582, -1.480659523195497096 ) ) ;
#18019=FACE_OUTER_BOUND ( 'NONE', #15926, .T. ) ;
#18021=ORIENTED_EDGE ( 'NONE', *, *, #15780, .F. ) ;
#18022=CARTESIAN_POINT ( 'NONE',  ( 113.3122167782374277, -0.7662911109077388261, -1.849990392679231599 ) ) ;
#18026=EDGE_CURVE ( 'NONE', #19914, #12110, #21474, .T. ) ;
#18044=CARTESIAN_POINT ( 'NONE',  ( 106.2886751345948255, 2.000000000000029310, 1.110223024625156540E-13 ) ) ;
#18048=CARTESIAN_POINT ( 'NONE',  ( 0.000000000000000000, 0.000000000000000000, 0.000000000000000000 ) ) ;
#18053=ORIENTED_EDGE ( 'NONE', *, *, #10409, .F. ) ;
#18055=CARTESIAN_POINT ( 'NONE',  ( 110.8124999999999432, 1.035533905932719101, -2.499999999999904521 ) ) ;
#18057=DIRECTION ( 'NONE',  ( 5.551115123125785167E-17, -1.000000000000000000, -8.881784197001256268E-16 ) ) ;
#18065=ORIENTED_EDGE ( 'NONE', *, *, #27920, .T. ) ;
#18094=CARTESIAN_POINT ( 'NONE',  ( 116.8127832217622597, -1.849990392679441875, 0.7662911109078888172 ) ) ;
#18108=CARTESIAN_POINT ( 'NONE',  ( 118.1249999999999147, 1.767766952966320915, 1.767766952966431937 ) ) ;
#18109=ADVANCED_FACE ( 'NONE', ( #13924 ), #8661, .F. ) ;
#18111=CARTESIAN_POINT ( 'NONE',  ( 105.8988248654050750, 0.8284271247463257382, 2.000000000000271783 ) ) ;
#18118=CARTESIAN_POINT ( 'NONE',  ( 117.8749999999998010, 1.767766952966320915, -1.767766952966209892 ) ) ;
#18119=CARTESIAN_POINT ( 'NONE',  ( 110.8752832217622029, -1.849990392679495832, 0.000000000000000000 ) ) ;
#18130=VERTEX_POINT ( 'NONE', #2060 ) ;
#18144=LINE ( 'NONE', #29782, #26448 ) ;
#18148=CARTESIAN_POINT ( 'NONE',  ( 110.9377832217620323, -1.849990392679411677, -0.7662911109076485650 ) ) ;
#18158=ORIENTED_EDGE ( 'NONE', *, *, #1937, .F. ) ;
#18160=VECTOR ( 'NONE', #28185, 1000.000000000000000 ) ;
#18167=CARTESIAN_POINT ( 'NONE',  ( 108.3747167782376124, -1.665334536937734811E-13, -1.849990392679523588 ) ) ;
#18192=EDGE_CURVE ( 'NONE', #27528, #29800, #29461, .T. ) ;
#18201=CARTESIAN_POINT ( 'NONE',  ( 105.5624999999997726, -2.499999999999874767, -1.035533905932568777 ) ) ;
#18216=CARTESIAN_POINT ( 'NONE',  ( 105.0199988333806544, -0.2475512722506234553, -1.999999999999938938 ) ) ;
#18219=( GEOMETRIC_REPRESENTATION_CONTEXT ( 3 ) GLOBAL_UNCERTAINTY_ASSIGNED_CONTEXT ( ( #14321 ) ) GLOBAL_UNIT_ASSIGNED_CONTEXT ( ( #24252, #21968, #3658 ) ) REPRESENTATION_CONTEXT ( 'NONE', 'WORKASPACE' ) );
#18230=CARTESIAN_POINT ( 'NONE',  ( 118.7886751345946692, -1.999999999999918510, 2.220446049250313081E-13 ) ) ;
#18240=CARTESIAN_POINT ( 'NONE',  ( 118.0002832217622171, -1.308140751793612777, -1.308140751793418488 ) ) ;
#18259=DIRECTION ( 'NONE',  ( 1.000000000000000000, 0.000000000000000000, 0.000000000000000000 ) ) ;
#18264=CARTESIAN_POINT ( 'NONE',  ( 114.5624999999997442, -2.499999999999934719, -1.035533905932448873 ) ) ;
#18273=CARTESIAN_POINT ( 'NONE',  ( 115.3124999999998863, -1.035533905932659149, 2.500000000000205169 ) ) ;
#18275=CARTESIAN_POINT ( 'NONE',  ( 110.0627832217622313, -0.7662911109076785410, -1.849990392679171425 ) ) ;
#18279=CARTESIAN_POINT ( 'NONE',  ( 109.1872167782375413, -1.849990392679441875, -0.7662911109077087390 ) ) ;
#18282=CARTESIAN_POINT ( 'NONE',  ( 111.0863248654051318, -1.414213562373034527, 1.414213562373145550 ) ) ;
#18291=ORIENTED_EDGE ( 'NONE', *, *, #28855, .F. ) ;
#18296=CARTESIAN_POINT ( 'NONE',  ( 5.000000000000018652, -5.999999999999914735, 1.056932319443149026E-13 ) ) ;
#18303=FACE_OUTER_BOUND ( 'NONE', #12802, .T. ) ;
#18313=( BOUNDED_CURVE ( )  B_SPLINE_CURVE ( 2, ( #10789, #12793, #26862, #26571, #3673, #3364, #19536, #5520, #20138 ),
 .UNSPECIFIED., .F., .T. ) 
 B_SPLINE_CURVE_WITH_KNOTS ( ( 3, 2, 2, 2, 3 ),
 ( 0.7647058823529411242, 0.7720588235294117974, 0.7794117647058823595, 0.7867647058823529216, 0.7941176470588234837 ),
 .UNSPECIFIED. ) 
 CURVE ( )  GEOMETRIC_REPRESENTATION_ITEM ( )  RATIONAL_B_SPLINE_CURVE ( ( 1.000000000000000000, 0.9238795325112867385, 1.000000000000000000, 0.9238795325112867385, 1.000000000000000000, 0.9238795325112867385, 1.000000000000000000, 0.9238795325112867385, 1.000000000000000000 ) ) 
 REPRESENTATION_ITEM ( '' )  );
#18317=CARTESIAN_POINT ( 'NONE',  ( 108.2113248654050892, -1.999999999999946265, 0.000000000000000000 ) ) ;
#18321=CARTESIAN_POINT ( 'NONE',  ( 107.8747167782375840, 0.000000000000000000, 1.849990392679523588 ) ) ;
#18323=CARTESIAN_POINT ( 'NONE',  ( 113.7497167782375698, 1.308140751793557266, 1.308140751793751555 ) ) ;
#18326=COLOUR_RGB ( '', 0.40784314, 0.44705882, 0.49803922) ;
#18327=CARTESIAN_POINT ( 'NONE',  ( 104.7401757384975127, 1.770091586386960403, 0.5493589524125325196 ) ) ;
#18341=EDGE_CURVE ( 'NONE', #27528, #25684, #16151, .T. ) ;
#18344=CARTESIAN_POINT ( 'NONE',  ( 111.7113248654050892, 2.000000000000057288, 0.000000000000000000 ) ) ;
#18347=CARTESIAN_POINT ( 'NONE',  ( 110.4374999999997442, -2.500000000000024425, 1.035533905932809473 ) ) ;
#18357=CARTESIAN_POINT ( 'NONE',  ( 105.7499999999998010, 1.110223024625156540E-13, -2.499999999999946709 ) ) ;
#18375=CARTESIAN_POINT ( 'NONE',  ( 119.0627832217622739, -0.7662911109077388261, -1.849990392679291551 ) ) ;
#18387=CARTESIAN_POINT ( 'NONE',  ( 0.000000000000000000, 0.000000000000000000, 0.000000000000000000 ) ) ;
#18390=CARTESIAN_POINT ( 'NONE',  ( 116.8122167782373992, 0.7662911109079189043, 1.849990392679652151 ) ) ;
#18391=DIRECTION ( 'NONE',  ( 0.8660254037844379305, 0.5000000000000011102, 6.363854784884201318E-16 ) ) ;
#18396=CARTESIAN_POINT ( 'NONE',  ( 115.8752832217622313, -1.849990392679468076, 1.110223024625156540E-13 ) ) ;
#18409=VERTEX_POINT ( 'NONE', #23363 ) ;
#18414=CARTESIAN_POINT ( 'NONE',  ( 116.6874999999997726, -1.035533905932659149, -2.499999999999784173 ) ) ;
#18420=ORIENTED_EDGE ( 'NONE', *, *, #25836, .T. ) ;
#18421=CARTESIAN_POINT ( 'NONE',  ( 117.6250000000000000, -1.767766952966376426, -1.767766952966320915 ) ) ;
#18423=CARTESIAN_POINT ( 'NONE',  ( 107.7502832217622881, -1.308140751793585022, 1.308140751793751555 ) ) ;
#18441=EDGE_LOOP ( 'NONE', ( #12762, #13690, #19207, #1362, #23451, #29155, #18291 ) ) ;
#18448=FACE_OUTER_BOUND ( 'NONE', #24424, .T. ) ;
#18452=CARTESIAN_POINT ( 'NONE',  ( 110.3752832217623592, 1.849990392679495832, 0.000000000000000000 ) ) ;
#18460=CARTESIAN_POINT ( 'NONE',  ( 114.6636751345947829, -1.414213562373034527, 1.414213562373367594 ) ) ;
#18463=EDGE_CURVE ( 'NONE', #15450, #18409, #13555, .T. ) ;
#18466=CARTESIAN_POINT ( 'NONE',  ( 109.8747167782376124, -2.775557561562891351E-14, 1.849990392679523588 ) ) ;
#18468=CARTESIAN_POINT ( 'NONE',  ( 112.9997167782376835, -1.308140751793557266, 1.308140751793751555 ) ) ;
#18473=CARTESIAN_POINT ( 'NONE',  ( 104.7401757384972996, 1.536076471655371645, 1.055243095569078138 ) ) ;
#18490=CARTESIAN_POINT ( 'NONE',  ( 111.8511751345945839, -2.000000000000061728, -0.8284271247458748766 ) ) ;
#18495=CARTESIAN_POINT ( 'NONE',  ( 108.6249999999999289, -1.767766952966320915, -1.767766952966320915 ) ) ;
#18496=CARTESIAN_POINT ( 'NONE',  ( 106.4761751345946834, 0.8284271247463257382, 2.000000000000091926 ) ) ;
#18506=CARTESIAN_POINT ( 'NONE',  ( 106.7499999999999147, -8.326672684688674053E-14, -2.499999999999946709 ) ) ;
#18523=CARTESIAN_POINT ( 'NONE',  ( 120.1252832217621176, -5.551115123125782702E-14, -1.849990392679523588 ) ) ;
#18530=EDGE_CURVE ( 'NONE', #7379, #1437, #19102, .T. ) ;
#18536=CARTESIAN_POINT ( 'NONE',  ( 111.7886751345948255, -1.999999999999974021, 0.000000000000000000 ) ) ;
#18542=CARTESIAN_POINT ( 'NONE',  ( 118.2497167782374419, -1.308140751793585022, -1.308140751793640533 ) ) ;
#18548=CARTESIAN_POINT ( 'NONE',  ( 113.6877832217621460, -0.7662911109077987781, 1.849990392679591977 ) ) ;
#18566=CARTESIAN_POINT ( 'NONE',  ( 111.2499999999999432, -1.110223024625156540E-13, 2.500000000000057732 ) ) ;
#18567=ADVANCED_FACE ( 'NONE', ( #24229 ), #2594, .T. ) ;
#18578=CARTESIAN_POINT ( 'NONE',  ( 118.6249999999998010, -1.767766952966431937, -1.767766952966209892 ) ) ;
#18580=CARTESIAN_POINT ( 'NONE',  ( 105.2502832217622881, 1.308140751793668288, -1.308140751793640533 ) ) ;
#18600=DIRECTION ( 'NONE',  ( 5.551115123125785167E-17, -1.000000000000000000, -8.881784197001256268E-16 ) ) ;
#18602=CARTESIAN_POINT ( 'NONE',  ( 109.5002832217622881, 1.308140751793640533, 1.308140751793640533 ) ) ;
#18609=EDGE_CURVE ( 'NONE', #26967, #23925, #2219, .T. ) ;
#18616=CARTESIAN_POINT ( 'NONE',  ( 108.5622167782374277, 1.849990392679501827, -0.7662911109077087390 ) ) ;
#18637=CARTESIAN_POINT ( 'NONE',  ( 111.9761751345947118, -0.8284271247462053900, -1.999999999999731104 ) ) ;
#18642=CARTESIAN_POINT ( 'NONE',  ( 111.1874999999999858, 1.035533905932749299, 2.500000000000265121 ) ) ;
#18648=CARTESIAN_POINT ( 'NONE',  ( 114.9761751345945697, -0.8284271247461453269, -1.999999999999791278 ) ) ;
#18657=CARTESIAN_POINT ( 'NONE',  ( 105.4999999999999147, -2.499999999999919176, 1.110223024625156540E-13 ) ) ;
#18674=CARTESIAN_POINT ( 'NONE',  ( 106.4997167782374845, 1.308140751793640533, -1.308140751793418488 ) ) ;
#18676=CARTESIAN_POINT ( 'NONE',  ( 117.5002832217622455, 1.308140751793696044, 1.308140751793862577 ) ) ;
#18694=CARTESIAN_POINT ( 'NONE',  ( 119.8511751345945981, -1.999999999999941602, -0.8284271247460553989 ) ) ;
#18695=CARTESIAN_POINT ( 'NONE',  ( 119.4372167782374419, 0.7662911109078888172, -1.849990392679291551 ) ) ;
#18700=CARTESIAN_POINT ( 'NONE',  ( 114.1877832217620892, 0.7662911109078588412, -1.849990392679291551 ) ) ;
#18707=AXIS2_PLACEMENT_3D ( 'NONE', #6135, #26848, #3509 ) ;
#18718=DIRECTION ( 'NONE',  ( -1.000000000000000000, -1.665334536937736783E-16, -2.220446049250315546E-16 ) ) ;
#18720=CARTESIAN_POINT ( 'NONE',  ( 111.9999999999999716, 2.500000000000002220, 0.000000000000000000 ) ) ;
#18724=CARTESIAN_POINT ( 'NONE',  ( 115.2886751345946550, 2.000000000000112799, 3.330669073875469621E-13 ) ) ;
#18729=CARTESIAN_POINT ( 'NONE',  ( 114.8749999999998295, 1.767766952966320915, -1.767766952966209892 ) ) ;
#18732=CARTESIAN_POINT ( 'NONE',  ( 106.6252832217623023, 2.775557561562891351E-14, 1.849990392679634610 ) ) ;
#18735=CARTESIAN_POINT ( 'NONE',  ( 113.8511751345944987, -1.999999999999881650, -0.8284271247459952248 ) ) ;
#18738=CARTESIAN_POINT ( 'NONE',  ( 106.1872167782374703, -1.849990392679381701, -0.7662911109075283278 ) ) ;
#18751=CARTESIAN_POINT ( 'NONE',  ( 110.0624999999998295, 2.499999999999994671, 1.035533905932809473 ) ) ;
#18752=VECTOR ( 'NONE', #1071, 1000.000000000000000 ) ;
#18754=CARTESIAN_POINT ( 'NONE',  ( 109.3511751345945981, 2.000000000000091926, 0.8284271247462955401 ) ) ;
#18757=CARTESIAN_POINT ( 'NONE',  ( 107.0002832217622597, -1.308140751793585022, -1.308140751793640533 ) ) ;
#18765=AXIS2_PLACEMENT_3D ( 'NONE', #18387, #4370, #73 ) ;
#18771=CARTESIAN_POINT ( 'NONE',  ( 116.4761751345946124, 0.8284271247462955401, 2.000000000000271783 ) ) ;
#18774=CARTESIAN_POINT ( 'NONE',  ( 108.3122167782374135, -0.7662911109077388261, -1.849990392679351725 ) ) ;
#18778=CARTESIAN_POINT ( 'NONE',  ( 113.2738248654050182, -1.999999999999941602, -0.8284271247459952248 ) ) ;
#18796=CARTESIAN_POINT ( 'NONE',  ( 108.8363248654051034, 1.414213562373090038, 1.414213562373034527 ) ) ;
#18797=CARTESIAN_POINT ( 'NONE',  ( 111.9374999999998010, 2.500000000000115019, -1.035533905932508825 ) ) ;
#18805=AXIS2_PLACEMENT_3D ( 'NONE', #20700, #11038, #18259 ) ;
#18808=CARTESIAN_POINT ( 'NONE',  ( 106.2499999999999716, -2.775557561562891351E-14, 2.499999999999946709 ) ) ;
#18820=CARTESIAN_POINT ( 'NONE',  ( 108.9136751345947260, -1.414213562373228816, -1.414213562373034527 ) ) ;
#18823=CARTESIAN_POINT ( 'NONE',  ( 119.9613248654051034, 1.110223024625156540E-13, 2.000000000000001776 ) ) ;
#18824=CARTESIAN_POINT ( 'NONE',  ( 105.9997167782375982, -1.308140751793612777, 1.308140751793640533 ) ) ;
#18826=CARTESIAN_POINT ( 'NONE',  ( 120.8127832217621318, -1.849990392679411677, 0.7662911109079489913 ) ) ;
#18831=CARTESIAN_POINT ( 'NONE',  ( 116.2886751345946124, 2.000000000000168310, 3.330669073875469621E-13 ) ) ;
#18846=CARTESIAN_POINT ( 'NONE',  ( 117.9997167782376266, -1.308140751793696044, 1.308140751793751555 ) ) ;
#18851=CARTESIAN_POINT ( 'NONE',  ( 114.5002832217623023, 1.308140751793696044, 1.308140751793640533 ) ) ;
#18854=ORIENTED_EDGE ( 'NONE', *, *, #29631, .T. ) ;
#18855=ORIENTED_EDGE ( 'NONE', *, *, #20409, .F. ) ;
#18869=CARTESIAN_POINT ( 'NONE',  ( 113.9374999999997300, 2.500000000000114575, -1.035533905932629173 ) ) ;
#18872=DIRECTION ( 'NONE',  ( -1.000000000000000000, -1.665334536937736783E-16, -2.220446049250315546E-16 ) ) ;
#18881=CARTESIAN_POINT ( 'NONE',  ( 113.8124999999998437, 1.035533905932749299, -2.499999999999904521 ) ) ;
#18884=CARTESIAN_POINT ( 'NONE',  ( 107.2502832217623450, 1.308140751793640533, -1.308140751793640533 ) ) ;
#18889=CARTESIAN_POINT ( 'NONE',  ( 106.8122167782374277, 0.7662911109079189043, 1.849990392679712103 ) ) ;
#18890=CARTESIAN_POINT ( 'NONE',  ( 111.1488248654049329, -1.999999999999941602, 0.8284271247462955401 ) ) ;
#18892=EDGE_LOOP ( 'NONE', ( #3734, #7073, #20563, #21671 ) ) ;
#18906=CARTESIAN_POINT ( 'NONE',  ( 106.6874999999998010, -1.035533905932689347, -2.499999999999784173 ) ) ;
#18908=VERTEX_POINT ( 'NONE', #17283 ) ;
#18912=CARTESIAN_POINT ( 'NONE',  ( 106.2502832217621460, 1.308140751793696044, -1.308140751793640533 ) ) ;
#18922=FACE_OUTER_BOUND ( 'NONE', #24182, .T. ) ;
#18927=CARTESIAN_POINT ( 'NONE',  ( 118.5863248654051461, 1.414213562373117794, -1.414213562373034527 ) ) ;
#18928=CARTESIAN_POINT ( 'NONE',  ( 110.4372167782375840, 0.7662911109078888172, -1.849990392679231599 ) ) ;
#18934=( BOUNDED_CURVE ( )  B_SPLINE_CURVE ( 2, ( #20208, #19734, #13012, #19886, #17769, #3585, #24938, #8193, #8512 ),
 .UNSPECIFIED., .F., .F. ) 
 B_SPLINE_CURVE_WITH_KNOTS ( ( 3, 2, 2, 2, 3 ),
 ( 0.8235294117647058432, 0.8308823529411765163, 0.8382352941176470784, 0.8455882352941176405, 0.8529411764705882026 ),
 .UNSPECIFIED. ) 
 CURVE ( )  GEOMETRIC_REPRESENTATION_ITEM ( )  RATIONAL_B_SPLINE_CURVE ( ( 1.000000000000000000, 0.9238795325112867385, 1.000000000000000000, 0.9238795325112867385, 1.000000000000000000, 0.9238795325112867385, 1.000000000000000000, 0.9238795325112867385, 1.000000000000000000 ) ) 
 REPRESENTATION_ITEM ( '' )  );
#18940=( BOUNDED_CURVE ( )  B_SPLINE_CURVE ( 2, ( #22025, #517, #17438, #14971, #22182, #26752, #29214, #29067, #12692 ),
 .UNSPECIFIED., .F., .T. ) 
 B_SPLINE_CURVE_WITH_KNOTS ( ( 3, 2, 2, 2, 3 ),
 ( 0.3235294117647058987, 0.3308823529411764608, 0.3382352941176470784, 0.3455882352941176405, 0.3529411764705882582 ),
 .UNSPECIFIED. ) 
 CURVE ( )  GEOMETRIC_REPRESENTATION_ITEM ( )  RATIONAL_B_SPLINE_CURVE ( ( 1.000000000000000000, 0.9238795325112867385, 1.000000000000000000, 0.9238795325112867385, 1.000000000000000000, 0.9238795325112867385, 1.000000000000000000, 0.9238795325112867385, 1.000000000000000000 ) ) 
 REPRESENTATION_ITEM ( '' )  );
#18954=CARTESIAN_POINT ( 'NONE',  ( 110.7499999999998010, 2.775557561562891351E-14, -2.499999999999946709 ) ) ;
#18965=CARTESIAN_POINT ( 'NONE',  ( 117.6247167782375840, 1.849990392679551343, 0.000000000000000000 ) ) ;
#18971=CARTESIAN_POINT ( 'NONE',  ( 117.1249999999999432, 1.767766952966320915, 1.767766952966431937 ) ) ;
#18977=CARTESIAN_POINT ( 'NONE',  ( 108.8511751345945981, -1.999999999999941602, -0.8284271247459952248 ) ) ;
#18979=CARTESIAN_POINT ( 'NONE',  ( 104.4372167782374419, 0.7662911109077987781, -1.849990392679231599 ) ) ;
#18981=( BOUNDED_CURVE ( )  B_SPLINE_CURVE ( 2, ( #9408, #9864, #21543, #11905, #28712, #7249, #18796, #5223, #16944 ),
 .UNSPECIFIED., .F., .F. ) 
 B_SPLINE_CURVE_WITH_KNOTS ( ( 3, 2, 2, 2, 3 ),
 ( 0.6764705882352941568, 0.6838235294117647189, 0.6911764705882352811, 0.6985294117647058432, 0.7058823529411765163 ),
 .UNSPECIFIED. ) 
 CURVE ( )  GEOMETRIC_REPRESENTATION_ITEM ( )  RATIONAL_B_SPLINE_CURVE ( ( 1.000000000000000000, 0.9238795325112867385, 1.000000000000000000, 0.9238795325112867385, 1.000000000000000000, 0.9238795325112867385, 1.000000000000000000, 0.9238795325112867385, 1.000000000000000000 ) ) 
 REPRESENTATION_ITEM ( '' )  );
#18982=CARTESIAN_POINT ( 'NONE',  ( 120.9377832217621034, -1.849990392679562001, -0.7662911109077087390 ) ) ;
#18999=CARTESIAN_POINT ( 'NONE',  ( 118.9997167782376266, -1.308140751793529510, 1.308140751793973600 ) ) ;
#19003=CARTESIAN_POINT ( 'NONE',  ( 115.0002832217621886, -1.308140751793585022, -1.308140751793640533 ) ) ;
#19025=CARTESIAN_POINT ( 'NONE',  ( 111.1249999999999289, 1.767766952966320915, 1.767766952966431937 ) ) ;
#19036=CARTESIAN_POINT ( 'NONE',  ( 111.2499999999999432, -1.110223024625156540E-13, 2.500000000000057732 ) ) ;
#19038=CARTESIAN_POINT ( 'NONE',  ( 106.1252832217622171, -5.551115123125782702E-14, -1.849990392679523588 ) ) ;
#19044=CARTESIAN_POINT ( 'NONE',  ( 106.8747167782375840, 2.775557561562891351E-14, 1.849990392679745632 ) ) ;
#19054=CARTESIAN_POINT ( 'NONE',  ( 107.0624999999998010, 2.500000000000114575, 1.035533905932989551 ) ) ;
#19061=CARTESIAN_POINT ( 'NONE',  ( 107.3127832217622313, 1.849990392679501827, -0.7662911109076485650 ) ) ;
#19088=ADVANCED_FACE ( 'NONE', ( #1419 ), #29831, .F. ) ;
#19095=CARTESIAN_POINT ( 'NONE',  ( 105.3749999999999005, -1.767766952966320915, 1.767766952966431937 ) ) ;
#19102=( BOUNDED_CURVE ( )  B_SPLINE_CURVE ( 2, ( #5332, #7496, #23951, #26385, #26234, #14743, #7789, #12602, #28671 ),
 .UNSPECIFIED., .F., .T. ) 
 B_SPLINE_CURVE_WITH_KNOTS ( ( 3, 2, 2, 2, 3 ),
 ( 0.5000000000000000000, 0.5073529411764705621, 0.5147058823529411242, 0.5220588235294116863, 0.5294117647058823595 ),
 .UNSPECIFIED. ) 
 CURVE ( )  GEOMETRIC_REPRESENTATION_ITEM ( )  RATIONAL_B_SPLINE_CURVE ( ( 1.000000000000000000, 0.9238795325112867385, 1.000000000000000000, 0.9238795325112867385, 1.000000000000000000, 0.9238795325112867385, 1.000000000000000000, 0.9238795325112867385, 1.000000000000000000 ) ) 
 REPRESENTATION_ITEM ( '' )  );
#19104=CARTESIAN_POINT ( 'NONE',  ( 116.1872167782374987, -1.849990392679532247, -0.7662911109077087390 ) ) ;
#19121=CARTESIAN_POINT ( 'NONE',  ( 116.9377832217621460, -1.849990392679441875, -0.7662911109077087390 ) ) ;
#19130=CARTESIAN_POINT ( 'NONE',  ( 104.9735375947738589, -0.8915860325701192579, -1.786451901258863995 ) ) ;
#19134=CARTESIAN_POINT ( 'NONE',  ( 115.2497167782374419, -1.308140751793557266, -1.308140751793751555 ) ) ;
#19138=CARTESIAN_POINT ( 'NONE',  ( 119.2886751345947260, 1.999999999999946265, 1.110223024625156540E-13 ) ) ;
#19139=VECTOR ( 'NONE', #10126, 1000.000000000000000 ) ;
#19140=CARTESIAN_POINT ( 'NONE',  ( 112.9377832217622171, -1.849990392679381701, -0.7662911109076485650 ) ) ;
#19141=AXIS2_PLACEMENT_3D ( 'NONE', #26337, #14559, #2990 ) ;
#19162=CARTESIAN_POINT ( 'NONE',  ( 111.8124999999997584, 1.035533905932779275, -2.499999999999964473 ) ) ;
#19170=CARTESIAN_POINT ( 'NONE',  ( 113.9999999999998153, 2.500000000000085265, 0.000000000000000000 ) ) ;
#19177=CARTESIAN_POINT ( 'NONE',  ( 106.0622167782373708, -1.849990392679441875, 0.7662911109080090544 ) ) ;
#19188=CARTESIAN_POINT ( 'NONE',  ( 113.7738248654049471, 2.000000000000061728, 0.8284271247462955401 ) ) ;
#19190=CARTESIAN_POINT ( 'NONE',  ( 108.0624999999998010, 2.500000000000114575, 1.035533905932929599 ) ) ;
#19195=CARTESIAN_POINT ( 'NONE',  ( 109.3127832217620607, 1.849990392679591977, -0.7662911109076485650 ) ) ;
#19207=ORIENTED_EDGE ( 'NONE', *, *, #16202, .F. ) ;
#19208=CARTESIAN_POINT ( 'NONE',  ( 118.7113248654050750, 1.999999999999946265, 1.110223024625156540E-13 ) ) ;
#19212=CARTESIAN_POINT ( 'NONE',  ( 110.2497167782375698, -1.308140751793585022, -1.308140751793529510 ) ) ;
#19218=VERTEX_POINT ( 'NONE', #27060 ) ;
#19221=VECTOR ( 'NONE', #13215, 1000.000000000000000 ) ;
#19226=VECTOR ( 'NONE', #8478, 1000.000000000000000 ) ;
#19231=CARTESIAN_POINT ( 'NONE',  ( 117.7886751345947545, -1.999999999999946265, 1.110223024625156540E-13 ) ) ;
#19239=CARTESIAN_POINT ( 'NONE',  ( 107.9374999999997726, 2.500000000000144773, -1.035533905932508825 ) ) ;
#19249=CARTESIAN_POINT ( 'NONE',  ( 118.6872167782374703, 1.849990392679501827, 0.7662911109080090544 ) ) ;
#19256=CARTESIAN_POINT ( 'NONE',  ( 116.8749999999998863, 1.767766952966320915, -1.767766952966320915 ) ) ;
#19270=CARTESIAN_POINT ( 'NONE',  ( 107.6872167782374561, 1.849990392679562001, 0.7662911109080090544 ) ) ;
#19273=CARTESIAN_POINT ( 'NONE',  ( 114.5002832217623023, 1.308140751793696044, 1.308140751793640533 ) ) ;
#19274=( BOUNDED_CURVE ( )  B_SPLINE_CURVE ( 2, ( #17976, #4105, #1805, #15841, #11210, #6406, #10593, #1657, #26989 ),
 .UNSPECIFIED., .F., .T. ) 
 B_SPLINE_CURVE_WITH_KNOTS ( ( 3, 2, 2, 2, 3 ),
 ( 0.7352941176470588758, 0.7426470588235294379, 0.7500000000000000000, 0.7573529411764705621, 0.7647058823529411242 ),
 .UNSPECIFIED. ) 
 CURVE ( )  GEOMETRIC_REPRESENTATION_ITEM ( )  RATIONAL_B_SPLINE_CURVE ( ( 1.000000000000000000, 0.9238795325112867385, 1.000000000000000000, 0.9238795325112867385, 1.000000000000000000, 0.9238795325112867385, 1.000000000000000000, 0.9238795325112867385, 1.000000000000000000 ) ) 
 REPRESENTATION_ITEM ( '' )  );
#19293=CARTESIAN_POINT ( 'NONE',  ( 104.9580272744090479, -0.1377225354489101661, 1.978757841790981686 ) ) ;
#19303=CARTESIAN_POINT ( 'NONE',  ( 104.8415063509460055, -1.908493649053821795, 1.110223024625156540E-13 ) ) ;
#19315=CARTESIAN_POINT ( 'NONE',  ( 115.5386751345946408, 1.387778780781445676E-13, 2.000000000000112799 ) ) ;
#19318=CARTESIAN_POINT ( 'NONE',  ( 109.3363248654050182, -1.414213562373034527, -1.414213562373034527 ) ) ;
#19321=CARTESIAN_POINT ( 'NONE',  ( 112.8749999999998437, 1.767766952966320915, -1.767766952966320915 ) ) ;
#19329=CARTESIAN_POINT ( 'NONE',  ( 104.8747167782376550, -2.775557561562891351E-14, 1.849990392679523588 ) ) ;
#19338=EDGE_LOOP ( 'NONE', ( #15959, #4945, #20698, #4068 ) ) ;
#19341=CARTESIAN_POINT ( 'NONE',  ( 107.3749999999999574, -1.767766952966293159, 1.767766952966431937 ) ) ;
#19349=CARTESIAN_POINT ( 'NONE',  ( 119.4374999999997868, -2.499999999999994671, 1.035533905932809473 ) ) ;
#19371=ORIENTED_EDGE ( 'NONE', *, *, #16274, .F. ) ;
#19386=EDGE_CURVE ( 'NONE', #30081, #10990, #9866, .T. ) ;
#19389=CARTESIAN_POINT ( 'NONE',  ( 106.9374999999998010, 2.500000000000054623, -1.035533905932568999 ) ) ;
#19392=CARTESIAN_POINT ( 'NONE',  ( 108.3988248654050324, -0.8284271247460250898, -1.999999999999851674 ) ) ;
#19393=CARTESIAN_POINT ( 'NONE',  ( 104.7401757384974275, 1.755445637970139305, -0.5961972863698411507 ) ) ;
#19394=ORIENTED_EDGE ( 'NONE', *, *, #16912, .T. ) ;
#19397=CARTESIAN_POINT ( 'NONE',  ( 108.2261751345945129, 2.000000000000061728, -0.8284271247460553989 ) ) ;
#19401=CARTESIAN_POINT ( 'NONE',  ( 117.0622167782374561, -1.849990392679472073, 0.7662911109078888172 ) ) ;
#19405=CARTESIAN_POINT ( 'NONE',  ( 117.4374999999997584, -2.499999999999844569, 1.035533905932929599 ) ) ;
#19423=CARTESIAN_POINT ( 'NONE',  ( 115.0627832217623592, -0.7662911109076785410, -1.849990392679171425 ) ) ;
#19432=EDGE_CURVE ( 'NONE', #13422, #15655, #8861, .T. ) ;
#19440=CARTESIAN_POINT ( 'NONE',  ( 114.6872167782375982, 1.849990392679621953, 0.7662911109080090544 ) ) ;
#19448=( BOUNDED_CURVE ( )  B_SPLINE_CURVE ( 2, ( #8785, #13574, #6619, #16040, #13731, #14041, #14190, #18778, #163 ),
 .UNSPECIFIED., .F., .T. ) 
 B_SPLINE_CURVE_WITH_KNOTS ( ( 3, 2, 2, 2, 3 ),
 ( 0.4117647058823529216, 0.4191176470588235392, 0.4264705882352941013, 0.4338235294117647189, 0.4411764705882352811 ),
 .UNSPECIFIED. ) 
 CURVE ( )  GEOMETRIC_REPRESENTATION_ITEM ( )  RATIONAL_B_SPLINE_CURVE ( ( 1.000000000000000000, 0.9238795325112867385, 1.000000000000000000, 0.9238795325112867385, 1.000000000000000000, 0.9238795325112867385, 1.000000000000000000, 0.9238795325112867385, 1.000000000000000000 ) ) 
 REPRESENTATION_ITEM ( '' )  );
#19449=ORIENTED_EDGE ( 'NONE', *, *, #8508, .T. ) ;
#19460=CARTESIAN_POINT ( 'NONE',  ( 117.2886751345947971, 2.000000000000140332, 2.220446049250313081E-13 ) ) ;
#19462=CARTESIAN_POINT ( 'NONE',  ( 115.7886751345947118, -1.999999999999974021, 0.000000000000000000 ) ) ;
#19468=CARTESIAN_POINT ( 'NONE',  ( 108.6249999999999289, -1.767766952966320915, -1.767766952966320915 ) ) ;
#19472=ORIENTED_EDGE ( 'NONE', *, *, #20556, .T. ) ;
#19475=CARTESIAN_POINT ( 'NONE',  ( 119.1252832217622597, -5.551115123125782702E-14, -1.849990392679412565 ) ) ;
#19485=CARTESIAN_POINT ( 'NONE',  ( 105.0624999999998437, 2.500000000000055067, 1.035533905932869425 ) ) ;
#19495=CARTESIAN_POINT ( 'NONE',  ( 118.4999999999998437, -2.499999999999919176, 0.000000000000000000 ) ) ;
#19507=CARTESIAN_POINT ( 'NONE',  ( 119.8124999999998863, 1.035533905932839449, -2.499999999999844569 ) ) ;
#19533=DIRECTION ( 'NONE',  ( -1.000000000000000000, -1.665334536937736783E-16, -2.220446049250315546E-16 ) ) ;
#19535=CARTESIAN_POINT ( 'NONE',  ( 107.8749999999999858, 1.767766952966431937, -1.767766952966209892 ) ) ;
#19536=CARTESIAN_POINT ( 'NONE',  ( 107.3363248654051887, -1.414213562373034527, -1.414213562373034527 ) ) ;
#19546=CARTESIAN_POINT ( 'NONE',  ( 118.4372167782374135, 0.7662911109079189043, -1.849990392679291551 ) ) ;
#19548=CARTESIAN_POINT ( 'NONE',  ( 118.7886751345946692, -1.999999999999918510, 2.220446049250313081E-13 ) ) ;
#19551=CARTESIAN_POINT ( 'NONE',  ( 113.7499999999997584, 0.000000000000000000, -2.500000000000057732 ) ) ;
#19579=CARTESIAN_POINT ( 'NONE',  ( 114.8122167782375698, 0.7662911109077388261, 1.849990392679591977 ) ) ;
#19613=CARTESIAN_POINT ( 'NONE',  ( 110.1636751345947260, 1.414213562373201061, -1.414213562372812483 ) ) ;
#19614=CARTESIAN_POINT ( 'NONE',  ( 104.9372167782373566, -0.7662911109077388261, 1.849990392679772278 ) ) ;
#19622=EDGE_CURVE ( 'NONE', #18908, #10100, #17362, .T. ) ;
#19635=CARTESIAN_POINT ( 'NONE',  ( 116.1011751345945555, 0.8284271247463257382, -1.999999999999791278 ) ) ;
#19639=CARTESIAN_POINT ( 'NONE',  ( 120.4999999999998437, -2.499999999999891198, 3.330669073875469621E-13 ) ) ;
#19646=CARTESIAN_POINT ( 'NONE',  ( -1.110223024625164676E-16, 2.000000000000012879, 2.021286199229734960E-15 ) ) ;
#19678=CARTESIAN_POINT ( 'NONE',  ( 105.6249999999999005, -1.767766952966376426, -1.767766952966320915 ) ) ;
#19686=LINE ( 'NONE', #29175, #17545 ) ;
#19689=CARTESIAN_POINT ( 'NONE',  ( 108.7261751345945555, -1.999999999999941602, 0.8284271247463557142 ) ) ;
#19691=CARTESIAN_POINT ( 'NONE',  ( 114.8122167782375698, 0.7662911109077388261, 1.849990392679591977 ) ) ;
#19696=CARTESIAN_POINT ( 'NONE',  ( 114.1250000000000142, 1.767766952966293159, 1.767766952966320915 ) ) ;
#19698=DIRECTION ( 'NONE',  ( -1.000000000000000000, -1.665334536937736783E-16, -2.220446049250315546E-16 ) ) ;
#19709=( BOUNDED_CURVE ( )  B_SPLINE_CURVE ( 2, ( #12071, #11928, #15963, #2797, #25261, #4946, #28587, #2368, #5248 ),
 .UNSPECIFIED., .F., .T. ) 
 B_SPLINE_CURVE_WITH_KNOTS ( ( 3, 2, 2, 2, 3 ),
 ( 0.2941176470588235392, 0.3014705882352941013, 0.3088235294117647189, 0.3161764705882352811, 0.3235294117647058987 ),
 .UNSPECIFIED. ) 
 CURVE ( )  GEOMETRIC_REPRESENTATION_ITEM ( )  RATIONAL_B_SPLINE_CURVE ( ( 1.000000000000000000, 0.9238795325112867385, 1.000000000000000000, 0.9238795325112867385, 1.000000000000000000, 0.9238795325112867385, 1.000000000000000000, 0.9238795325112867385, 1.000000000000000000 ) ) 
 REPRESENTATION_ITEM ( '' )  );
#19725=CARTESIAN_POINT ( 'NONE',  ( 119.9999999999997868, 1.387778780781445676E-13, 1.110223024625156540E-13 ) ) ;
#19734=CARTESIAN_POINT ( 'NONE',  ( 106.6488248654051318, 2.000000000000122125, -0.8284271247459350507 ) ) ;
#19737=FILL_AREA_STYLE ('',( #10535 ) ) ;
#19760=CARTESIAN_POINT ( 'NONE',  ( 120.8127832217621318, -1.849990392679411677, 0.7662911109079489913 ) ) ;
#19769=CARTESIAN_POINT ( 'NONE',  ( 106.1249999999999858, 1.767766952966320915, 1.767766952966431937 ) ) ;
#19777=CARTESIAN_POINT ( 'NONE',  ( 105.5627832217622597, 0.7662911109077686911, 1.849990392679772278 ) ) ;
#19788=VERTEX_POINT ( 'NONE', #30060 ) ;
#19790=CARTESIAN_POINT ( 'NONE',  ( 119.3749999999998863, -1.767766952966209892, 1.767766952966542959 ) ) ;
#19801=ORIENTED_EDGE ( 'NONE', *, *, #23425, .T. ) ;
#19833=CARTESIAN_POINT ( 'NONE',  ( 112.1872167782374135, -1.849990392679411677, -0.7662911109075883909 ) ) ;
#19838=CARTESIAN_POINT ( 'NONE',  ( 115.4999999999998153, -2.499999999999891198, 0.000000000000000000 ) ) ;
#19851=DIRECTION ( 'NONE',  ( 5.551115123125783935E-17, -1.000000000000000000, -8.881784197001254296E-16 ) ) ;
#19869=CARTESIAN_POINT ( 'NONE',  ( 111.1247167782376124, -1.849990392679579099, 1.110223024625156540E-13 ) ) ;
#19886=CARTESIAN_POINT ( 'NONE',  ( 106.5238248654050039, 0.8284271247463855792, -1.999999999999791278 ) ) ;
#19912=CARTESIAN_POINT ( 'NONE',  ( 120.7502832217623308, -1.308140751793640533, 1.308140751793751555 ) ) ;
#19913=DIRECTION ( 'NONE',  ( -1.000000000000000000, -1.665334536937736783E-16, -2.220446049250315546E-16 ) ) ;
#19914=VERTEX_POINT ( 'NONE', #23914 ) ;
#19923=CARTESIAN_POINT ( 'NONE',  ( 105.4999999999999147, -2.499999999999919176, 1.110223024625156540E-13 ) ) ;
#19932=CARTESIAN_POINT ( 'NONE',  ( 119.5624999999998153, -2.499999999999874767, -1.035533905932629173 ) ) ;
#19943=CARTESIAN_POINT ( 'NONE',  ( 118.8749999999998295, 1.767766952966320915, -1.767766952966320915 ) ) ;
#19945=CARTESIAN_POINT ( 'NONE',  ( 112.1252832217621460, -5.551115123125782702E-14, -1.849990392679523588 ) ) ;
#19949=CARTESIAN_POINT ( 'NONE',  ( 109.7497167782375698, 1.308140751793640533, 1.308140751793862577 ) ) ;
#19953=CARTESIAN_POINT ( 'NONE',  ( 107.0863248654050466, -1.414213562373034527, 1.414213562373145550 ) ) ;
#19965=EDGE_CURVE ( 'NONE', #16147, #7342, #29652, .T. ) ;
#19968=CARTESIAN_POINT ( 'NONE',  ( 116.0002832217622171, -1.308140751793585022, -1.308140751793640533 ) ) ;
#19984=CARTESIAN_POINT ( 'NONE',  ( 112.3511751345946976, 2.000000000000061728, 0.8284271247465359034 ) ) ;
#19987=CARTESIAN_POINT ( 'NONE',  ( 115.2497167782374419, -1.308140751793557266, -1.308140751793751555 ) ) ;
#19992=CARTESIAN_POINT ( 'NONE',  ( 115.3124999999998863, -1.035533905932659149, 2.500000000000205169 ) ) ;
#20001=EDGE_CURVE ( 'NONE', #15734, #2721, #29836, .T. ) ;
#20011=CARTESIAN_POINT ( 'NONE',  ( 105.5386751345947971, -1.110223024625156540E-13, 2.000000000000001776 ) ) ;
#20022=CARTESIAN_POINT ( 'NONE',  ( 109.3750000000000142, -1.767766952966320915, 1.767766952966431937 ) ) ;
#20027=CARTESIAN_POINT ( 'NONE',  ( 110.6247167782374987, 1.849990392679551343, 0.000000000000000000 ) ) ;
#20031=EDGE_LOOP ( 'NONE', ( #3186, #29463, #20725, #12621, #27570, #20681, #10520, #20269, #21395, #6383, #11960, #22412, #4118, #2121, #5163, #12582, #24209, #12895, #24275, #16676, #5396, #5020, #13411, #15550, #10684, #23231, #10733, #16896, #4841, #8895, #925, #12221, #3164, #24392, #14225 ) ) ;
#20033=EDGE_CURVE ( 'NONE', #6908, #23930, #8208, .T. ) ;
#20037=VERTEX_POINT ( 'NONE', #6071 ) ;
#20068=CARTESIAN_POINT ( 'NONE',  ( 109.9761751345946124, -0.8284271247461153509, -1.999999999999731104 ) ) ;
#20077=DIRECTION ( 'NONE',  ( -1.000000000000000000, -1.665334536937736783E-16, -2.220446049250315546E-16 ) ) ;
#20081=CARTESIAN_POINT ( 'NONE',  ( 104.4999999999998863, -2.499999999999919176, 0.000000000000000000 ) ) ;
#20090=CARTESIAN_POINT ( 'NONE',  ( 117.5624999999997584, -2.499999999999904521, -1.035533905932508825 ) ) ;
#20102=CARTESIAN_POINT ( 'NONE',  ( 120.9374999999996874, 2.500000000000114575, -1.035533905932629173 ) ) ;
#20103=CARTESIAN_POINT ( 'NONE',  ( 111.1877832217622029, 0.7662911109078588412, -1.849990392679411677 ) ) ;
#20111=CARTESIAN_POINT ( 'NONE',  ( 116.2113248654050750, -2.000000000000029310, 0.000000000000000000 ) ) ;
#20126=CARTESIAN_POINT ( 'NONE',  ( 107.6011751345946550, -0.8284271247461753029, 2.000000000000271783 ) ) ;
#20132=CARTESIAN_POINT ( 'NONE',  ( 114.4377832217621318, 1.849990392679562001, 0.7662911109079489913 ) ) ;
#20138=CARTESIAN_POINT ( 'NONE',  ( 107.2113248654050608, -1.999999999999946265, 0.000000000000000000 ) ) ;
#20150=CARTESIAN_POINT ( 'NONE',  ( 114.6247167782376124, 1.849990392679523588, 0.000000000000000000 ) ) ;
#20156=CARTESIAN_POINT ( 'NONE',  ( 115.0624999999998153, 2.499999999999994671, 1.035533905932929599 ) ) ;
#20178=VERTEX_POINT ( 'NONE', #18230 ) ;
#20186=CARTESIAN_POINT ( 'NONE',  ( 108.8749999999999574, 1.767766952966265404, -1.767766952966320915 ) ) ;
#20192=ADVANCED_FACE ( 'NONE', ( #6683 ), #20674, .F. ) ;
#20208=CARTESIAN_POINT ( 'NONE',  ( 106.7113248654050324, 2.000000000000001776, 1.110223024625156540E-13 ) ) ;
#20225=CARTESIAN_POINT ( 'NONE',  ( 114.5238248654049755, 0.8284271247463257382, -1.999999999999791278 ) ) ;
#20227=CARTESIAN_POINT ( 'NONE',  ( 111.8988248654051034, 0.8284271247462654530, 2.000000000000151879 ) ) ;
#20235=CARTESIAN_POINT ( 'NONE',  ( 116.6877832217621460, -0.7662911109077388261, 1.849990392679712103 ) ) ;
#20250=CARTESIAN_POINT ( 'NONE',  ( 117.1249999999999432, 1.767766952966320915, 1.767766952966431937 ) ) ;
#20262=CARTESIAN_POINT ( 'NONE',  ( 115.5624999999999005, -2.499999999999934719, -1.035533905932568777 ) ) ;
#20263=CARTESIAN_POINT ( 'NONE',  ( 109.0627832217621176, -0.7662911109076785410, -1.849990392679171425 ) ) ;
#20269=ORIENTED_EDGE ( 'NONE', *, *, #1937, .T. ) ;
#20271=VERTEX_POINT ( 'NONE', #18536 ) ;
#20289=CARTESIAN_POINT ( 'NONE',  ( 119.9999999999998153, -0.3289648646987480274, -2.003997983315188858 ) ) ;
#20302=CARTESIAN_POINT ( 'NONE',  ( 115.5622167782373850, 1.849990392679532247, -0.7662911109075883909 ) ) ;
#20307=CARTESIAN_POINT ( 'NONE',  ( 104.7401757384974417, 1.839718259470002781, 0.2240791434755549649 ) ) ;
#20321=LINE ( 'NONE', #22317, #29961 ) ;
#20331=CARTESIAN_POINT ( 'NONE',  ( 107.4999999999999716, -2.499999999999891198, 3.330669073875469621E-13 ) ) ;
#20347=CARTESIAN_POINT ( 'NONE',  ( 105.1636751345947260, 1.414213562373145550, -1.414213562373034527 ) ) ;
#20351=CARTESIAN_POINT ( 'NONE',  ( 121.3127832217621034, 1.849990392679682127, -0.7662911109075883909 ) ) ;
#20352=EDGE_CURVE ( 'NONE', #15916, #10146, #7919, .T. ) ;
#20370=DIRECTION ( 'NONE',  ( -1.000000000000000000, -1.665334536937736783E-16, -2.220446049250315546E-16 ) ) ;
#20371=CARTESIAN_POINT ( 'NONE',  ( 117.3127832217621318, 1.849990392679532247, -0.7662911109076485650 ) ) ;
#20387=CARTESIAN_POINT ( 'NONE',  ( 116.4999999999999574, -2.499999999999891198, 0.000000000000000000 ) ) ;
#20396=CARTESIAN_POINT ( 'NONE',  ( 118.8124999999998579, 1.035533905932749299, -2.499999999999784173 ) ) ;
#20398=CARTESIAN_POINT ( 'NONE',  ( 110.3127832217620323, 1.849990392679501827, -0.7662911109075883909 ) ) ;
#20401=CARTESIAN_POINT ( 'NONE',  ( 108.6247167782375271, 1.849990392679551343, 0.000000000000000000 ) ) ;
#20409=EDGE_CURVE ( 'NONE', #4583, #30412, #8672, .T. ) ;
#20443=CARTESIAN_POINT ( 'NONE',  ( 110.8747167782375556, 0.000000000000000000, 1.849990392679523588 ) ) ;
#20451=CARTESIAN_POINT ( 'NONE',  ( 105.7886751345946550, -1.999999999999946265, 0.000000000000000000 ) ) ;
#20477=CARTESIAN_POINT ( 'NONE',  ( 105.8749999999999574, 1.767766952966320915, -1.767766952966320915 ) ) ;
#20485=DIRECTION ( 'NONE',  ( -1.000000000000000000, -1.665334536937736783E-16, -2.220446049250315546E-16 ) ) ;
#20502=VECTOR ( 'NONE', #26994, 1000.000000000000000 ) ;
#20512=CARTESIAN_POINT ( 'NONE',  ( 104.8677751940535785, -1.887434372084343837, -0.4305587433837875788 ) ) ;
#20525=CARTESIAN_POINT ( 'NONE',  ( 117.8127832217621744, -1.849990392679501827, 0.7662911109078287542 ) ) ;
#20545=CARTESIAN_POINT ( 'NONE',  ( 115.3749999999999574, -1.767766952966320915, 1.767766952966431937 ) ) ;
#20555=CARTESIAN_POINT ( 'NONE',  ( 118.3749999999999147, -1.767766952966293159, 1.767766952966431937 ) ) ;
#20556=EDGE_CURVE ( 'NONE', #2147, #22177, #19274, .T. ) ;
#20557=CARTESIAN_POINT ( 'NONE',  ( 110.1252832217622029, -1.665334536937734811E-13, -1.849990392679412565 ) ) ;
#20561=CARTESIAN_POINT ( 'NONE',  ( 108.4372167782374419, 0.7662911109078588412, -1.849990392679231599 ) ) ;
#20563=ORIENTED_EDGE ( 'NONE', *, *, #30402, .T. ) ;
#20586=CARTESIAN_POINT ( 'NONE',  ( 111.5002832217621602, 1.308140751793723799, 1.308140751793640533 ) ) ;
#20594=CARTESIAN_POINT ( 'NONE',  ( 114.5386751345947403, -2.775557561562891351E-14, 2.000000000000112799 ) ) ;
#20595=ORIENTED_EDGE ( 'NONE', *, *, #2118, .F. ) ;
#20604=CARTESIAN_POINT ( 'NONE',  ( 109.8122167782375840, 0.7662911109078588412, 1.849990392679772278 ) ) ;
#20606=CARTESIAN_POINT ( 'NONE',  ( 111.8747167782376408, 0.000000000000000000, 1.849990392679523588 ) ) ;
#20628=CARTESIAN_POINT ( 'NONE',  ( 112.0386751345946834, 5.551115123125782702E-14, -1.999999999999890754 ) ) ;
#20633=CARTESIAN_POINT ( 'NONE',  ( 109.9374999999996874, 2.500000000000115019, -1.035533905932448873 ) ) ;
#20636=( LENGTH_UNIT ( ) NAMED_UNIT ( * ) SI_UNIT ( .MILLI., .METRE. ) );
#20646=CARTESIAN_POINT ( 'NONE',  ( 105.3749999999999005, -1.767766952966320915, 1.767766952966431937 ) ) ;
#20662=CARTESIAN_POINT ( 'NONE',  ( 121.1252832217622597, -5.551115123125782702E-14, -1.849990392679523588 ) ) ;
#20674=CYLINDRICAL_SURFACE ( 'NONE', #15506, 2.000000000000012879 ) ;
#20677=CYLINDRICAL_SURFACE ( 'NONE', #18765, 2.000000000000012879 ) ;
#20679=CARTESIAN_POINT ( 'NONE',  ( 116.2497167782374845, -1.308140751793585022, -1.308140751793640533 ) ) ;
#20680=LINE ( 'NONE', #9003, #29690 ) ;
#20681=ORIENTED_EDGE ( 'NONE', *, *, #19965, .T. ) ;
#20684=CARTESIAN_POINT ( 'NONE',  ( 117.8752832217622881, -1.849990392679551343, 0.000000000000000000 ) ) ;
#20692=ORIENTED_EDGE ( 'NONE', *, *, #20001, .F. ) ;
#20698=ORIENTED_EDGE ( 'NONE', *, *, #28989, .F. ) ;
#20700=CARTESIAN_POINT ( 'NONE',  ( 0.000000000000000000, 0.000000000000000000, 0.000000000000000000 ) ) ;
#20705=CARTESIAN_POINT ( 'NONE',  ( 114.2499999999999147, -1.110223024625156540E-13, 2.500000000000057732 ) ) ;
#20715=CARTESIAN_POINT ( 'NONE',  ( 117.8124999999998579, 1.035533905932869425, -2.499999999999784173 ) ) ;
#20717=FACE_OUTER_BOUND ( 'NONE', #21484, .T. ) ;
#20719=CARTESIAN_POINT ( 'NONE',  ( 109.7738248654049471, 2.000000000000031530, 0.8284271247464157772 ) ) ;
#20720=CARTESIAN_POINT ( 'NONE',  ( 107.8747167782375840, 0.000000000000000000, 1.849990392679523588 ) ) ;
#20725=ORIENTED_EDGE ( 'NONE', *, *, #9746, .T. ) ;
#20737=ORIENTED_EDGE ( 'NONE', *, *, #28582, .T. ) ;
#20740=CARTESIAN_POINT ( 'NONE',  ( 0.000000000000000000, 0.000000000000000000, 0.000000000000000000 ) ) ;
#20741=CARTESIAN_POINT ( 'NONE',  ( 109.4136751345946976, 1.414213562373090038, 1.414213562373034527 ) ) ;
#20744=CARTESIAN_POINT ( 'NONE',  ( 112.0002832217622739, -1.308140751793557266, -1.308140751793640533 ) ) ;
#20753=ADVANCED_FACE ( 'NONE', ( #20717 ), #21177, .F. ) ;
#20760=CARTESIAN_POINT ( 'NONE',  ( 116.2886751345946124, 2.000000000000168310, 3.330669073875469621E-13 ) ) ;
#20763=CARTESIAN_POINT ( 'NONE',  ( 111.4997167782375413, 1.308140751793696044, -1.308140751793640533 ) ) ;
#20765=CARTESIAN_POINT ( 'NONE',  ( 113.8747167782375556, 0.000000000000000000, 1.849990392679523588 ) ) ;
#20788=CARTESIAN_POINT ( 'NONE',  ( 108.9999999999998579, 2.500000000000030198, 1.110223024625156540E-13 ) ) ;
#20790=EDGE_CURVE ( 'NONE', #22257, #28223, #13828, .T. ) ;
#20801=CARTESIAN_POINT ( 'NONE',  ( 120.4997167782374703, 1.308140751793723799, -1.308140751793640533 ) ) ;
#20819=CARTESIAN_POINT ( 'NONE',  ( 120.3127832217622171, 1.849990392679591977, -0.7662911109075883909 ) ) ;
#20835=CARTESIAN_POINT ( 'NONE',  ( 119.1872167782375271, -1.849990392679562001, -0.7662911109077087390 ) ) ;
#20840=CARTESIAN_POINT ( 'NONE',  ( 113.8127832217621034, -1.849990392679441875, 0.7662911109079489913 ) ) ;
#20857=CARTESIAN_POINT ( 'NONE',  ( 113.8749999999998721, 1.767766952966431937, -1.767766952966209892 ) ) ;
#20867=CARTESIAN_POINT ( 'NONE',  ( 116.6249999999999716, -1.767766952966459693, -1.767766952966209892 ) ) ;
#20869=CARTESIAN_POINT ( 'NONE',  ( 105.4377832217621176, 1.849990392679562001, 0.7662911109078888172 ) ) ;
#20874=ORIENTED_EDGE ( 'NONE', *, *, #28855, .T. ) ;
#20898=CARTESIAN_POINT ( 'NONE',  ( 112.5002832217623023, 1.308140751793696044, 1.308140751793640533 ) ) ;
#20913=CARTESIAN_POINT ( 'NONE',  ( 108.1872167782373850, -1.849990392679472073, -0.7662911109077087390 ) ) ;
#20938=CARTESIAN_POINT ( 'NONE',  ( 108.5000000000000000, -2.500000000000002220, 2.220446049250313081E-13 ) ) ;
#20949=CARTESIAN_POINT ( 'NONE',  ( 120.2497167782375271, -1.308140751793529510, -1.308140751793640533 ) ) ;
#20969=CARTESIAN_POINT ( 'NONE',  ( 105.6872167782375413, 1.849990392679591977, 0.7662911109080692285 ) ) ;
#20972=CARTESIAN_POINT ( 'NONE',  ( 120.5627832217621460, 0.7662911109078287542, 1.849990392679652151 ) ) ;
#20993=CARTESIAN_POINT ( 'NONE',  ( 118.7497167782375982, 1.308140751793696044, 1.308140751793640533 ) ) ;
#20999=CARTESIAN_POINT ( 'NONE',  ( 115.8127832217621460, -1.849990392679472073, 0.7662911109078888172 ) ) ;
#21002=ORIENTED_EDGE ( 'NONE', *, *, #9259, .F. ) ;
#21014=CARTESIAN_POINT ( 'NONE',  ( 113.3124999999997300, -1.035533905932598975, 2.500000000000144773 ) ) ;
#21023=CARTESIAN_POINT ( 'NONE',  ( 114.4374999999998010, -2.499999999999964473, 1.035533905932929599 ) ) ;
#21026=CARTESIAN_POINT ( 'NONE',  ( 108.1877832217622881, 0.7662911109077388261, -1.849990392679291551 ) ) ;
#21032=CARTESIAN_POINT ( 'NONE',  ( 107.0622167782373708, -1.849990392679381701, 0.7662911109079489913 ) ) ;
#21034=CARTESIAN_POINT ( 'NONE',  ( 111.2113248654051176, -1.999999999999946265, 0.000000000000000000 ) ) ;
#21035=ORIENTED_EDGE ( 'NONE', *, *, #27893, .T. ) ;
#21045=CARTESIAN_POINT ( 'NONE',  ( 109.3750000000000142, -1.767766952966320915, 1.767766952966431937 ) ) ;
#21050=CARTESIAN_POINT ( 'NONE',  ( 108.6252832217621886, 5.551115123125782702E-14, 1.849990392679634610 ) ) ;
#21057=ORIENTED_EDGE ( 'NONE', *, *, #21744, .F. ) ;
#21064=CARTESIAN_POINT ( 'NONE',  ( 109.6872167782374561, 1.849990392679562001, 0.7662911109080090544 ) ) ;
#21082=CARTESIAN_POINT ( 'NONE',  ( 117.5238248654049897, 0.8284271247463557142, -1.999999999999791278 ) ) ;
#21091=CARTESIAN_POINT ( 'NONE',  ( 109.4999999999998579, -2.499999999999891198, 2.220446049250313081E-13 ) ) ;
#21103=CARTESIAN_POINT ( 'NONE',  ( 105.1249999999999005, 1.767766952966265404, 1.767766952966431937 ) ) ;
#21108=CARTESIAN_POINT ( 'NONE',  ( 119.3749999999998863, -1.767766952966209892, 1.767766952966542959 ) ) ;
#21117=CARTESIAN_POINT ( 'NONE',  ( 107.8122167782374135, 0.7662911109078888172, 1.849990392679712103 ) ) ;
#21120=CARTESIAN_POINT ( 'NONE',  ( 119.4377832217620607, 1.849990392679591977, 0.7662911109080692285 ) ) ;
#21139=CARTESIAN_POINT ( 'NONE',  ( 118.1872167782374845, -1.849990392679472073, -0.7662911109076485650 ) ) ;
#21143=CARTESIAN_POINT ( 'NONE',  ( 115.2502832217623592, 1.308140751793696044, -1.308140751793529510 ) ) ;
#21164=CARTESIAN_POINT ( 'NONE',  ( 112.6874999999997584, -1.035533905932659149, -2.499999999999603872 ) ) ;
#21173=CARTESIAN_POINT ( 'NONE',  ( 112.6874999999997584, -1.035533905932659149, -2.499999999999603872 ) ) ;
#21176=CARTESIAN_POINT ( 'NONE',  ( 105.8127832217621176, -1.849990392679501827, 0.7662911109077686911 ) ) ;
#21177=CYLINDRICAL_SURFACE ( 'NONE', #12544, 2.000000000000012879 ) ;
#21193=CARTESIAN_POINT ( 'NONE',  ( 110.2499999999998010, -5.551115123125782702E-14, 2.500000000000168754 ) ) ;
#21203=CARTESIAN_POINT ( 'NONE',  ( 109.8752832217622739, -1.849990392679468076, 1.110223024625156540E-13 ) ) ;
#21214=CARTESIAN_POINT ( 'NONE',  ( 110.2886751345946834, 2.000000000000085265, 1.110223024625156540E-13 ) ) ;
#21239=CARTESIAN_POINT ( 'NONE',  ( 110.4999999999999432, -2.499999999999891198, 3.330669073875469621E-13 ) ) ;
#21247=CARTESIAN_POINT ( 'NONE',  ( 117.9372167782374419, -0.7662911109077987781, 1.849990392679591977 ) ) ;
#21253=CARTESIAN_POINT ( 'NONE',  ( 119.3124999999998295, -1.035533905932689347, 2.500000000000265121 ) ) ;
#21265=CARTESIAN_POINT ( 'NONE',  ( 104.6872167782374277, 1.849990392679532247, 0.7662911109080692285 ) ) ;
#21267=CARTESIAN_POINT ( 'NONE',  ( 119.7502832217622455, -1.308140751793501755, 1.308140751793751555 ) ) ;
#21274=LINE ( 'NONE', #23733, #8744 ) ;
#21284=CARTESIAN_POINT ( 'NONE',  ( 116.7497167782375413, 1.308140751793585022, 1.308140751793751555 ) ) ;
#21288=CARTESIAN_POINT ( 'NONE',  ( 119.0386751345946976, 5.551115123125782702E-14, -1.999999999999890754 ) ) ;
#21289=CARTESIAN_POINT ( 'NONE',  ( 114.9377832217620750, -1.849990392679501827, -0.7662911109076485650 ) ) ;
#21304=( LENGTH_UNIT ( ) NAMED_UNIT ( * ) SI_UNIT ( .MILLI., .METRE. ) );
#21308=CARTESIAN_POINT ( 'NONE',  ( 112.3749999999999289, -1.767766952966320915, 1.767766952966431937 ) ) ;
#21311=CARTESIAN_POINT ( 'NONE',  ( 115.4136751345946976, 1.414213562373090038, 1.414213562373034527 ) ) ;
#21316=ORIENTED_EDGE ( 'NONE', *, *, #4417, .T. ) ;
#21319=CARTESIAN_POINT ( 'NONE',  ( 111.8749999999998437, 1.767766952966348670, -1.767766952966209892 ) ) ;
#21321=CARTESIAN_POINT ( 'NONE',  ( 104.9377832217622171, -1.849990392679411677, -0.7662911109076485650 ) ) ;
#21323=ORIENTED_EDGE ( 'NONE', *, *, #2899, .F. ) ;
#21326=CARTESIAN_POINT ( 'NONE',  ( 106.4372167782374419, 0.7662911109078588412, -1.849990392679231599 ) ) ;
#21327=EDGE_CURVE ( 'NONE', #19218, #30081, #20680, .T. ) ;
#21340=CARTESIAN_POINT ( 'NONE',  ( 107.3124999999996589, -1.035533905932598975, 2.500000000000205169 ) ) ;
#21346=CARTESIAN_POINT ( 'NONE',  ( 108.1877832217622881, 0.7662911109077388261, -1.849990392679291551 ) ) ;
#21373=CARTESIAN_POINT ( 'NONE',  ( 106.0386751345947118, 0.000000000000000000, -2.000000000000001776 ) ) ;
#21392=CARTESIAN_POINT ( 'NONE',  ( 106.3749999999999574, -1.767766952966320915, 1.767766952966431937 ) ) ;
#21395=ORIENTED_EDGE ( 'NONE', *, *, #20409, .T. ) ;
#21401=CARTESIAN_POINT ( 'NONE',  ( 116.4997167782376266, 1.308140751793640533, -1.308140751793640533 ) ) ;
#21407=CARTESIAN_POINT ( 'NONE',  ( 117.2499999999998721, 0.000000000000000000, 2.499999999999946709 ) ) ;
#21415=UNCERTAINTY_MEASURE_WITH_UNIT (LENGTH_MEASURE( 1.000000000000000082E-05 ), #21905, 'distance_accuracy_value', 'NONE');
#21417=CARTESIAN_POINT ( 'NONE',  ( 105.7497167782376266, 1.308140751793696044, 1.308140751793640533 ) ) ;
#21420=CARTESIAN_POINT ( 'NONE',  ( 116.4377832217621602, 1.849990392679621953, 0.7662911109081291805 ) ) ;
#21433=CARTESIAN_POINT ( 'NONE',  ( 108.4761751345945697, 0.8284271247462053900, 2.000000000000151879 ) ) ;
#21458=VECTOR ( 'NONE', #11413, 1000.000000000000000 ) ;
#21465=CARTESIAN_POINT ( 'NONE',  ( 111.9374999999997868, 2.500000000000114575, -1.035533905932508825 ) ) ;
#21474=CIRCLE ( 'NONE', #2784, 6.000000000000012434 ) ;
#21475=CARTESIAN_POINT ( 'NONE',  ( 112.2499999999998153, -5.551115123125782702E-14, 2.500000000000168754 ) ) ;
#21483=CARTESIAN_POINT ( 'NONE',  ( 106.4997167782374845, 1.308140751793640533, -1.308140751793418488 ) ) ;
#21484=EDGE_LOOP ( 'NONE', ( #28101, #13754, #18021, #29808 ) ) ;
#21492=ORIENTED_EDGE ( 'NONE', *, *, #8921, .T. ) ;
#21495=CARTESIAN_POINT ( 'NONE',  ( 110.3124999999998863, -1.035533905932659149, 2.500000000000144773 ) ) ;
#21503=CARTESIAN_POINT ( 'NONE',  ( 107.6877832217621744, -0.7662911109077987781, 1.849990392679652151 ) ) ;
#21540=LINE ( 'NONE', #14777, #14814 ) ;
#21543=CARTESIAN_POINT ( 'NONE',  ( 109.0863248654051034, -1.414213562373145550, 1.414213562373256572 ) ) ;
#21544=CARTESIAN_POINT ( 'NONE',  ( 105.7499999999998010, 1.110223024625156540E-13, -2.499999999999946709 ) ) ;
#21547=EDGE_LOOP ( 'NONE', ( #22763, #9991, #26377, #27232 ) ) ;
#21553=CARTESIAN_POINT ( 'NONE',  ( 115.7497167782375698, 1.308140751793751555, 1.308140751793973600 ) ) ;
#21558=CARTESIAN_POINT ( 'NONE',  ( 116.6874999999997726, -1.035533905932659149, -2.499999999999784173 ) ) ;
#21568=DIRECTION ( 'NONE',  ( 1.000000000000000000, 1.665334536937736783E-16, 2.220446049250315546E-16 ) ) ;
#21569=CARTESIAN_POINT ( 'NONE',  ( 106.3747167782374703, -5.551115123125782702E-14, -1.849990392679523588 ) ) ;
#21572=CARTESIAN_POINT ( 'NONE',  ( 113.4377832217621460, 1.849990392679591977, 0.7662911109080692285 ) ) ;
#21588=ORIENTED_EDGE ( 'NONE', *, *, #1725, .T. ) ;
#21597=EDGE_LOOP ( 'NONE', ( #15262, #29647, #7516, #6808, #15690 ) ) ;
#21606=CARTESIAN_POINT ( 'NONE',  ( 111.3363248654049755, -1.414213562373256572, -1.414213562372923505 ) ) ;
#21614=CARTESIAN_POINT ( 'NONE',  ( 104.8415063509460055, -1.908493649053821795, 1.110223024625156540E-13 ) ) ;
#21623=CARTESIAN_POINT ( 'NONE',  ( 114.1250000000000142, 1.767766952966293159, 1.767766952966320915 ) ) ;
#21624=CARTESIAN_POINT ( 'NONE',  ( 117.2886751345947971, 2.000000000000140332, 2.220446049250313081E-13 ) ) ;
#21625=LINE ( 'NONE', #998, #14629 ) ;
#21629=CARTESIAN_POINT ( 'NONE',  ( 119.1877832217621034, 0.7662911109078588412, -1.849990392679411677 ) ) ;
#21630=TOROIDAL_SURFACE ( 'NONE', #26986, 6.000000000000000000, 5.000000000000004441 ) ;
#21640=CARTESIAN_POINT ( 'NONE',  ( 108.1249999999999574, 1.767766952966293159, 1.767766952966431937 ) ) ;
#21646=CARTESIAN_POINT ( 'NONE',  ( 117.7886751345947545, -1.999999999999946265, 1.110223024625156540E-13 ) ) ;
#21648=CARTESIAN_POINT ( 'NONE',  ( 108.8752832217621744, -1.849990392679468076, 1.110223024625156540E-13 ) ) ;
#21652=CARTESIAN_POINT ( 'NONE',  ( 119.7261751345945413, -1.999999999999941602, 0.8284271247464759513 ) ) ;
#21671=ORIENTED_EDGE ( 'NONE', *, *, #12036, .F. ) ;
#21683=ORIENTED_EDGE ( 'NONE', *, *, #22928, .F. ) ;
#21689=DIRECTION ( 'NONE',  ( 0.8660254037844381525, -0.5000000000000008882, -2.220446049250315053E-16 ) ) ;
#21692=CARTESIAN_POINT ( 'NONE',  ( 107.3749999999999574, -1.767766952966293159, 1.767766952966431937 ) ) ;
#21695=CARTESIAN_POINT ( 'NONE',  ( 104.7401757384974275, 1.849990392679522477, -0.1213543097418731814 ) ) ;
#21703=CARTESIAN_POINT ( 'NONE',  ( 117.4997167782374987, 1.308140751793696044, -1.308140751793640533 ) ) ;
#21707=CARTESIAN_POINT ( 'NONE',  ( 117.6250000000000000, -1.767766952966376426, -1.767766952966320915 ) ) ;
#21723=CARTESIAN_POINT ( 'NONE',  ( 115.3127832217621886, 1.849990392679562001, -0.7662911109076485650 ) ) ;
#21744=EDGE_CURVE ( 'NONE', #20037, #29700, #10292, .T. ) ;
#21754=DIRECTION ( 'NONE',  ( -1.000000000000000000, -1.665334536937736783E-16, -2.220446049250315546E-16 ) ) ;
#21755=CARTESIAN_POINT ( 'NONE',  ( 111.2738248654049897, -1.999999999999881650, -0.8284271247459350507 ) ) ;
#21767=CARTESIAN_POINT ( 'NONE',  ( 109.8124999999997868, 1.035533905932779275, -2.499999999999784173 ) ) ;
#21773=CARTESIAN_POINT ( 'NONE',  ( 121.3127832217621034, 1.849990392679682127, -0.7662911109075883909 ) ) ;
#21774=CARTESIAN_POINT ( 'NONE',  ( 110.8988248654050182, 0.8284271247462654530, 2.000000000000271783 ) ) ;
#21780=ORIENTED_EDGE ( 'NONE', *, *, #16577, .T. ) ;
#21787=CARTESIAN_POINT ( 'NONE',  ( 106.3124999999997584, -1.035533905932659149, 2.500000000000205169 ) ) ;
#21794=CARTESIAN_POINT ( 'NONE',  ( 104.8752832217621602, -1.849990392679495832, 2.220446049250313081E-13 ) ) ;
#21797=CARTESIAN_POINT ( 'NONE',  ( 119.3511751345946550, 2.000000000000061728, 0.8284271247463557142 ) ) ;
#21800=DIRECTION ( 'NONE',  ( 5.551115123125785167E-17, -1.000000000000000000, -8.881784197001256268E-16 ) ) ;
#21806=CARTESIAN_POINT ( 'NONE',  ( 120.8124999999997726, 1.035533905932899401, -2.499999999999844569 ) ) ;
#21809=CARTESIAN_POINT ( 'NONE',  ( 111.6636751345947829, -1.414213562373090038, 1.414213562373034527 ) ) ;
#21823=PRESENTATION_STYLE_ASSIGNMENT (( #10453 ) ) ;
#21835=CARTESIAN_POINT ( 'NONE',  ( 105.8749999999999574, 1.767766952966320915, -1.767766952966320915 ) ) ;
#21844=CARTESIAN_POINT ( 'NONE',  ( 118.8747167782375840, 5.551115123125782702E-14, 1.849990392679523588 ) ) ;
#21845=CARTESIAN_POINT ( 'NONE',  ( 118.6636751345946550, -1.414213562373117794, 1.414213562373256572 ) ) ;
#21847=CONICAL_SURFACE ( 'NONE', #25770, 577.3502691896271699, 0.5235987755982998149 ) ;
#21851=CARTESIAN_POINT ( 'NONE',  ( 114.7499999999999147, -5.551115123125782702E-14, -2.499999999999946709 ) ) ;
#21861=( BOUNDED_CURVE ( )  B_SPLINE_CURVE ( 2, ( #1226, #7543, #16953, #14789, #23988, #17100, #24134, #26281, #14643 ),
 .UNSPECIFIED., .F., .T. ) 
 B_SPLINE_CURVE_WITH_KNOTS ( ( 3, 2, 2, 2, 3 ),
 ( 0.7647058823529411242, 0.7720588235294117974, 0.7794117647058823595, 0.7867647058823529216, 0.7941176470588234837 ),
 .UNSPECIFIED. ) 
 CURVE ( )  GEOMETRIC_REPRESENTATION_ITEM ( )  RATIONAL_B_SPLINE_CURVE ( ( 1.000000000000000000, 0.9238795325112867385, 1.000000000000000000, 0.9238795325112867385, 1.000000000000000000, 0.9238795325112867385, 1.000000000000000000, 0.9238795325112867385, 1.000000000000000000 ) ) 
 REPRESENTATION_ITEM ( '' )  );
#21863=CARTESIAN_POINT ( 'NONE',  ( 116.3988248654050039, -0.8284271247460852639, -1.999999999999911626 ) ) ;
#21865=CARTESIAN_POINT ( 'NONE',  ( 104.1247167782375556, -1.849990392679468076, 0.000000000000000000 ) ) ;
#21868=CARTESIAN_POINT ( 'NONE',  ( 114.1252832217622313, -8.326672684688674053E-14, -1.849990392679412565 ) ) ;
#21883=CARTESIAN_POINT ( 'NONE',  ( 0.000000000000000000, 0.000000000000000000, 0.000000000000000000 ) ) ;
#21885=EDGE_CURVE ( 'NONE', #29510, #17448, #21861, .T. ) ;
#21889=CARTESIAN_POINT ( 'NONE',  ( 104.8513327624231408, 0.7142157997211321385, 1.784475575595019459 ) ) ;
#21901=CARTESIAN_POINT ( 'NONE',  ( 119.9999999999998437, 2.090674230939232547, 1.116850201264615761 ) ) ;
#21905=( LENGTH_UNIT ( ) NAMED_UNIT ( * ) SI_UNIT ( .MILLI., .METRE. ) );
#21915=CARTESIAN_POINT ( 'NONE',  ( 106.9136751345946692, -1.414213562373034527, -1.414213562372812483 ) ) ;
#21916=CARTESIAN_POINT ( 'NONE',  ( 108.0624999999998010, 2.500000000000114575, 1.035533905932929599 ) ) ;
#21920=VERTEX_POINT ( 'NONE', #7026 ) ;
#21924=CARTESIAN_POINT ( 'NONE',  ( 119.0002832217622455, -1.308140751793585022, -1.308140751793529510 ) ) ;
#21932=CARTESIAN_POINT ( 'NONE',  ( 106.1874999999999289, 1.035533905932839449, 2.500000000000265121 ) ) ;
#21941=CARTESIAN_POINT ( 'NONE',  ( 105.8127832217621176, -1.849990392679501827, 0.7662911109077686911 ) ) ;
#21954=CARTESIAN_POINT ( 'NONE',  ( 120.0624999999998721, 2.500000000000114575, 1.035533905932869425 ) ) ;
#21968=( NAMED_UNIT ( * ) PLANE_ANGLE_UNIT ( ) SI_UNIT ( $, .RADIAN. ) );
#21981=CARTESIAN_POINT ( 'NONE',  ( 105.9374999999997584, 2.500000000000144773, -1.035533905932568999 ) ) ;
#21990=CARTESIAN_POINT ( 'NONE',  ( 112.5386751345946550, 8.326672684688674053E-14, 2.000000000000001776 ) ) ;
#21991=ORIENTED_EDGE ( 'NONE', *, *, #18192, .F. ) ;
#21992=CARTESIAN_POINT ( 'NONE',  ( 112.9997167782376835, -1.308140751793557266, 1.308140751793751555 ) ) ;
#21996=CARTESIAN_POINT ( 'NONE',  ( 112.7499999999998579, -5.551115123125782702E-14, -2.499999999999946709 ) ) ;
#22006=CARTESIAN_POINT ( 'NONE',  ( 1.110223024625164183E-16, -2.000000000000012879, -1.776356839400262692E-15 ) ) ;
#22025=CARTESIAN_POINT ( 'NONE',  ( 115.2113248654050750, -1.999999999999918510, 1.110223024625156540E-13 ) ) ;
#22026=CARTESIAN_POINT ( 'NONE',  ( 114.4372167782375271, 0.7662911109078588412, -1.849990392679351725 ) ) ;
#22042=CARTESIAN_POINT ( 'NONE',  ( 119.9999999999999289, 2.500000000000057732, 1.110223024625156540E-13 ) ) ;
#22051=CARTESIAN_POINT ( 'NONE',  ( 118.1488248654049613, -1.999999999999941602, 0.8284271247462955401 ) ) ;
#22071=CARTESIAN_POINT ( 'NONE',  ( 104.6247167782375271, 1.849990392679523588, 0.000000000000000000 ) ) ;
#22092=CARTESIAN_POINT ( 'NONE',  ( 118.6249999999998010, -1.767766952966431937, -1.767766952966209892 ) ) ;
#22106=CARTESIAN_POINT ( 'NONE',  ( 119.4999999999999289, -2.499999999999919176, 0.000000000000000000 ) ) ;
#22109=ORIENTED_EDGE ( 'NONE', *, *, #5445, .F. ) ;
#22122=( LENGTH_UNIT ( ) NAMED_UNIT ( * ) SI_UNIT ( .MILLI., .METRE. ) );
#22138=ORIENTED_EDGE ( 'NONE', *, *, #23072, .F. ) ;
#22142=CARTESIAN_POINT ( 'NONE',  ( 112.7261751345945413, -1.999999999999941602, 0.8284271247465359034 ) ) ;
#22143=VERTEX_POINT ( 'NONE', #21624 ) ;
#22144=CARTESIAN_POINT ( 'NONE',  ( 112.7497167782374845, 1.308140751793779311, 1.308140751793973600 ) ) ;
#22151=CARTESIAN_POINT ( 'NONE',  ( 113.4374999999998721, -2.499999999999994671, 1.035533905932869425 ) ) ;
#22177=VERTEX_POINT ( 'NONE', #26204 ) ;
#22182=CARTESIAN_POINT ( 'NONE',  ( 114.9613248654051318, 1.665334536937734811E-13, 2.000000000000223821 ) ) ;
#22183=CARTESIAN_POINT ( 'NONE',  ( 113.4997167782376550, 1.308140751793640533, -1.308140751793640533 ) ) ;
#22184=ORIENTED_EDGE ( 'NONE', *, *, #2899, .T. ) ;
#22206=( NAMED_UNIT ( * ) SI_UNIT ( $, .STERADIAN. ) SOLID_ANGLE_UNIT ( ) );
#22222=CARTESIAN_POINT ( 'NONE',  ( 120.1252832217621176, -5.551115123125782702E-14, -1.849990392679523588 ) ) ;
#22232=CARTESIAN_POINT ( 'NONE',  ( 106.3749999999999574, -1.767766952966320915, 1.767766952966431937 ) ) ;
#22238=CARTESIAN_POINT ( 'NONE',  ( 110.0622167782374987, -1.849990392679441875, 0.7662911109079489913 ) ) ;
#22242=CARTESIAN_POINT ( 'NONE',  ( 104.9377832217622171, -1.849990392679411677, -0.7662911109076485650 ) ) ;
#22254=CARTESIAN_POINT ( 'NONE',  ( 119.1249999999999432, 1.767766952966348670, 1.767766952966431937 ) ) ;
#22255=EDGE_CURVE ( 'NONE', #4728, #22693, #26148, .T. ) ;
#22257=VERTEX_POINT ( 'NONE', #15644 ) ;
#22298=CARTESIAN_POINT ( 'NONE',  ( 114.5622167782375556, 1.849990392679682127, -0.7662911109076485650 ) ) ;
#22303=CARTESIAN_POINT ( 'NONE',  ( 113.8124999999998437, 1.035533905932749299, -2.499999999999904521 ) ) ;
#22317=CARTESIAN_POINT ( 'NONE',  ( -1.110223024625164676E-16, 2.000000000000012879, 2.021286199229734960E-15 ) ) ;
#22332=FACE_OUTER_BOUND ( 'NONE', #24707, .T. ) ;
#22335=CARTESIAN_POINT ( 'NONE',  ( 110.6872167782375840, 1.849990392679562001, 0.7662911109078287542 ) ) ;
#22339=EDGE_LOOP ( 'NONE', ( #25083, #15020, #21780, #18855 ) ) ;
#22370=CARTESIAN_POINT ( 'NONE',  ( 120.3122167782375413, -0.7662911109077686911, -1.849990392679411677 ) ) ;
#22380=FACE_OUTER_BOUND ( 'NONE', #16417, .T. ) ;
#22394=CARTESIAN_POINT ( 'NONE',  ( 119.6874999999998010, -1.035533905932809473, -2.499999999999784173 ) ) ;
#22409=CARTESIAN_POINT ( 'NONE',  ( 109.3127832217620607, 1.849990392679591977, -0.7662911109076485650 ) ) ;
#22412=ORIENTED_EDGE ( 'NONE', *, *, #12673, .T. ) ;
#22414=CARTESIAN_POINT ( 'NONE',  ( 108.6872167782374277, 1.849990392679591977, 0.7662911109078888172 ) ) ;
#22417=AXIS2_PLACEMENT_3D ( 'NONE', #22791, #24775, #10831 ) ;
#22430=CARTESIAN_POINT ( 'NONE',  ( 107.4761751345946550, 0.8284271247461753029, 2.000000000000212275 ) ) ;
#22437=DIRECTION ( 'NONE',  ( 0.000000000000000000, -1.000000000000000000, -8.881784197001262184E-16 ) ) ;
#22438=CARTESIAN_POINT ( 'NONE',  ( 115.5002832217623308, 1.308140751793640533, 1.308140751793640533 ) ) ;
#22447=ADVANCED_FACE ( 'NONE', ( #27866 ), #2244, .F. ) ;
#22451=DIRECTION ( 'NONE',  ( -1.000000000000000000, -1.665334536937736783E-16, -2.220446049250315546E-16 ) ) ;
#22452=CARTESIAN_POINT ( 'NONE',  ( 104.7401757384973280, -1.849990392679412565, 2.220446049250313081E-13 ) ) ;
#22456=CARTESIAN_POINT ( 'NONE',  ( 114.9997167782375698, -1.308140751793612777, 1.308140751793862577 ) ) ;
#22460=CARTESIAN_POINT ( 'NONE',  ( 113.4999999999999147, -2.499999999999919176, 0.000000000000000000 ) ) ;
#22491=CARTESIAN_POINT ( 'NONE',  ( 108.1249999999999574, 1.767766952966293159, 1.767766952966431937 ) ) ;
#22502=EDGE_LOOP ( 'NONE', ( #24619, #26073, #1271, #11547 ) ) ;
#22517=SHAPE_DEFINITION_REPRESENTATION ( #13898, #4035 ) ;
#22519=CARTESIAN_POINT ( 'NONE',  ( 117.9613248654051318, 5.551115123125782702E-14, 2.000000000000001776 ) ) ;
#22529=CARTESIAN_POINT ( 'NONE',  ( 119.9997167782376124, -1.308140751793529510, 1.308140751793973600 ) ) ;
#22534=CARTESIAN_POINT ( 'NONE',  ( 117.0627832217621318, -0.7662911109077686911, -1.849990392679231599 ) ) ;
#22549=CARTESIAN_POINT ( 'NONE',  ( 108.7886751345946834, -1.999999999999946265, 1.110223024625156540E-13 ) ) ;
#22552=CARTESIAN_POINT ( 'NONE',  ( 119.0863248654051461, -1.414213562373145550, 1.414213562373145550 ) ) ;
#22554=CARTESIAN_POINT ( 'NONE',  ( 114.6249999999999574, -1.767766952966431937, -1.767766952966431937 ) ) ;
#22565=CARTESIAN_POINT ( 'NONE',  ( 116.1874999999999005, 1.035533905932839449, 2.500000000000205169 ) ) ;
#22566=CARTESIAN_POINT ( 'NONE',  ( 110.2502832217623165, 1.308140751793640533, -1.308140751793640533 ) ) ;
#22574=ORIENTED_EDGE ( 'NONE', *, *, #21327, .F. ) ;
#22589=CYLINDRICAL_SURFACE ( 'NONE', #25983, 2.000000000000012879 ) ;
#22594=CARTESIAN_POINT ( 'NONE',  ( 112.0627832217620750, -0.7662911109077388261, -1.849990392679231599 ) ) ;
#22596=CARTESIAN_POINT ( 'NONE',  ( 119.2113248654050466, -1.999999999999946265, 2.220446049250313081E-13 ) ) ;
#22605=DIRECTION ( 'NONE',  ( 5.551115123125785167E-17, -1.000000000000000000, -8.881784197001256268E-16 ) ) ;
#22609=CARTESIAN_POINT ( 'NONE',  ( 114.2497167782375698, -1.308140751793557266, -1.308140751793640533 ) ) ;
#22641=CARTESIAN_POINT ( 'NONE',  ( 109.1249999999999289, 1.767766952966265404, 1.767766952966431937 ) ) ;
#22668=CARTESIAN_POINT ( 'NONE',  ( 117.0238248654050324, -0.8284271247462354770, 2.000000000000212275 ) ) ;
#22673=DIRECTION ( 'NONE',  ( 5.551115123125785167E-17, -1.000000000000000000, -8.881784197001256268E-16 ) ) ;
#22686=CARTESIAN_POINT ( 'NONE',  ( 116.1877832217621886, 0.7662911109078888172, -1.849990392679291551 ) ) ;
#22691=DIRECTION ( 'NONE',  ( 5.551115123125785167E-17, -1.000000000000000000, -8.881784197001256268E-16 ) ) ;
#22693=VERTEX_POINT ( 'NONE', #18344 ) ;
#22703=CARTESIAN_POINT ( 'NONE',  ( 117.8124999999998579, 1.035533905932869425, -2.499999999999784173 ) ) ;
#22706=CARTESIAN_POINT ( 'NONE',  ( 106.2886751345948255, 2.000000000000029310, 1.110223024625156540E-13 ) ) ;
#22713=CARTESIAN_POINT ( 'NONE',  ( 109.0002832217621034, -1.308140751793640533, -1.308140751793640533 ) ) ;
#22736=ORIENTED_EDGE ( 'NONE', *, *, #24418, .F. ) ;
#22742=CARTESIAN_POINT ( 'NONE',  ( 110.0627832217622313, -0.7662911109076785410, -1.849990392679171425 ) ) ;
#22746=CARTESIAN_POINT ( 'NONE',  ( 119.5863248654052029, 1.414213562373145550, -1.414213562373034527 ) ) ;
#22748=CARTESIAN_POINT ( 'NONE',  ( 119.9999999999998579, 0.6961469067503631702, -2.048720570868077573 ) ) ;
#22752=AXIS2_PLACEMENT_3D ( 'NONE', #6330, #3717, #13148 ) ;
#22759=CARTESIAN_POINT ( 'NONE',  ( 109.3747167782375556, -1.665334536937734811E-13, -1.849990392679523588 ) ) ;
#22762=CARTESIAN_POINT ( 'NONE',  ( 104.7401757384974559, 1.799749494549046203, 0.4423533583444329009 ) ) ;
#22763=ORIENTED_EDGE ( 'NONE', *, *, #25836, .F. ) ;
#22771=CARTESIAN_POINT ( 'NONE',  ( 117.4761751345945839, 0.8284271247463257382, 2.000000000000151879 ) ) ;
#22772=CARTESIAN_POINT ( 'NONE',  ( 105.1488248654049329, -1.999999999999941602, 0.8284271247463557142 ) ) ;
#22791=CARTESIAN_POINT ( 'NONE',  ( 0.000000000000000000, 0.000000000000000000, 0.000000000000000000 ) ) ;
#22794=CARTESIAN_POINT ( 'NONE',  ( 107.4374999999997868, -2.499999999999964473, 1.035533905932989551 ) ) ;
#22811=CARTESIAN_POINT ( 'NONE',  ( 114.7113248654050750, 2.000000000000057288, 0.000000000000000000 ) ) ;
#22825=CARTESIAN_POINT ( 'NONE',  ( 0.000000000000000000, 0.000000000000000000, 0.000000000000000000 ) ) ;
#22833=CARTESIAN_POINT ( 'NONE',  ( 117.7502832217623592, -1.308140751793585022, 1.308140751793862577 ) ) ;
#22836=VECTOR ( 'NONE', #19913, 1000.000000000000000 ) ;
#22853=CARTESIAN_POINT ( 'NONE',  ( 117.7499999999998721, 1.387778780781445676E-13, -2.499999999999835687 ) ) ;
#22865=CARTESIAN_POINT ( 'NONE',  ( 117.6874999999997726, -1.035533905932719101, -2.499999999999844569 ) ) ;
#22866=CARTESIAN_POINT ( 'NONE',  ( 110.8127832217621318, -1.849990392679381701, 0.7662911109078888172 ) ) ;
#22908=CARTESIAN_POINT ( 'NONE',  ( 111.6872167782374135, 1.849990392679562001, 0.7662911109079489913 ) ) ;
#22909=CARTESIAN_POINT ( 'NONE',  ( 118.2738248654049329, -1.999999999999971800, -0.8284271247458748766 ) ) ;
#22910=CARTESIAN_POINT ( 'NONE',  ( 113.6872167782373850, 1.849990392679532247, 0.7662911109078888172 ) ) ;
#22912=( BOUNDED_CURVE ( )  B_SPLINE_CURVE ( 2, ( #24485, #26633, #17015, #12562, #988, #10087, #26344, #5292, #19460 ),
 .UNSPECIFIED., .F., .F. ) 
 B_SPLINE_CURVE_WITH_KNOTS ( ( 3, 2, 2, 2, 3 ),
 ( 0.7058823529411764053, 0.7132352941176470784, 0.7205882352941176405, 0.7279411764705882026, 0.7352941176470588758 ),
 .UNSPECIFIED. ) 
 CURVE ( )  GEOMETRIC_REPRESENTATION_ITEM ( )  RATIONAL_B_SPLINE_CURVE ( ( 1.000000000000000000, 0.9238795325112867385, 1.000000000000000000, 0.9238795325112867385, 1.000000000000000000, 0.9238795325112867385, 1.000000000000000000, 0.9238795325112867385, 1.000000000000000000 ) ) 
 REPRESENTATION_ITEM ( '' )  );
#22928=EDGE_CURVE ( 'NONE', #21920, #24100, #16869, .T. ) ;
#22936=CARTESIAN_POINT ( 'NONE',  ( 109.1249999999999289, 1.767766952966265404, 1.767766952966431937 ) ) ;
#22947=CARTESIAN_POINT ( 'NONE',  ( 105.6249999999999005, -1.767766952966376426, -1.767766952966320915 ) ) ;
#22954=CARTESIAN_POINT ( 'NONE',  ( 119.7499999999998721, 1.110223024625156540E-13, -2.499999999999946709 ) ) ;
#22967=CARTESIAN_POINT ( 'NONE',  ( 120.5002832217621886, 1.308140751793723799, 1.308140751793751555 ) ) ;
#22986=CARTESIAN_POINT ( 'NONE',  ( 117.0622167782374561, -1.849990392679472073, 0.7662911109078888172 ) ) ;
#23010=CARTESIAN_POINT ( 'NONE',  ( 114.8124999999998010, 1.035533905932749299, -2.499999999999844569 ) ) ;
#23018=CARTESIAN_POINT ( 'NONE',  ( 117.9999999999997868, 2.500000000000002220, 2.220446049250313081E-13 ) ) ;
#23020=CARTESIAN_POINT ( 'NONE',  ( 112.2502832217622739, 1.308140751793640533, -1.308140751793640533 ) ) ;
#23022=ORIENTED_EDGE ( 'NONE', *, *, #12364, .T. ) ;
#23023=CARTESIAN_POINT ( 'NONE',  ( 107.8122167782374135, 0.7662911109078888172, 1.849990392679712103 ) ) ;
#23026=CARTESIAN_POINT ( 'NONE',  ( 110.9613248654051176, -5.551115123125782702E-14, 2.000000000000112799 ) ) ;
#23028=CARTESIAN_POINT ( 'NONE',  ( 107.0238248654051176, -0.8284271247461153509, 2.000000000000212275 ) ) ;
#23046=CARTESIAN_POINT ( 'NONE',  ( 110.9761751345946266, -0.8284271247460852639, -1.999999999999791278 ) ) ;
#23050=CARTESIAN_POINT ( 'NONE',  ( 110.3127832217620323, 1.849990392679501827, -0.7662911109075883909 ) ) ;
#23068=CARTESIAN_POINT ( 'NONE',  ( 108.2497167782376266, -1.308140751793585022, -1.308140751793640533 ) ) ;
#23070=CARTESIAN_POINT ( 'NONE',  ( 112.4372167782373708, 0.7662911109079189043, -1.849990392679231599 ) ) ;
#23072=EDGE_CURVE ( 'NONE', #28223, #4728, #17940, .T. ) ;
#23094=CARTESIAN_POINT ( 'NONE',  ( 109.6249999999999858, -1.767766952966376426, -1.767766952966320915 ) ) ;
#23095=LINE ( 'NONE', #23401, #41 ) ;
#23106=CARTESIAN_POINT ( 'NONE',  ( 104.4999999999998863, -2.499999999999919176, 0.000000000000000000 ) ) ;
#23112=DIRECTION ( 'NONE',  ( 5.551115123125785167E-17, -1.000000000000000000, -8.881784197001256268E-16 ) ) ;
#23125=CARTESIAN_POINT ( 'NONE',  ( 117.8752832217622881, -1.849990392679551343, 0.000000000000000000 ) ) ;
#23145=CARTESIAN_POINT ( 'NONE',  ( 119.3747167782375413, -5.551115123125782702E-14, -1.849990392679523588 ) ) ;
#23151=CARTESIAN_POINT ( 'NONE',  ( 115.1252832217622881, -2.220446049250313081E-13, -1.849990392679523588 ) ) ;
#23169=CARTESIAN_POINT ( 'NONE',  ( 112.5624999999998010, -2.499999999999994671, -1.035533905932689347 ) ) ;
#23174=PLANE ( 'NONE',  #5917 ) ;
#23179=CARTESIAN_POINT ( 'NONE',  ( 118.4374999999998863, -2.499999999999964473, 1.035533905932929599 ) ) ;
#23181=CARTESIAN_POINT ( 'NONE',  ( 106.3752832217622171, 1.849990392679523588, 0.000000000000000000 ) ) ;
#23185=CARTESIAN_POINT ( 'NONE',  ( 109.8363248654051603, 1.414213562373090038, 1.414213562373034527 ) ) ;
#23186=CARTESIAN_POINT ( 'NONE',  ( 107.1872167782375840, -1.849990392679441875, -0.7662911109076485650 ) ) ;
#23202=CARTESIAN_POINT ( 'NONE',  ( 110.9136751345947260, -1.414213562373090038, -1.414213562373145550 ) ) ;
#23204=CYLINDRICAL_SURFACE ( 'NONE', #15307, 2.000000000000012879 ) ;
#23206=CARTESIAN_POINT ( 'NONE',  ( 112.3752832217621176, 1.849990392679551343, 0.000000000000000000 ) ) ;
#23221=AXIS2_PLACEMENT_3D ( 'NONE', #13639, #16108, #30338 ) ;
#23223=CARTESIAN_POINT ( 'NONE',  ( 108.6872167782374277, 1.849990392679591977, 0.7662911109078888172 ) ) ;
#23225=CARTESIAN_POINT ( 'NONE',  ( 112.9372167782374987, -0.7662911109076785410, 1.849990392679591977 ) ) ;
#23231=ORIENTED_EDGE ( 'NONE', *, *, #24477, .T. ) ;
#23244=DIRECTION ( 'NONE',  ( 0.000000000000000000, -1.000000000000000000, -8.881784197001262184E-16 ) ) ;
#23250=CARTESIAN_POINT ( 'NONE',  ( 110.0624999999998437, 2.499999999999994671, 1.035533905932809473 ) ) ;
#23262=CARTESIAN_POINT ( 'NONE',  ( 119.9372167782374277, -0.7662911109077388261, 1.849990392679652151 ) ) ;
#23279=CARTESIAN_POINT ( 'NONE',  ( 107.0622167782373708, -1.849990392679381701, 0.7662911109079489913 ) ) ;
#23280=CYLINDRICAL_SURFACE ( 'NONE', #1777, 2.000000000000012879 ) ;
#23284=CARTESIAN_POINT ( 'NONE',  ( 121.0002832217622739, -1.308140751793557266, -1.308140751793529510 ) ) ;
#23301=CARTESIAN_POINT ( 'NONE',  ( 118.0622167782374277, -1.849990392679381701, 0.7662911109079489913 ) ) ;
#23306=CARTESIAN_POINT ( 'NONE',  ( 114.1252832217622313, -8.326672684688674053E-14, -1.849990392679412565 ) ) ;
#23308=ORIENTED_EDGE ( 'NONE', *, *, #29570, .T. ) ;
#23323=CARTESIAN_POINT ( 'NONE',  ( 111.0624999999998295, 2.500000000000055067, 1.035533905932929599 ) ) ;
#23331=ORIENTED_EDGE ( 'NONE', *, *, #4461, .T. ) ;
#23333=CARTESIAN_POINT ( 'NONE',  ( 112.3749999999999289, -1.767766952966320915, 1.767766952966431937 ) ) ;
#23335=CARTESIAN_POINT ( 'NONE',  ( 105.5627832217622597, 0.7662911109077686911, 1.849990392679772278 ) ) ;
#23341=CARTESIAN_POINT ( 'NONE',  ( 105.5622167782374419, 1.849990392679591977, -0.7662911109075883909 ) ) ;
#23345=ADVANCED_FACE ( 'NONE', ( #14696 ), #26336, .F. ) ;
#23356=CARTESIAN_POINT ( 'NONE',  ( 107.9374999999997726, 2.500000000000144773, -1.035533905932508825 ) ) ;
#23361=CARTESIAN_POINT ( 'NONE',  ( 108.5627832217621886, 0.7662911109077987781, 1.849990392679652151 ) ) ;
#23363=CARTESIAN_POINT ( 'NONE',  ( 110.7886751345946834, -1.999999999999946265, 0.000000000000000000 ) ) ;
#23374=CARTESIAN_POINT ( 'NONE',  ( 110.5622167782373992, 1.849990392679501827, -0.7662911109077087390 ) ) ;
#23375=CARTESIAN_POINT ( 'NONE',  ( 116.7113248654051318, 2.000000000000057288, 0.000000000000000000 ) ) ;
#23376=CARTESIAN_POINT ( 'NONE',  ( 110.1872167782374703, -1.849990392679501827, -0.7662911109076485650 ) ) ;
#23384=ADVANCED_FACE ( 'NONE', ( #17157 ), #386, .F. ) ;
#23400=CARTESIAN_POINT ( 'NONE',  ( 108.2499999999998863, 5.551115123125782702E-14, 2.499999999999946709 ) ) ;
#23401=CARTESIAN_POINT ( 'NONE',  ( 1.110223024625164183E-16, -2.000000000000012879, -1.776356839400262692E-15 ) ) ;
#23410=CARTESIAN_POINT ( 'NONE',  ( 106.9374999999997868, 2.500000000000055067, -1.035533905932568777 ) ) ;
#23425=EDGE_CURVE ( 'NONE', #18908, #6908, #18934, .T. ) ;
#23428=CARTESIAN_POINT ( 'NONE',  ( 107.2497167782375129, -1.308140751793585022, -1.308140751793640533 ) ) ;
#23430=CARTESIAN_POINT ( 'NONE',  ( 119.8752832217623450, -1.849990392679523588, 0.000000000000000000 ) ) ;
#23444=CARTESIAN_POINT ( 'NONE',  ( 0.000000000000000000, 0.000000000000000000, 0.000000000000000000 ) ) ;
#23449=CARTESIAN_POINT ( 'NONE',  ( 118.4997167782374135, 1.308140751793696044, -1.308140751793640533 ) ) ;
#23451=ORIENTED_EDGE ( 'NONE', *, *, #7915, .F. ) ;
#23476=CARTESIAN_POINT ( 'NONE',  ( 112.9999999999998579, 2.500000000000057732, 0.000000000000000000 ) ) ;
#23485=CARTESIAN_POINT ( 'NONE',  ( 114.6249999999999574, -1.767766952966431937, -1.767766952966431937 ) ) ;
#23490=CARTESIAN_POINT ( 'NONE',  ( 105.8122167782375129, 0.7662911109077987781, 1.849990392679652151 ) ) ;
#23502=CARTESIAN_POINT ( 'NONE',  ( 107.1874999999997584, 1.035533905932779275, 2.500000000000205169 ) ) ;
#23509=CARTESIAN_POINT ( 'NONE',  ( 106.4377832217622029, 1.849990392679562001, 0.7662911109078287542 ) ) ;
#23512=DIRECTION ( 'NONE',  ( -1.000000000000000000, -1.665334536937736783E-16, -2.220446049250315546E-16 ) ) ;
#23516=CARTESIAN_POINT ( 'NONE',  ( 114.3511751345946408, 2.000000000000031530, 0.8284271247462955401 ) ) ;
#23522=CARTESIAN_POINT ( 'NONE',  ( 116.4136751345946834, 1.414213562373145550, 1.414213562373034527 ) ) ;
#23524=CARTESIAN_POINT ( 'NONE',  ( 118.2113248654050466, -1.999999999999946265, 2.220446049250313081E-13 ) ) ;
#23539=CARTESIAN_POINT ( 'NONE',  ( 117.6488248654050039, 2.000000000000151879, -0.8284271247458149245 ) ) ;
#23546=CARTESIAN_POINT ( 'NONE',  ( 110.3749999999999289, -1.767766952966209892, 1.767766952966542959 ) ) ;
#23554=ORIENTED_EDGE ( 'NONE', *, *, #18341, .T. ) ;
#23555=CARTESIAN_POINT ( 'NONE',  ( 106.8749999999998437, 1.767766952966320915, -1.767766952966320915 ) ) ;
#23561=CARTESIAN_POINT ( 'NONE',  ( 116.3124999999997158, -1.035533905932598975, 2.500000000000144773 ) ) ;
#23572=CARTESIAN_POINT ( 'NONE',  ( 119.7738248654049613, 2.000000000000061728, 0.8284271247464759513 ) ) ;
#23573=CARTESIAN_POINT ( 'NONE',  ( 105.0622167782375840, -1.849990392679501827, 0.7662911109077686911 ) ) ;
#23575=CARTESIAN_POINT ( 'NONE',  ( 120.7502832217623308, -1.308140751793640533, 1.308140751793751555 ) ) ;
#23594=CARTESIAN_POINT ( 'NONE',  ( 118.8122167782374987, 0.7662911109078287542, 1.849990392679712103 ) ) ;
#23600=CARTESIAN_POINT ( 'NONE',  ( 114.3752832217622597, 1.849990392679551343, 0.000000000000000000 ) ) ;
#23619=CARTESIAN_POINT ( 'NONE',  ( 112.8749999999998437, 1.767766952966320915, -1.767766952966320915 ) ) ;
#23628=CARTESIAN_POINT ( 'NONE',  ( 106.7886751345947403, -1.999999999999946265, 0.000000000000000000 ) ) ;
#23630=CARTESIAN_POINT ( 'NONE',  ( 111.6874999999997584, -1.035533905932719101, -2.499999999999844569 ) ) ;
#23632=CARTESIAN_POINT ( 'NONE',  ( 106.2502832217621460, 1.308140751793696044, -1.308140751793640533 ) ) ;
#23633=DIRECTION ( 'NONE',  ( 5.551115123125785167E-17, -1.000000000000000000, -8.881784197001256268E-16 ) ) ;
#23637=CARTESIAN_POINT ( 'NONE',  ( 106.5622167782373708, 1.849990392679501827, -0.7662911109076485650 ) ) ;
#23650=CARTESIAN_POINT ( 'NONE',  ( 109.8124999999997868, 1.035533905932779275, -2.499999999999784173 ) ) ;
#23656=CARTESIAN_POINT ( 'NONE',  ( 109.5627832217622455, 0.7662911109077987781, 1.849990392679652151 ) ) ;
#23674=( BOUNDED_CURVE ( )  B_SPLINE_CURVE ( 2, ( #1646, #8410, #1795, #29747, #29283, #18111, #25130, #1489, #13517 ),
 .UNSPECIFIED., .F., .T. ) 
 B_SPLINE_CURVE_WITH_KNOTS ( ( 3, 2, 2, 2, 3 ),
 ( 0.8529411764705882026, 0.8602941176470588758, 0.8676470588235294379, 0.8750000000000000000, 0.8823529411764705621 ),
 .UNSPECIFIED. ) 
 CURVE ( )  GEOMETRIC_REPRESENTATION_ITEM ( )  RATIONAL_B_SPLINE_CURVE ( ( 1.000000000000000000, 0.9238795325112867385, 1.000000000000000000, 0.9238795325112867385, 1.000000000000000000, 0.9238795325112867385, 1.000000000000000000, 0.9238795325112867385, 1.000000000000000000 ) ) 
 REPRESENTATION_ITEM ( '' )  );
#23683=ADVANCED_FACE ( 'NONE', ( #25392 ), #23280, .F. ) ;
#23687=CARTESIAN_POINT ( 'NONE',  ( 117.5863248654050608, 1.414213562373090038, -1.414213562373034527 ) ) ;
#23693=DIRECTION ( 'NONE',  ( -1.000000000000000000, -1.665334536937736783E-16, -2.220446049250315546E-16 ) ) ;
#23695=CARTESIAN_POINT ( 'NONE',  ( 106.9999999999999716, 2.500000000000030198, 0.000000000000000000 ) ) ;
#23697=EDGE_CURVE ( 'NONE', #29700, #7379, #7323, .T. ) ;
#23704=ORIENTED_EDGE ( 'NONE', *, *, #13066, .T. ) ;
#23705=CARTESIAN_POINT ( 'NONE',  ( 116.6247167782376692, 1.849990392679523588, 0.000000000000000000 ) ) ;
#23715=( BOUNDED_CURVE ( )  B_SPLINE_CURVE ( 2, ( #11933, #18977, #18820, #9436, #5251, #2800, #2370, #14381, #4949 ),
 .UNSPECIFIED., .F., .F. ) 
 B_SPLINE_CURVE_WITH_KNOTS ( ( 3, 2, 2, 2, 3 ),
 ( 0.2352941176470587648, 0.2426470588235294379, 0.2500000000000000000, 0.2573529411764705621, 0.2647058823529411242 ),
 .UNSPECIFIED. ) 
 CURVE ( )  GEOMETRIC_REPRESENTATION_ITEM ( )  RATIONAL_B_SPLINE_CURVE ( ( 1.000000000000000000, 0.9238795325112867385, 1.000000000000000000, 0.9238795325112867385, 1.000000000000000000, 0.9238795325112867385, 1.000000000000000000, 0.9238795325112867385, 1.000000000000000000 ) ) 
 REPRESENTATION_ITEM ( '' )  );
#23720=CARTESIAN_POINT ( 'NONE',  ( 106.9997167782376550, -1.308140751793612777, 1.308140751793640533 ) ) ;
#23723=CARTESIAN_POINT ( 'NONE',  ( 113.5627832217622029, 0.7662911109078888172, 1.849990392679652151 ) ) ;
#23733=CARTESIAN_POINT ( 'NONE',  ( -1.110223024625164676E-16, 2.000000000000012879, 2.021286199229734960E-15 ) ) ;
#23743=CARTESIAN_POINT ( 'NONE',  ( 115.4997167782375129, 1.308140751793640533, -1.308140751793640533 ) ) ;
#23761=( BOUNDED_CURVE ( )  B_SPLINE_CURVE ( 2, ( #18044, #15751, #2190, #18496, #1724, #29978, #11280, #1876, #25207 ),
 .UNSPECIFIED., .F., .T. ) 
 B_SPLINE_CURVE_WITH_KNOTS ( ( 3, 2, 2, 2, 3 ),
 ( 0.08823529411764707842, 0.09558823529411764053, 0.1029411764705882026, 0.1102941176470587648, 0.1176470588235294379 ),
 .UNSPECIFIED. ) 
 CURVE ( )  GEOMETRIC_REPRESENTATION_ITEM ( )  RATIONAL_B_SPLINE_CURVE ( ( 1.000000000000000000, 0.9238795325112867385, 1.000000000000000000, 0.9238795325112867385, 1.000000000000000000, 0.9238795325112867385, 1.000000000000000000, 0.9238795325112867385, 1.000000000000000000 ) ) 
 REPRESENTATION_ITEM ( '' )  );
#23766=CARTESIAN_POINT ( 'NONE',  ( 113.4999999999999147, -2.499999999999919176, 0.000000000000000000 ) ) ;
#23771=CARTESIAN_POINT ( 'NONE',  ( 114.6874999999997300, -1.035533905932689347, -2.499999999999784173 ) ) ;
#23778=CARTESIAN_POINT ( 'NONE',  ( 106.6247167782375840, 1.849990392679523588, 0.000000000000000000 ) ) ;
#23788=CARTESIAN_POINT ( 'NONE',  ( 108.5624999999997442, -2.499999999999934719, -1.035533905932568777 ) ) ;
#23795=CARTESIAN_POINT ( 'NONE',  ( 106.0627832217622455, -0.7662911109077388261, -1.849990392679351725 ) ) ;
#23798=CARTESIAN_POINT ( 'NONE',  ( 119.4136751345947403, 1.414213562373117794, 1.414213562373034527 ) ) ;
#23812=CARTESIAN_POINT ( 'NONE',  ( 111.5386751345947403, 5.551115123125782702E-14, 2.000000000000001776 ) ) ;
#23841=CARTESIAN_POINT ( 'NONE',  ( 106.2499999999999716, -2.775557561562891351E-14, 2.499999999999946709 ) ) ;
#23847=CARTESIAN_POINT ( 'NONE',  ( 115.8122167782375982, 0.7662911109078588412, 1.849990392679712103 ) ) ;
#23852=CARTESIAN_POINT ( 'NONE',  ( 117.9374999999998721, 2.500000000000115019, -1.035533905932448873 ) ) ;
#23865=CARTESIAN_POINT ( 'NONE',  ( 107.7497167782375982, 1.308140751793668288, 1.308140751793640533 ) ) ;
#23866=CARTESIAN_POINT ( 'NONE',  ( 116.5627832217621034, 0.7662911109078888172, 1.849990392679652151 ) ) ;
#23885=DIRECTION ( 'NONE',  ( 0.000000000000000000, -1.000000000000000000, -8.881784197001264156E-16 ) ) ;
#23911=CARTESIAN_POINT ( 'NONE',  ( 104.5938208054404299, -2.337497598169785640, 2.220446049250313081E-13 ) ) ;
#23914=CARTESIAN_POINT ( 'NONE',  ( 119.9999999999997868, 6.000000000000152767, 2.049675791781414311E-14 ) ) ;
#23917=CARTESIAN_POINT ( 'NONE',  ( 113.1874999999998295, 1.035533905932779275, 2.500000000000205169 ) ) ;
#23924=CARTESIAN_POINT ( 'NONE',  ( 119.4377832217620607, 1.849990392679591977, 0.7662911109080692285 ) ) ;
#23925=VERTEX_POINT ( 'NONE', #9743 ) ;
#23930=VERTEX_POINT ( 'NONE', #15115 ) ;
#23939=CARTESIAN_POINT ( 'NONE',  ( 108.8124999999997442, 1.035533905932839449, -2.499999999999964473 ) ) ;
#23948=CARTESIAN_POINT ( 'NONE',  ( 108.2502832217622029, 1.308140751793640533, -1.308140751793640533 ) ) ;
#23951=CARTESIAN_POINT ( 'NONE',  ( 113.4136751345947260, 1.414213562373117794, 1.414213562373034527 ) ) ;
#23963=ORIENTED_EDGE ( 'NONE', *, *, #28989, .T. ) ;
#23965=VERTEX_POINT ( 'NONE', #15275 ) ;
#23967=LINE ( 'NONE', #28691, #767 ) ;
#23982=CARTESIAN_POINT ( 'NONE',  ( 105.3124999999998437, -1.035533905932598975, 2.500000000000265121 ) ) ;
#23987=CARTESIAN_POINT ( 'NONE',  ( 107.9761751345945839, -0.8284271247461453269, -1.999999999999791278 ) ) ;
#23988=CARTESIAN_POINT ( 'NONE',  ( 118.0386751345946976, 8.326672684688674053E-14, -2.000000000000001776 ) ) ;
#23992=CARTESIAN_POINT ( 'NONE',  ( 118.2497167782374419, -1.308140751793585022, -1.308140751793640533 ) ) ;
#23997=CARTESIAN_POINT ( 'NONE',  ( 118.1874999999997300, 1.035533905932719101, 2.500000000000205169 ) ) ;
#24012=CARTESIAN_POINT ( 'NONE',  ( 116.6877832217621460, -0.7662911109077388261, 1.849990392679712103 ) ) ;
#24024=VECTOR ( 'NONE', #10735, 1000.000000000000000 ) ;
#24040=CARTESIAN_POINT ( 'NONE',  ( 119.9999999999999005, 0.6961469067658530019, 2.048720570865176338 ) ) ;
#24043=CARTESIAN_POINT ( 'NONE',  ( 111.2886751345946834, 2.000000000000001776, 3.330669073875469621E-13 ) ) ;
#24049=DIRECTION ( 'NONE',  ( 0.000000000000000000, -1.000000000000000000, -8.881784197001264156E-16 ) ) ;
#24051=CARTESIAN_POINT ( 'NONE',  ( 115.7261751345947118, -1.999999999999941602, 0.8284271247464759513 ) ) ;
#24058=CARTESIAN_POINT ( 'NONE',  ( 109.0624999999997868, 2.500000000000055067, 1.035533905932809473 ) ) ;
#24061=CARTESIAN_POINT ( 'NONE',  ( 113.1488248654051176, -1.999999999999941602, 0.8284271247465359034 ) ) ;
#24064=CARTESIAN_POINT ( 'NONE',  ( 119.6252832217623165, 0.000000000000000000, 1.849990392679523588 ) ) ;
#24073=CARTESIAN_POINT ( 'NONE',  ( 113.8988248654049755, 0.8284271247462654530, 2.000000000000271783 ) ) ;
#24075=CARTESIAN_POINT ( 'NONE',  ( 104.7499999999998295, 5.551115123125782702E-14, -2.499999999999835687 ) ) ;
#24083=CARTESIAN_POINT ( 'NONE',  ( 119.1249999999999432, 1.767766952966348670, 1.767766952966431937 ) ) ;
#24084=LINE ( 'NONE', #431, #19139 ) ;
#24100=VERTEX_POINT ( 'NONE', #25060 ) ;
#24105=ORIENTED_EDGE ( 'NONE', *, *, #28474, .F. ) ;
#24107=CARTESIAN_POINT ( 'NONE',  ( 1.110223024625164183E-16, -2.000000000000012879, -1.776356839400262692E-15 ) ) ;
#24112=CARTESIAN_POINT ( 'NONE',  ( 104.4999999999998863, -2.499999999999919176, 0.000000000000000000 ) ) ;
#24134=CARTESIAN_POINT ( 'NONE',  ( 118.1636751345947829, 1.414213562373090038, -1.414213562373145550 ) ) ;
#24137=CARTESIAN_POINT ( 'NONE',  ( 119.4997167782375982, 1.308140751793723799, -1.308140751793640533 ) ) ;
#24142=CARTESIAN_POINT ( 'NONE',  ( 113.5624999999997016, -2.499999999999964473, -1.035533905932689347 ) ) ;
#24154=EDGE_CURVE ( 'NONE', #2721, #14144, #18981, .T. ) ;
#24160=CARTESIAN_POINT ( 'NONE',  ( 115.6252832217622597, 0.000000000000000000, 1.849990392679523588 ) ) ;
#24182=EDGE_LOOP ( 'NONE', ( #30076, #21002, #21316, #3112 ) ) ;
#24190=CARTESIAN_POINT ( 'NONE',  ( 111.6488248654050750, 2.000000000000061728, -0.8284271247459952248 ) ) ;
#24208=CARTESIAN_POINT ( 'NONE',  ( 119.6877832217621176, -0.7662911109077686911, 1.849990392679532247 ) ) ;
#24209=ORIENTED_EDGE ( 'NONE', *, *, #21744, .T. ) ;
#24227=CARTESIAN_POINT ( 'NONE',  ( 120.5624999999997442, -2.499999999999964473, -1.035533905932508825 ) ) ;
#24229=FACE_OUTER_BOUND ( 'NONE', #13691, .T. ) ;
#24252=( LENGTH_UNIT ( ) NAMED_UNIT ( * ) SI_UNIT ( .MILLI., .METRE. ) );
#24263=CARTESIAN_POINT ( 'NONE',  ( 106.6874999999998010, -1.035533905932689347, -2.499999999999784173 ) ) ;
#24267=CARTESIAN_POINT ( 'NONE',  ( 104.7401757384974417, 1.849990392679521589, 1.011113220803300925E-30 ) ) ;
#24275=ORIENTED_EDGE ( 'NONE', *, *, #18530, .T. ) ;
#24276=CARTESIAN_POINT ( 'NONE',  ( 119.6247167782376124, 1.849990392679523588, 0.000000000000000000 ) ) ;
#24283=CARTESIAN_POINT ( 'NONE',  ( 114.9374999999997726, 2.500000000000054623, -1.035533905932629173 ) ) ;
#24284=AXIS2_PLACEMENT_3D ( 'NONE', #10960, #8622, #6309 ) ;
#24301=CARTESIAN_POINT ( 'NONE',  ( 105.4761751345946976, 0.8284271247463257382, 2.000000000000212275 ) ) ;
#24313=CARTESIAN_POINT ( 'NONE',  ( 114.3747167782375556, -1.665334536937734811E-13, -1.849990392679523588 ) ) ;
#24326=CARTESIAN_POINT ( 'NONE',  ( 119.9999999999998579, 0.3537249946243956056, 2.089338094881703967 ) ) ;
#24330=PRESENTATION_STYLE_ASSIGNMENT (( #26340 ) ) ;
#24356=CARTESIAN_POINT ( 'NONE',  ( 121.2502832217622171, 1.308140751793640533, -1.308140751793418488 ) ) ;
#24370=CARTESIAN_POINT ( 'NONE',  ( 104.8749999999998437, 1.767766952966320915, -1.767766952966431937 ) ) ;
#24381=CARTESIAN_POINT ( 'NONE',  ( 118.9374999999996589, 2.500000000000234479, -1.035533905932568777 ) ) ;
#24392=ORIENTED_EDGE ( 'NONE', *, *, #18192, .T. ) ;
#24393=CARTESIAN_POINT ( 'NONE',  ( 119.6249999999999716, -1.767766952966404181, -1.767766952966320915 ) ) ;
#24409=SURFACE_STYLE_USAGE ( .BOTH. , #13245 ) ;
#24418=EDGE_CURVE ( 'NONE', #29800, #15916, #28849, .T. ) ;
#24424=EDGE_LOOP ( 'NONE', ( #6271, #12445, #27455, #26649 ) ) ;
#24430=CARTESIAN_POINT ( 'NONE',  ( 112.4997167782373992, 1.308140751793751555, -1.308140751793640533 ) ) ;
#24434=CARTESIAN_POINT ( 'NONE',  ( 112.9999999999998579, 2.500000000000057732, 0.000000000000000000 ) ) ;
#24442=( BOUNDED_CURVE ( )  B_SPLINE_CURVE ( 2, ( #20111, #27152, #28997, #3649, #26996, #15538, #29146, #24706, #3052 ),
 .UNSPECIFIED., .F., .T. ) 
 B_SPLINE_CURVE_WITH_KNOTS ( ( 3, 2, 2, 2, 3 ),
 ( 0.2647058823529411797, 0.2720588235294117418, 0.2794117647058823595, 0.2867647058823529216, 0.2941176470588235392 ),
 .UNSPECIFIED. ) 
 CURVE ( )  GEOMETRIC_REPRESENTATION_ITEM ( )  RATIONAL_B_SPLINE_CURVE ( ( 1.000000000000000000, 0.9238795325112867385, 1.000000000000000000, 0.9238795325112867385, 1.000000000000000000, 0.9238795325112867385, 1.000000000000000000, 0.9238795325112867385, 1.000000000000000000 ) ) 
 REPRESENTATION_ITEM ( '' )  );
#24443=CARTESIAN_POINT ( 'NONE',  ( 116.2738248654050750, -2.000000000000001776, -0.8284271247461753029 ) ) ;
#24460=LINE ( 'NONE', #2969, #15613 ) ;
#24461=CARTESIAN_POINT ( 'NONE',  ( 112.4997167782373992, 1.308140751793751555, -1.308140751793640533 ) ) ;
#24477=EDGE_CURVE ( 'NONE', #18130, #22143, #22912, .T. ) ;
#24478=FACE_OUTER_BOUND ( 'NONE', #2501, .T. ) ;
#24485=CARTESIAN_POINT ( 'NONE',  ( 116.7886751345947687, -2.000000000000001776, 0.000000000000000000 ) ) ;
#24504=CARTESIAN_POINT ( 'NONE',  ( 120.6877832217621176, -0.7662911109077388261, 1.849990392679652151 ) ) ;
#24506=ORIENTED_EDGE ( 'NONE', *, *, #1550, .F. ) ;
#24524=CARTESIAN_POINT ( 'NONE',  ( 118.6874999999998295, -1.035533905932719101, -2.499999999999844569 ) ) ;
#24538=CARTESIAN_POINT ( 'NONE',  ( 118.9999999999998437, 2.500000000000057732, 2.220446049250313081E-13 ) ) ;
#24539=TOROIDAL_SURFACE ( 'NONE', #18707, 6.000000000000000000, 5.000000000000004441 ) ;
#24558=ORIENTED_EDGE ( 'NONE', *, *, #9259, .T. ) ;
#24574=CARTESIAN_POINT ( 'NONE',  ( 108.7113248654051176, 2.000000000000057288, 0.000000000000000000 ) ) ;
#24582=CARTESIAN_POINT ( 'NONE',  ( 112.6247167782375271, 1.849990392679523588, 0.000000000000000000 ) ) ;
#24587=CARTESIAN_POINT ( 'NONE',  ( 112.2499999999998153, -5.551115123125782702E-14, 2.500000000000168754 ) ) ;
#24616=AXIS2_PLACEMENT_3D ( 'NONE', #24779, #13301, #18057 ) ;
#24617=ADVANCED_BREP_SHAPE_REPRESENTATION ( '', ( #14219, #18805 ), #1104 ) ;
#24618=CARTESIAN_POINT ( 'NONE',  ( 110.8747167782375556, 0.000000000000000000, 1.849990392679523588 ) ) ;
#24619=ORIENTED_EDGE ( 'NONE', *, *, #16161, .F. ) ;
#24623=EDGE_LOOP ( 'NONE', ( #5540, #1934, #30352, #25420 ) ) ;
#24636=ORIENTED_EDGE ( 'NONE', *, *, #18530, .F. ) ;
#24641=SURFACE_SIDE_STYLE ('',( #1288 ) ) ;
#24643=CARTESIAN_POINT ( 'NONE',  ( 117.8988248654050750, 0.8284271247462354770, 2.000000000000212275 ) ) ;
#24658=VECTOR ( 'NONE', #8873, 1000.000000000000000 ) ;
#24659=ORIENTED_EDGE ( 'NONE', *, *, #4249, .F. ) ;
#24662=CARTESIAN_POINT ( 'NONE',  ( 109.8511751345945839, -1.999999999999941602, -0.8284271247459952248 ) ) ;
#24663=CARTESIAN_POINT ( 'NONE',  ( 117.0002832217621602, -1.308140751793557266, -1.308140751793529510 ) ) ;
#24665=CARTESIAN_POINT ( 'NONE',  ( -1.110223024625164676E-16, 2.000000000000012879, 2.021286199229734960E-15 ) ) ;
#24668=DIRECTION ( 'NONE',  ( -1.000000000000000000, -1.665334536937736783E-16, -2.220446049250315546E-16 ) ) ;
#24672=EDGE_CURVE ( 'NONE', #16270, #4691, #11171, .T. ) ;
#24684=CARTESIAN_POINT ( 'NONE',  ( 119.1874999999998153, 1.035533905932779275, 2.500000000000205169 ) ) ;
#24691=DIRECTION ( 'NONE',  ( -1.000000000000000000, -1.665334536937736783E-16, -2.220446049250315546E-16 ) ) ;
#24696=CARTESIAN_POINT ( 'NONE',  ( 110.5002832217622881, 1.308140751793668288, 1.308140751793640533 ) ) ;
#24701=AXIS2_PLACEMENT_3D ( 'NONE', #2735, #883, #21800 ) ;
#24706=CARTESIAN_POINT ( 'NONE',  ( 115.7738248654051034, 2.000000000000001776, 0.8284271247463557142 ) ) ;
#24707=EDGE_LOOP ( 'NONE', ( #9873, #29659, #8309, #5692 ) ) ;
#24726=CARTESIAN_POINT ( 'NONE',  ( 115.7502832217623308, -1.308140751793585022, 1.308140751793640533 ) ) ;
#24735=CARTESIAN_POINT ( 'NONE',  ( 104.7401757384973564, -0.2415688265503397880, -1.838109686700451384 ) ) ;
#24742=VERTEX_POINT ( 'NONE', #18831 ) ;
#24743=CARTESIAN_POINT ( 'NONE',  ( 112.8747167782376124, 2.775557561562891351E-14, 1.849990392679634610 ) ) ;
#24750=CARTESIAN_POINT ( 'NONE',  ( 114.1874999999998153, 1.035533905932779275, 2.500000000000445421 ) ) ;
#24768=CARTESIAN_POINT ( 'NONE',  ( 104.1247167782375556, -1.849990392679468076, 0.000000000000000000 ) ) ;
#24775=DIRECTION ( 'NONE',  ( -1.000000000000000000, -1.665334536937736783E-16, -2.220446049250315546E-16 ) ) ;
#24777=CARTESIAN_POINT ( 'NONE',  ( 110.0624999999998295, 2.499999999999994671, 1.035533905932809473 ) ) ;
#24779=CARTESIAN_POINT ( 'NONE',  ( 0.000000000000000000, 0.000000000000000000, 0.000000000000000000 ) ) ;
#24788=ORIENTED_EDGE ( 'NONE', *, *, #28474, .T. ) ;
#24813=CARTESIAN_POINT ( 'NONE',  ( 120.0622167782374419, -1.849990392679472073, 0.7662911109078888172 ) ) ;
#24819=CARTESIAN_POINT ( 'NONE',  ( 118.4377832217621034, 1.849990392679591977, 0.7662911109080090544 ) ) ;
#24835=CARTESIAN_POINT ( 'NONE',  ( 117.1874999999997726, 1.035533905932659149, 2.500000000000205169 ) ) ;
#24846=CARTESIAN_POINT ( 'NONE',  ( 116.9374999999998295, 2.500000000000024425, -1.035533905932629173 ) ) ;
#24847=CARTESIAN_POINT ( 'NONE',  ( 109.4377832217621460, 1.849990392679562001, 0.7662911109080692285 ) ) ;
#24867=FILL_AREA_STYLE_COLOUR ( '', #6903 ) ;
#24870=CARTESIAN_POINT ( 'NONE',  ( 114.7886751345947403, -1.999999999999946265, 0.000000000000000000 ) ) ;
#24874=CARTESIAN_POINT ( 'NONE',  ( 112.7502832217623734, -1.308140751793640533, 1.308140751793640533 ) ) ;
#24878=CARTESIAN_POINT ( 'NONE',  ( 119.9999999999997442, 2.445790564474693340, -0.3393521411465372783 ) ) ;
#24890=CARTESIAN_POINT ( 'NONE',  ( 114.2261751345945839, 2.000000000000091926, -0.8284271247460553989 ) ) ;
#24898=( BOUNDED_CURVE ( )  B_SPLINE_CURVE ( 2, ( #25828, #23539, #23687, #21082, #25353, #27954, #14348, #2478, #2624 ),
 .UNSPECIFIED., .F., .F. ) 
 B_SPLINE_CURVE_WITH_KNOTS ( ( 3, 2, 2, 2, 3 ),
 ( 0.1764705882352941291, 0.1838235294117647189, 0.1911764705882352811, 0.1985294117647058709, 0.2058823529411764608 ),
 .UNSPECIFIED. ) 
 CURVE ( )  GEOMETRIC_REPRESENTATION_ITEM ( )  RATIONAL_B_SPLINE_CURVE ( ( 1.000000000000000000, 0.9238795325112867385, 1.000000000000000000, 0.9238795325112867385, 1.000000000000000000, 0.9238795325112867385, 1.000000000000000000, 0.9238795325112867385, 1.000000000000000000 ) ) 
 REPRESENTATION_ITEM ( '' )  );
#24900=ORIENTED_EDGE ( 'NONE', *, *, #17630, .F. ) ;
#24914=DIRECTION ( 'NONE',  ( -1.000000000000000000, -1.665334536937736783E-16, -2.220446049250315546E-16 ) ) ;
#24921=CARTESIAN_POINT ( 'NONE',  ( 110.7499999999998010, 2.775557561562891351E-14, -2.499999999999946709 ) ) ;
#24929=ORIENTED_EDGE ( 'NONE', *, *, #28096, .F. ) ;
#24938=CARTESIAN_POINT ( 'NONE',  ( 106.3363248654051034, -1.414213562373228816, -1.414213562373034527 ) ) ;
#24946=CARTESIAN_POINT ( 'NONE',  ( 101.5358983848621932, -1.203706215242021998E-32, -9.216943876758866938E-48 ) ) ;
#24951=DIRECTION ( 'NONE',  ( -1.000000000000000000, -1.665334536937736783E-16, -2.220446049250315546E-16 ) ) ;
#24954=CARTESIAN_POINT ( 'NONE',  ( 119.7497167782375556, 1.308140751793696044, 1.308140751793862577 ) ) ;
#24978=CARTESIAN_POINT ( 'NONE',  ( 115.9374999999998010, 2.500000000000055067, -1.035533905932629173 ) ) ;
#24989=CARTESIAN_POINT ( 'NONE',  ( 115.2499999999998721, -5.551115123125782702E-14, 2.500000000000057732 ) ) ;
#24990=CARTESIAN_POINT ( 'NONE',  ( 109.5002832217622881, 1.308140751793640533, 1.308140751793640533 ) ) ;
#24993=CARTESIAN_POINT ( 'NONE',  ( 109.7113248654051176, 2.000000000000057288, 0.000000000000000000 ) ) ;
#25019=CARTESIAN_POINT ( 'NONE',  ( 110.4377832217621034, 1.849990392679562001, 0.7662911109079489913 ) ) ;
#25035=CARTESIAN_POINT ( 'NONE',  ( 110.8122167782374987, 0.7662911109077388261, 1.849990392679772278 ) ) ;
#25050=CARTESIAN_POINT ( 'NONE',  ( 117.4136751345946834, 1.414213562373145550, 1.414213562373034527 ) ) ;
#25060=CARTESIAN_POINT ( 'NONE',  ( 10.00000000000002132, 6.000000000000083489, 2.049675791781519072E-14 ) ) ;
#25062=CARTESIAN_POINT ( 'NONE',  ( 101.5358983848621932, -1.203706215242021998E-32, -9.216943876758866938E-48 ) ) ;
#25070=CARTESIAN_POINT ( 'NONE',  ( 110.2499999999998010, -5.551115123125782702E-14, 2.500000000000168754 ) ) ;
#25083=ORIENTED_EDGE ( 'NONE', *, *, #28582, .F. ) ;
#25098=CARTESIAN_POINT ( 'NONE',  ( 104.4372167782374277, 0.7662911109077987781, -1.849990392679231599 ) ) ;
#25127=CARTESIAN_POINT ( 'NONE',  ( 116.5624999999998863, -2.499999999999844569, -1.035533905932629173 ) ) ;
#25130=CARTESIAN_POINT ( 'NONE',  ( 105.8363248654049613, 1.414213562373201061, 1.414213562373367594 ) ) ;
#25131=DIRECTION ( 'NONE',  ( -1.000000000000000000, -1.665334536937736783E-16, -2.220446049250315546E-16 ) ) ;
#25138=CARTESIAN_POINT ( 'NONE',  ( 116.8124999999998010, 1.035533905932719101, -2.499999999999784173 ) ) ;
#25139=CARTESIAN_POINT ( 'NONE',  ( 109.3752832217621744, 1.849990392679579099, 1.110223024625156540E-13 ) ) ;
#25143=CARTESIAN_POINT ( 'NONE',  ( 110.0238248654050182, -0.8284271247460852639, 2.000000000000212275 ) ) ;
#25165=CARTESIAN_POINT ( 'NONE',  ( 112.2113248654051176, -1.999999999999946265, 0.000000000000000000 ) ) ;
#25166=CARTESIAN_POINT ( 'NONE',  ( 110.6877832217622739, -0.7662911109076785410, 1.849990392679712103 ) ) ;
#25171=CARTESIAN_POINT ( 'NONE',  ( 1.110223024625164183E-16, -2.000000000000012879, -1.776356839400262692E-15 ) ) ;
#25182=CARTESIAN_POINT ( 'NONE',  ( 107.9997167782376835, -1.308140751793585022, 1.308140751793640533 ) ) ;
#25183=CARTESIAN_POINT ( 'NONE',  ( 118.3988248654050182, -0.8284271247461453269, -1.999999999999791278 ) ) ;
#25184=CARTESIAN_POINT ( 'NONE',  ( 113.9997167782376266, -1.308140751793585022, 1.308140751793862577 ) ) ;
#25207=CARTESIAN_POINT ( 'NONE',  ( 106.7886751345947403, -1.999999999999946265, 0.000000000000000000 ) ) ;
#25209=DIRECTION ( 'NONE',  ( 0.8660254037844380415, -0.5000000000000008882, -1.905606012543395233E-16 ) ) ;
#25220=CARTESIAN_POINT ( 'NONE',  ( 119.9997167782376124, -1.308140751793529510, 1.308140751793973600 ) ) ;
#25241=CARTESIAN_POINT ( 'NONE',  ( 116.8363248654050039, 1.414213562373173305, 1.414213562373034527 ) ) ;
#25250=CARTESIAN_POINT ( 'NONE',  ( 118.3122167782374561, -0.7662911109076485650, -1.849990392679411677 ) ) ;
#25255=CARTESIAN_POINT ( 'NONE',  ( 117.6877832217621034, -0.7662911109077388261, 1.849990392679712103 ) ) ;
#25261=CARTESIAN_POINT ( 'NONE',  ( 115.4613248654051318, 2.775557561562891351E-14, -2.000000000000001776 ) ) ;
#25273=CARTESIAN_POINT ( 'NONE',  ( 114.9999999999999716, 2.500000000000002220, 0.000000000000000000 ) ) ;
#25285=CARTESIAN_POINT ( 'NONE',  ( 118.5624999999997016, -2.499999999999874767, -1.035533905932568777 ) ) ;
#25287=CARTESIAN_POINT ( 'NONE',  ( 111.6877832217621176, -0.7662911109077388261, 1.849990392679652151 ) ) ;
#25289=ORIENTED_EDGE ( 'NONE', *, *, #6574, .T. ) ;
#25291=CARTESIAN_POINT ( 'NONE',  ( 109.4372167782374845, 0.7662911109079189043, -1.849990392679231599 ) ) ;
#25295=CARTESIAN_POINT ( 'NONE',  ( 111.0238248654050608, -0.8284271247461753029, 2.000000000000271783 ) ) ;
#25312=CARTESIAN_POINT ( 'NONE',  ( 0.000000000000000000, 0.000000000000000000, 0.000000000000000000 ) ) ;
#25313=CARTESIAN_POINT ( 'NONE',  ( 112.5863248654050608, 1.414213562373145550, -1.414213562373145550 ) ) ;
#25314=CARTESIAN_POINT ( 'NONE',  ( 110.7502832217622881, -1.308140751793585022, 1.308140751793640533 ) ) ;
#25321=CARTESIAN_POINT ( 'NONE',  ( 105.3511751345946124, 2.000000000000121680, 0.8284271247464761734 ) ) ;
#25322=EDGE_CURVE ( 'NONE', #28323, #27307, #7991, .T. ) ;
#25332=CARTESIAN_POINT ( 'NONE',  ( 110.1872167782374703, -1.849990392679501827, -0.7662911109076485650 ) ) ;
#25334=CARTESIAN_POINT ( 'NONE',  ( 114.0622167782374845, -1.849990392679501827, 0.7662911109078287542 ) ) ;
#25338=CARTESIAN_POINT ( 'NONE',  ( 106.7886751345947403, -1.999999999999946265, 0.000000000000000000 ) ) ;
#25353=CARTESIAN_POINT ( 'NONE',  ( 117.4613248654050750, 5.551115123125782702E-14, -2.000000000000001776 ) ) ;
#25360=CARTESIAN_POINT ( 'NONE',  ( 110.1249999999998437, 1.767766952966265404, 1.767766952966431937 ) ) ;
#25374=CARTESIAN_POINT ( 'NONE',  ( 105.2499999999999147, -2.775557561562891351E-14, 2.499999999999946709 ) ) ;
#25392=FACE_OUTER_BOUND ( 'NONE', #18892, .T. ) ;
#25393=CARTESIAN_POINT ( 'NONE',  ( 118.0002832217622171, -1.308140751793612777, -1.308140751793418488 ) ) ;
#25407=DIRECTION ( 'NONE',  ( 5.551115123125785167E-17, -1.000000000000000000, -8.881784197001256268E-16 ) ) ;
#25412=CARTESIAN_POINT ( 'NONE',  ( 119.5622167782373708, 1.849990392679621953, -0.7662911109075283278 ) ) ;
#25420=ORIENTED_EDGE ( 'NONE', *, *, #7595, .F. ) ;
#25431=CARTESIAN_POINT ( 'NONE',  ( 109.2886751345947971, 2.000000000000057288, 1.110223024625156540E-13 ) ) ;
#25436=CARTESIAN_POINT ( 'NONE',  ( 115.8749999999998579, 1.767766952966431937, -1.767766952966320915 ) ) ;
#25445=CARTESIAN_POINT ( 'NONE',  ( 116.9999999999999005, 2.500000000000057732, 1.110223024625156540E-13 ) ) ;
#25447=CARTESIAN_POINT ( 'NONE',  ( 108.5002832217622313, 1.308140751793696044, 1.308140751793640533 ) ) ;
#25451=CARTESIAN_POINT ( 'NONE',  ( 105.6872167782375413, 1.849990392679591977, 0.7662911109080692285 ) ) ;
#25474=CARTESIAN_POINT ( 'NONE',  ( 112.7113248654049897, 2.000000000000057288, 0.000000000000000000 ) ) ;
#25475=CARTESIAN_POINT ( 'NONE',  ( 112.1252832217621460, -5.551115123125782702E-14, -1.849990392679523588 ) ) ;
#25483=CARTESIAN_POINT ( 'NONE',  ( 114.2886751345947971, 2.000000000000029310, 1.110223024625156540E-13 ) ) ;
#25489=CARTESIAN_POINT ( 'NONE',  ( 116.3511751345946408, 2.000000000000061728, 0.8284271247464157772 ) ) ;
#25492=CARTESIAN_POINT ( 'NONE',  ( 109.6247167782375840, 1.849990392679634610, 1.110223024625156540E-13 ) ) ;
#25494=CARTESIAN_POINT ( 'NONE',  ( 112.8122167782374419, 0.7662911109079189043, 1.849990392679772278 ) ) ;
#25520=CARTESIAN_POINT ( 'NONE',  ( 109.7499999999999147, 5.551115123125782702E-14, -2.499999999999835687 ) ) ;
#25533=CARTESIAN_POINT ( 'NONE',  ( 107.1874999999997584, 1.035533905932779275, 2.500000000000205169 ) ) ;
#25552=CARTESIAN_POINT ( 'NONE',  ( 107.3747167782375840, -5.551115123125782702E-14, -1.849990392679523588 ) ) ;
#25556=CARTESIAN_POINT ( 'NONE',  ( 117.7502832217623592, -1.308140751793585022, 1.308140751793862577 ) ) ;
#25563=CARTESIAN_POINT ( 'NONE',  ( 105.5863248654051034, 1.414213562373090038, -1.414213562373145550 ) ) ;
#25566=CARTESIAN_POINT ( 'NONE',  ( 117.1488248654051176, -1.999999999999971800, 0.8284271247462955401 ) ) ;
#25572=AXIS2_PLACEMENT_3D ( 'NONE', #22825, #13190, #22673 ) ;
#25573=EDGE_CURVE ( 'NONE', #30412, #30347, #23715, .T. ) ;
#25580=CARTESIAN_POINT ( 'NONE',  ( 116.9372167782374845, -0.7662911109078588412, 1.849990392679652151 ) ) ;
#25607=CARTESIAN_POINT ( 'NONE',  ( 111.3124999999998295, -1.035533905932629173, 2.500000000000325517 ) ) ;
#25609=CYLINDRICAL_SURFACE ( 'NONE', #2021, 6.000000000000005329 ) ;
#25615=CARTESIAN_POINT ( 'NONE',  ( 112.6249999999998437, -1.767766952966431937, -1.767766952966320915 ) ) ;
#25618=CARTESIAN_POINT ( 'NONE',  ( 107.3127832217622313, 1.849990392679501827, -0.7662911109076485650 ) ) ;
#25623=CARTESIAN_POINT ( 'NONE',  ( 107.6872167782374561, 1.849990392679562001, 0.7662911109080090544 ) ) ;
#25641=CARTESIAN_POINT ( 'NONE',  ( 108.0627832217621034, -0.7662911109077388261, -1.849990392679351725 ) ) ;
#25648=CARTESIAN_POINT ( 'NONE',  ( 114.7261751345946976, -1.999999999999881650, 0.8284271247462955401 ) ) ;
#25656=CARTESIAN_POINT ( 'NONE',  ( 110.9997167782376266, -1.308140751793585022, 1.308140751793640533 ) ) ;
#25680=CARTESIAN_POINT ( 'NONE',  ( 108.4374999999999005, -2.499999999999934719, 1.035533905932929599 ) ) ;
#25684=VERTEX_POINT ( 'NONE', #5095 ) ;
#25690=ORIENTED_EDGE ( 'NONE', *, *, #13761, .F. ) ;
#25691=CARTESIAN_POINT ( 'NONE',  ( 105.0624999999998437, 2.500000000000055067, 1.035533905932869425 ) ) ;
#25697=AXIS2_PLACEMENT_3D ( 'NONE', #3220, #12645, #28875 ) ;
#25707=CARTESIAN_POINT ( 'NONE',  ( 113.2261751345946550, 2.000000000000031530, -0.8284271247459350507 ) ) ;
#25709=CARTESIAN_POINT ( 'NONE',  ( 119.6252832217623165, 0.000000000000000000, 1.849990392679523588 ) ) ;
#25710=( BOUNDED_CURVE ( )  B_SPLINE_CURVE ( 2, ( #13478, #25566, #16098, #22668, #13632, #4365, #25241, #13790, #30175 ),
 .UNSPECIFIED., .F., .T. ) 
 B_SPLINE_CURVE_WITH_KNOTS ( ( 3, 2, 2, 2, 3 ),
 ( 0.2058823529411764608, 0.2132352941176470507, 0.2205882352941176405, 0.2279411764705882304, 0.2352941176470588203 ),
 .UNSPECIFIED. ) 
 CURVE ( )  GEOMETRIC_REPRESENTATION_ITEM ( )  RATIONAL_B_SPLINE_CURVE ( ( 1.000000000000000000, 0.9238795325112867385, 1.000000000000000000, 0.9238795325112867385, 1.000000000000000000, 0.9238795325112867385, 1.000000000000000000, 0.9238795325112867385, 1.000000000000000000 ) ) 
 REPRESENTATION_ITEM ( '' )  );
#25727=DIRECTION ( 'NONE',  ( -1.000000000000000000, -1.665334536937736783E-16, -2.220446049250315546E-16 ) ) ;
#25732=CARTESIAN_POINT ( 'NONE',  ( 118.9372167782374277, -0.7662911109077686911, 1.849990392679652151 ) ) ;
#25737=CARTESIAN_POINT ( 'NONE',  ( 113.0627832217621886, -0.7662911109076184779, -1.849990392679291551 ) ) ;
#25755=CARTESIAN_POINT ( 'NONE',  ( 110.6874999999997868, -1.035533905932689347, -2.499999999999844569 ) ) ;
#25765=ORIENTED_EDGE ( 'NONE', *, *, #16912, .F. ) ;
#25768=CARTESIAN_POINT ( 'NONE',  ( 114.3124999999997726, -1.035533905932719101, 2.500000000000205169 ) ) ;
#25770=AXIS2_PLACEMENT_3D ( 'NONE', #1312, #10879, #13041 ) ;
#25771=CARTESIAN_POINT ( 'NONE',  ( 106.9377832217621318, -1.849990392679441875, -0.7662911109075883909 ) ) ;
#25788=CARTESIAN_POINT ( 'NONE',  ( 108.3124999999997442, -1.035533905932629173, 2.500000000000205169 ) ) ;
#25795=CARTESIAN_POINT ( 'NONE',  ( 106.6252832217623023, 2.775557561562891351E-14, 1.849990392679634610 ) ) ;
#25807=CARTESIAN_POINT ( 'NONE',  ( 116.7886751345947687, -2.000000000000001776, 0.000000000000000000 ) ) ;
#25811=CARTESIAN_POINT ( 'NONE',  ( 110.4997167782375698, 1.308140751793668288, -1.308140751793640533 ) ) ;
#25817=ORIENTED_EDGE ( 'NONE', *, *, #17878, .T. ) ;
#25824=VECTOR ( 'NONE', #24951, 1000.000000000000000 ) ;
#25828=CARTESIAN_POINT ( 'NONE',  ( 117.7113248654050466, 2.000000000000085265, 0.000000000000000000 ) ) ;
#25835=CARTESIAN_POINT ( 'NONE',  ( 111.6874999999997584, -1.035533905932719101, -2.499999999999844569 ) ) ;
#25836=EDGE_CURVE ( 'NONE', #22177, #7342, #5547, .T. ) ;
#25844=CARTESIAN_POINT ( 'NONE',  ( 104.8749999999998437, 1.767766952966320915, -1.767766952966431937 ) ) ;
#25849=CARTESIAN_POINT ( 'NONE',  ( 117.8124999999998437, 1.035533905932869425, -2.499999999999784173 ) ) ;
#25864=CARTESIAN_POINT ( 'NONE',  ( 105.1247167782375840, -1.849990392679468076, 0.000000000000000000 ) ) ;
#25866=CARTESIAN_POINT ( 'NONE',  ( 120.8752832217622029, -1.849990392679523588, 0.000000000000000000 ) ) ;
#25871=CARTESIAN_POINT ( 'NONE',  ( 105.3363248654050750, -1.414213562373256572, -1.414213562372923505 ) ) ;
#25876=CARTESIAN_POINT ( 'NONE',  ( 119.7886751345947829, -1.999999999999946265, 3.330669073875469621E-13 ) ) ;
#25877=CARTESIAN_POINT ( 'NONE',  ( 118.5622167782375698, 1.849990392679621953, -0.7662911109077087390 ) ) ;
#25882=CARTESIAN_POINT ( 'NONE',  ( 115.6252832217622597, 0.000000000000000000, 1.849990392679523588 ) ) ;
#25898=CARTESIAN_POINT ( 'NONE',  ( -1.110223024625164676E-16, 2.000000000000012879, 2.021286199229734960E-15 ) ) ;
#25901=CARTESIAN_POINT ( 'NONE',  ( 113.5624999999997158, -2.499999999999964473, -1.035533905932689347 ) ) ;
#25905=DIRECTION ( 'NONE',  ( -2.220446049250313574E-16, 1.000000000000000000, 8.049116928532386890E-16 ) ) ;
#25913=CARTESIAN_POINT ( 'NONE',  ( 111.4999999999998863, -2.499999999999946709, 1.110223024625156540E-13 ) ) ;
#25915=CARTESIAN_POINT ( 'NONE',  ( 106.3127832217621318, 1.849990392679501827, -0.7662911109075883909 ) ) ;
#25920=CARTESIAN_POINT ( 'NONE',  ( 105.7497167782376266, 1.308140751793696044, 1.308140751793640533 ) ) ;
#25932=CARTESIAN_POINT ( 'NONE',  ( 108.7499999999998579, 8.326672684688674053E-14, -2.499999999999835687 ) ) ;
#25938=CARTESIAN_POINT ( 'NONE',  ( 109.0627832217621176, -0.7662911109076785410, -1.849990392679171425 ) ) ;
#25940=DIRECTION ( 'NONE',  ( 5.551115123125783935E-17, -1.000000000000000000, -8.881784197001254296E-16 ) ) ;
#25950=DIRECTION ( 'NONE',  ( 5.551115123125785167E-17, -1.000000000000000000, -8.881784197001256268E-16 ) ) ;
#25964=EDGE_CURVE ( 'NONE', #22143, #29510, #28790, .T. ) ;
#25981=CARTESIAN_POINT ( 'NONE',  ( 110.6874999999997868, -1.035533905932689347, -2.499999999999844569 ) ) ;
#25983=AXIS2_PLACEMENT_3D ( 'NONE', #8121, #27317, #27167 ) ;
#25991=CARTESIAN_POINT ( 'NONE',  ( 116.6872167782373708, 1.849990392679501827, 0.7662911109079489913 ) ) ;
#26007=CARTESIAN_POINT ( 'NONE',  ( 104.2497167782374845, -1.308140751793640533, -1.308140751793640533 ) ) ;
#26020=CARTESIAN_POINT ( 'NONE',  ( 108.6011751345945697, -0.8284271247461453269, 2.000000000000332179 ) ) ;
#26028=EDGE_LOOP ( 'NONE', ( #16447, #7929, #13373, #3128 ) ) ;
#26031=CARTESIAN_POINT ( 'NONE',  ( 113.8752832217622313, -1.849990392679523588, 0.000000000000000000 ) ) ;
#26040=( GEOMETRIC_REPRESENTATION_CONTEXT ( 3 ) GLOBAL_UNCERTAINTY_ASSIGNED_CONTEXT ( ( #148 ) ) GLOBAL_UNIT_ASSIGNED_CONTEXT ( ( #22122, #8593, #8271 ) ) REPRESENTATION_CONTEXT ( 'NONE', 'WORKASPACE' ) );
#26053=CARTESIAN_POINT ( 'NONE',  ( 112.6249999999998437, -1.767766952966431937, -1.767766952966320915 ) ) ;
#26058=CARTESIAN_POINT ( 'NONE',  ( 107.2261751345946550, 2.000000000000031530, -0.8284271247458748766 ) ) ;
#26061=CARTESIAN_POINT ( 'NONE',  ( 112.9374999999997868, 2.500000000000114575, -1.035533905932448873 ) ) ;
#26064=CARTESIAN_POINT ( 'NONE',  ( 105.1877832217621176, 0.7662911109078588412, -1.849990392679291551 ) ) ;
#26066=ORIENTED_EDGE ( 'NONE', *, *, #24672, .T. ) ;
#26070=CARTESIAN_POINT ( 'NONE',  ( 107.3747167782375840, -5.551115123125782702E-14, -1.849990392679523588 ) ) ;
#26072=( BOUNDED_CURVE ( )  B_SPLINE_CURVE ( 2, ( #26793, #24662, #17633, #20068, #29256, #3449, #19613, #5457, #17793 ),
 .UNSPECIFIED., .F., .T. ) 
 B_SPLINE_CURVE_WITH_KNOTS ( ( 3, 2, 2, 2, 3 ),
 ( 0.2941176470588234837, 0.3014705882352941568, 0.3088235294117647189, 0.3161764705882352811, 0.3235294117647058432 ),
 .UNSPECIFIED. ) 
 CURVE ( )  GEOMETRIC_REPRESENTATION_ITEM ( )  RATIONAL_B_SPLINE_CURVE ( ( 1.000000000000000000, 0.9238795325112867385, 1.000000000000000000, 0.9238795325112867385, 1.000000000000000000, 0.9238795325112867385, 1.000000000000000000, 0.9238795325112867385, 1.000000000000000000 ) ) 
 REPRESENTATION_ITEM ( '' )  );
#26073=ORIENTED_EDGE ( 'NONE', *, *, #5508, .T. ) ;
#26081=CARTESIAN_POINT ( 'NONE',  ( 107.8124999999997442, 1.035533905932809473, -2.499999999999784173 ) ) ;
#26089=CARTESIAN_POINT ( 'NONE',  ( 107.5627832217621744, 0.7662911109077987781, 1.849990392679772278 ) ) ;
#26093=FACE_OUTER_BOUND ( 'NONE', #24623, .T. ) ;
#26123=CARTESIAN_POINT ( 'NONE',  ( 116.2261751345945129, 2.000000000000031530, -0.8284271247459350507 ) ) ;
#26128=CARTESIAN_POINT ( 'NONE',  ( 106.8749999999998437, 1.767766952966320915, -1.767766952966320915 ) ) ;
#26135=EDGE_LOOP ( 'NONE', ( #20874, #22736, #10595, #5014 ) ) ;
#26136=CARTESIAN_POINT ( 'NONE',  ( 116.3122167782374845, -0.7662911109077388261, -1.849990392679351725 ) ) ;
#26141=CARTESIAN_POINT ( 'NONE',  ( 118.2499999999997584, -8.326672684688674053E-14, 2.500000000000057732 ) ) ;
#26148=( BOUNDED_CURVE ( )  B_SPLINE_CURVE ( 2, ( #9645, #28355, #16738, #3443, #1305, #20227, #29250, #8532, #1460 ),
 .UNSPECIFIED., .F., .T. ) 
 B_SPLINE_CURVE_WITH_KNOTS ( ( 3, 2, 2, 2, 3 ),
 ( 0.5000000000000000000, 0.5073529411764705621, 0.5147058823529411242, 0.5220588235294117974, 0.5294117647058823595 ),
 .UNSPECIFIED. ) 
 CURVE ( )  GEOMETRIC_REPRESENTATION_ITEM ( )  RATIONAL_B_SPLINE_CURVE ( ( 1.000000000000000000, 0.9238795325112867385, 1.000000000000000000, 0.9238795325112867385, 1.000000000000000000, 0.9238795325112867385, 1.000000000000000000, 0.9238795325112867385, 1.000000000000000000 ) ) 
 REPRESENTATION_ITEM ( '' )  );
#26152=CARTESIAN_POINT ( 'NONE',  ( 105.8122167782375129, 0.7662911109077987781, 1.849990392679652151 ) ) ;
#26154=CARTESIAN_POINT ( 'NONE',  ( 115.5627832217620892, 0.7662911109077987781, 1.849990392679772278 ) ) ;
#26166=CARTESIAN_POINT ( 'NONE',  ( 104.9349859426397273, -1.403591609995181955, -1.388700252127261336 ) ) ;
#26171=CARTESIAN_POINT ( 'NONE',  ( 114.1872167782375413, -1.849990392679411677, -0.7662911109076485650 ) ) ;
#26175=CARTESIAN_POINT ( 'NONE',  ( 112.7502832217623734, -1.308140751793640533, 1.308140751793640533 ) ) ;
#26194=CARTESIAN_POINT ( 'NONE',  ( 114.1874999999998295, 1.035533905932779275, 2.500000000000445421 ) ) ;
#26203=CARTESIAN_POINT ( 'NONE',  ( 113.8749999999998721, 1.767766952966431937, -1.767766952966209892 ) ) ;
#26204=CARTESIAN_POINT ( 'NONE',  ( 107.7113248654050892, 2.000000000000057288, 0.000000000000000000 ) ) ;
#26205=CARTESIAN_POINT ( 'NONE',  ( 112.7113248654049897, 2.000000000000057288, 0.000000000000000000 ) ) ;
#26209=CARTESIAN_POINT ( 'NONE',  ( 119.7502832217622455, -1.308140751793501755, 1.308140751793751555 ) ) ;
#26219=CARTESIAN_POINT ( 'NONE',  ( 108.9374999999997442, 2.500000000000114575, -1.035533905932508825 ) ) ;
#26231=CARTESIAN_POINT ( 'NONE',  ( 106.5627832217621602, 0.7662911109078588412, 1.849990392679712103 ) ) ;
#26234=CARTESIAN_POINT ( 'NONE',  ( 113.5386751345947687, 5.551115123125782702E-14, 2.000000000000001776 ) ) ;
#26246=( BOUNDED_CURVE ( )  B_SPLINE_CURVE ( 2, ( #13862, #18754, #20741, #7203, #11860, #1986, #28229, #30091, #16615 ),
 .UNSPECIFIED., .F., .T. ) 
 B_SPLINE_CURVE_WITH_KNOTS ( ( 3, 2, 2, 2, 3 ),
 ( 0.2647058823529411242, 0.2720588235294117974, 0.2794117647058823595, 0.2867647058823529216, 0.2941176470588234837 ),
 .UNSPECIFIED. ) 
 CURVE ( )  GEOMETRIC_REPRESENTATION_ITEM ( )  RATIONAL_B_SPLINE_CURVE ( ( 1.000000000000000000, 0.9238795325112867385, 1.000000000000000000, 0.9238795325112867385, 1.000000000000000000, 0.9238795325112867385, 1.000000000000000000, 0.9238795325112867385, 1.000000000000000000 ) ) 
 REPRESENTATION_ITEM ( '' )  );
#26254=ORIENTED_EDGE ( 'NONE', *, *, #15154, .F. ) ;
#26274=CARTESIAN_POINT ( 'NONE',  ( 104.6249999999999005, -1.767766952966376426, -1.767766952966320915 ) ) ;
#26277=CARTESIAN_POINT ( 'NONE',  ( 104.7401757384973848, 1.791171210506977474, -0.4782956395680261763 ) ) ;
#26279=CARTESIAN_POINT ( 'NONE',  ( 107.9136751345947260, -1.414213562373256572, -1.414213562373034527 ) ) ;
#26281=CARTESIAN_POINT ( 'NONE',  ( 118.2261751345946408, 2.000000000000091926, -0.8284271247458748766 ) ) ;
#26284=CARTESIAN_POINT ( 'NONE',  ( 118.8122167782374987, 0.7662911109078287542, 1.849990392679712103 ) ) ;
#26304=CARTESIAN_POINT ( 'NONE',  ( 116.2502832217621886, 1.308140751793612777, -1.308140751793418488 ) ) ;
#26316=CARTESIAN_POINT ( 'NONE',  ( 115.3122167782374845, -0.7662911109077388261, -1.849990392679291551 ) ) ;
#26334=CARTESIAN_POINT ( 'NONE',  ( 119.9999999999998579, 1.988103546247746323, 1.253414257839255752 ) ) ;
#26336=CYLINDRICAL_SURFACE ( 'NONE', #3770, 2.000000000000012879 ) ;
#26337=CARTESIAN_POINT ( 'NONE',  ( 119.9999999999998437, 2.000000000000057288, 0.000000000000000000 ) ) ;
#26340=SURFACE_STYLE_USAGE ( .BOTH. , #24641 ) ;
#26344=CARTESIAN_POINT ( 'NONE',  ( 117.1636751345947545, 1.414213562373201061, -1.414213562373145550 ) ) ;
#26352=CARTESIAN_POINT ( 'NONE',  ( 110.5624999999998295, -2.499999999999994671, -1.035533905932568777 ) ) ;
#26360=CARTESIAN_POINT ( 'NONE',  ( 105.0622167782375840, -1.849990392679501827, 0.7662911109077686911 ) ) ;
#26377=ORIENTED_EDGE ( 'NONE', *, *, #17630, .T. ) ;
#26382=CARTESIAN_POINT ( 'NONE',  ( 120.9374999999996874, 2.500000000000114575, -1.035533905932629173 ) ) ;
#26385=CARTESIAN_POINT ( 'NONE',  ( 113.4761751345945555, 0.8284271247462053900, 2.000000000000212275 ) ) ;
#26403=ORIENTED_EDGE ( 'NONE', *, *, #5271, .T. ) ;
#26409=CARTESIAN_POINT ( 'NONE',  ( 104.1247167782375556, -1.849990392679468076, 0.000000000000000000 ) ) ;
#26421=CARTESIAN_POINT ( 'NONE',  ( 105.1249999999999005, 1.767766952966265404, 1.767766952966431937 ) ) ;
#26429=CARTESIAN_POINT ( 'NONE',  ( 118.6247167782376408, 1.849990392679468076, 0.000000000000000000 ) ) ;
#26436=CARTESIAN_POINT ( 'NONE',  ( 118.9374999999996589, 2.500000000000234479, -1.035533905932568999 ) ) ;
#26438=DIRECTION ( 'NONE',  ( 0.000000000000000000, -1.000000000000000000, -1.010643099614862550E-15 ) ) ;
#26448=VECTOR ( 'NONE', #12941, 1000.000000000000000 ) ;
#26453=CARTESIAN_POINT ( 'NONE',  ( 114.5627832217621602, 0.7662911109078588412, 1.849990392679712103 ) ) ;
#26464=EDGE_CURVE ( 'NONE', #29267, #20178, #1326, .T. ) ;
#26493=CARTESIAN_POINT ( 'NONE',  ( 108.9999999999998579, 2.500000000000030198, 1.110223024625156540E-13 ) ) ;
#26504=CARTESIAN_POINT ( 'NONE',  ( 104.3747167782376124, -5.551115123125782702E-14, -1.849990392679523588 ) ) ;
#26516=CARTESIAN_POINT ( 'NONE',  ( 113.9613248654051034, 2.775557561562891351E-14, 2.000000000000223821 ) ) ;
#26518=CARTESIAN_POINT ( 'NONE',  ( -1.110223024625164676E-16, 2.000000000000012879, 2.021286199229734960E-15 ) ) ;
#26526=CARTESIAN_POINT ( 'NONE',  ( 105.3752832217622739, 1.849990392679523588, 0.000000000000000000 ) ) ;
#26569=CARTESIAN_POINT ( 'NONE',  ( 108.0624999999998153, 2.500000000000115019, 1.035533905932929599 ) ) ;
#26571=CARTESIAN_POINT ( 'NONE',  ( 107.5238248654050466, 0.8284271247462654530, -1.999999999999851674 ) ) ;
#26580=CARTESIAN_POINT ( 'NONE',  ( 119.1247167782375698, -1.849990392679412565, 1.110223024625156540E-13 ) ) ;
#26584=CARTESIAN_POINT ( 'NONE',  ( 113.9999999999998153, 2.500000000000085265, 0.000000000000000000 ) ) ;
#26618=CARTESIAN_POINT ( 'NONE',  ( 104.9785324208944957, -0.3128015976218990746, 1.970815887930343235 ) ) ;
#26624=ORIENTED_EDGE ( 'NONE', *, *, #26868, .F. ) ;
#26626=CYLINDRICAL_SURFACE ( 'NONE', #3901, 2.000000000000012879 ) ;
#26628=( NAMED_UNIT ( * ) SI_UNIT ( $, .STERADIAN. ) SOLID_ANGLE_UNIT ( ) );
#26633=CARTESIAN_POINT ( 'NONE',  ( 116.8511751345945129, -1.999999999999881650, -0.8284271247460553989 ) ) ;
#26648=CARTESIAN_POINT ( 'NONE',  ( 120.9377832217621034, -1.849990392679562001, -0.7662911109077087390 ) ) ;
#26649=ORIENTED_EDGE ( 'NONE', *, *, #647, .F. ) ;
#26658=CARTESIAN_POINT ( 'NONE',  ( 104.6249999999999005, -1.767766952966376426, -1.767766952966320915 ) ) ;
#26666=CARTESIAN_POINT ( 'NONE',  ( 118.9613248654051318, 5.551115123125782702E-14, 2.000000000000001776 ) ) ;
#26668=CARTESIAN_POINT ( 'NONE',  ( 118.9999999999998437, 2.500000000000057732, 2.220446049250313081E-13 ) ) ;
#26680=CARTESIAN_POINT ( 'NONE',  ( 120.1249999999998295, 1.767766952966348670, 1.767766952966431937 ) ) ;
#26706=CARTESIAN_POINT ( 'NONE',  ( 108.1874999999998721, 1.035533905932719101, 2.500000000000205169 ) ) ;
#26710=CARTESIAN_POINT ( 'NONE',  ( 104.7401757384973848, 1.616881886637318688, -0.9308393922784925500 ) ) ;
#26717=CARTESIAN_POINT ( 'NONE',  ( 104.9868134515153031, -0.6968434951807797040, -1.879196483909238102 ) ) ;
#26719=CARTESIAN_POINT ( 'NONE',  ( 118.6011751345946550, -0.8284271247461453269, 2.000000000000332179 ) ) ;
#26724=CARTESIAN_POINT ( 'NONE',  ( 113.0624999999997726, 2.500000000000084821, 1.035533905932989551 ) ) ;
#26729=ORIENTED_EDGE ( 'NONE', *, *, #13761, .T. ) ;
#26752=CARTESIAN_POINT ( 'NONE',  ( 114.8988248654050182, 0.8284271247462955401, 2.000000000000212275 ) ) ;
#26753=CARTESIAN_POINT ( 'NONE',  ( 111.4997167782375413, 1.308140751793696044, -1.308140751793640533 ) ) ;
#26756=DIRECTION ( 'NONE',  ( 0.000000000000000000, -1.000000000000000000, -8.881784197001262184E-16 ) ) ;
#26758=EDGE_CURVE ( 'NONE', #11212, #18409, #13164, .T. ) ;
#26793=CARTESIAN_POINT ( 'NONE',  ( 109.7886751345948255, -2.000000000000001776, 0.000000000000000000 ) ) ;
#26815=CARTESIAN_POINT ( 'NONE',  ( 118.3124999999997726, -1.035533905932598975, 2.500000000000205169 ) ) ;
#26824=ADVANCED_FACE ( 'NONE', ( #1603 ), #16918, .T. ) ;
#26825=CARTESIAN_POINT ( 'NONE',  ( 119.1874999999998153, 1.035533905932779275, 2.500000000000205169 ) ) ;
#26848=DIRECTION ( 'NONE',  ( -1.000000000000000000, -1.665334536937736783E-16, -2.220446049250315546E-16 ) ) ;
#26861=CARTESIAN_POINT ( 'NONE',  ( 119.9999999999997868, 1.752251084791750291, -1.505035388676465580 ) ) ;
#26862=CARTESIAN_POINT ( 'NONE',  ( 107.5863248654051318, 1.414213562373145550, -1.414213562373145550 ) ) ;
#26868=EDGE_CURVE ( 'NONE', #11262, #3485, #7778, .T. ) ;
#26874=CARTESIAN_POINT ( 'NONE',  ( 112.0622167782374277, -1.849990392679472073, 0.7662911109078888172 ) ) ;
#26881=CARTESIAN_POINT ( 'NONE',  ( 114.5624999999997442, -2.499999999999934719, -1.035533905932448873 ) ) ;
#26896=MECHANICAL_DESIGN_GEOMETRIC_PRESENTATION_REPRESENTATION('',(#2465),#4352);
#26900=EDGE_CURVE ( 'NONE', #24100, #21920, #5373, .T. ) ;
#26908=CARTESIAN_POINT ( 'NONE',  ( 110.9997167782376266, -1.308140751793585022, 1.308140751793640533 ) ) ;
#26930=( NAMED_UNIT ( * ) PLANE_ANGLE_UNIT ( ) SI_UNIT ( $, .RADIAN. ) );
#26949=CARTESIAN_POINT ( 'NONE',  ( 120.6247167782375413, 1.849990392679579099, 0.000000000000000000 ) ) ;
#26965=CARTESIAN_POINT ( 'NONE',  ( 105.9999999999998863, 2.500000000000002220, 1.110223024625156540E-13 ) ) ;
#26967=VERTEX_POINT ( 'NONE', #27566 ) ;
#26968=CARTESIAN_POINT ( 'NONE',  ( 115.7886751345947118, -1.999999999999974021, 0.000000000000000000 ) ) ;
#26972=CARTESIAN_POINT ( 'NONE',  ( 105.4377832217621176, 1.849990392679562001, 0.7662911109078888172 ) ) ;
#26986=AXIS2_PLACEMENT_3D ( 'NONE', #12778, #7816, #27162 ) ;
#26988=CARTESIAN_POINT ( 'NONE',  ( 110.7502832217622881, -1.308140751793585022, 1.308140751793640533 ) ) ;
#26989=CARTESIAN_POINT ( 'NONE',  ( 107.7113248654050892, 2.000000000000057288, 0.000000000000000000 ) ) ;
#26994=DIRECTION ( 'NONE',  ( -1.000000000000000000, -1.665334536937736783E-16, -2.220446049250315546E-16 ) ) ;
#26996=CARTESIAN_POINT ( 'NONE',  ( 115.9613248654051603, 1.665334536937734811E-13, 2.000000000000223821 ) ) ;
#27019=CARTESIAN_POINT ( 'NONE',  ( 116.8752832217622313, -1.849990392679579099, 0.000000000000000000 ) ) ;
#27029=FACE_OUTER_BOUND ( 'NONE', #9886, .T. ) ;
#27033=CARTESIAN_POINT ( 'NONE',  ( 113.3747167782374987, -1.110223024625156540E-13, -1.849990392679523588 ) ) ;
#27038=CARTESIAN_POINT ( 'NONE',  ( 116.0624999999999005, 2.500000000000054623, 1.035533905932929599 ) ) ;
#27051=CARTESIAN_POINT ( 'NONE',  ( 116.6488248654049471, 2.000000000000091926, -0.8284271247460553989 ) ) ;
#27059=CARTESIAN_POINT ( 'NONE',  ( 105.7261751345946976, -1.999999999999881650, 0.8284271247462955401 ) ) ;
#27060=CARTESIAN_POINT ( 'NONE',  ( 101.5358983848621932, 0.000000000000000000, 0.000000000000000000 ) ) ;
#27064=DIRECTION ( 'NONE',  ( -1.000000000000000000, -1.665334536937736783E-16, -2.220446049250315546E-16 ) ) ;
#27067=CARTESIAN_POINT ( 'NONE',  ( 107.8124999999997442, 1.035533905932809473, -2.499999999999784173 ) ) ;
#27107=CARTESIAN_POINT ( 'NONE',  ( 120.1247167782375698, -1.849990392679523588, 0.000000000000000000 ) ) ;
#27112=CARTESIAN_POINT ( 'NONE',  ( 118.2502832217622739, 1.308140751793640533, -1.308140751793418488 ) ) ;
#27132=CARTESIAN_POINT ( 'NONE',  ( 116.2499999999998437, 5.551115123125782702E-14, 2.500000000000168754 ) ) ;
#27145=CARTESIAN_POINT ( 'NONE',  ( 109.1877832217621034, 0.7662911109079489913, -1.849990392679291551 ) ) ;
#27150=CARTESIAN_POINT ( 'NONE',  ( -1.110223024625164676E-16, 2.000000000000012879, 2.021286199229734960E-15 ) ) ;
#27152=CARTESIAN_POINT ( 'NONE',  ( 116.1488248654049755, -1.999999999999941602, 0.8284271247463557142 ) ) ;
#27162=DIRECTION ( 'NONE',  ( 1.665334536937739001E-16, -1.000000000000000000, -8.881784197001260212E-16 ) ) ;
#27167=DIRECTION ( 'NONE',  ( 5.551115123125785167E-17, -1.000000000000000000, -8.881784197001256268E-16 ) ) ;
#27171=CARTESIAN_POINT ( 'NONE',  ( 111.6877832217621176, -0.7662911109077388261, 1.849990392679652151 ) ) ;
#27176=CARTESIAN_POINT ( 'NONE',  ( 119.9999999999998295, 1.988103546243131570, -1.253414257844930102 ) ) ;
#27187=CARTESIAN_POINT ( 'NONE',  ( 114.3122167782374419, -0.7662911109077388261, -1.849990392679231599 ) ) ;
#27192=CARTESIAN_POINT ( 'NONE',  ( 114.9999999999999716, 2.500000000000002220, 0.000000000000000000 ) ) ;
#27218=CARTESIAN_POINT ( 'NONE',  ( 107.6249999999998721, -1.767766952966376426, -1.767766952966320915 ) ) ;
#27223=( BOUNDED_CURVE ( )  B_SPLINE_CURVE ( 2, ( #11529, #27291, #1969, #25143, #15843, #6408, #23185, #20719, #24993 ),
 .UNSPECIFIED., .F., .T. ) 
 B_SPLINE_CURVE_WITH_KNOTS ( ( 3, 2, 2, 2, 3 ),
 ( 0.6176470588235294379, 0.6250000000000000000, 0.6323529411764705621, 0.6397058823529411242, 0.6470588235294117974 ),
 .UNSPECIFIED. ) 
 CURVE ( )  GEOMETRIC_REPRESENTATION_ITEM ( )  RATIONAL_B_SPLINE_CURVE ( ( 1.000000000000000000, 0.9238795325112867385, 1.000000000000000000, 0.9238795325112867385, 1.000000000000000000, 0.9238795325112867385, 1.000000000000000000, 0.9238795325112867385, 1.000000000000000000 ) ) 
 REPRESENTATION_ITEM ( '' )  );
#27230=EDGE_CURVE ( 'NONE', #13661, #29800, #5697, .T. ) ;
#27232=ORIENTED_EDGE ( 'NONE', *, *, #27812, .F. ) ;
#27259=CARTESIAN_POINT ( 'NONE',  ( 116.5002832217622171, 1.308140751793696044, 1.308140751793640533 ) ) ;
#27277=CARTESIAN_POINT ( 'NONE',  ( 118.0624999999998010, 2.500000000000055067, 1.035533905932929599 ) ) ;
#27287=CARTESIAN_POINT ( 'NONE',  ( 116.5624999999998863, -2.499999999999844569, -1.035533905932629173 ) ) ;
#27289=CARTESIAN_POINT ( 'NONE',  ( 111.3752832217622739, 1.849990392679468076, 0.000000000000000000 ) ) ;
#27291=CARTESIAN_POINT ( 'NONE',  ( 110.1488248654049897, -2.000000000000001776, 0.8284271247464157772 ) ) ;
#27297=ADVANCED_FACE ( 'NONE', ( #1365 ), #21630, .T. ) ;
#27307=VERTEX_POINT ( 'NONE', #17531 ) ;
#27311=VECTOR ( 'NONE', #20370, 1000.000000000000000 ) ;
#27314=APPLICATION_CONTEXT ( 'automotive_design' ) ;
#27317=DIRECTION ( 'NONE',  ( -1.000000000000000000, -1.665334536937736783E-16, -2.220446049250315546E-16 ) ) ;
#27323=CARTESIAN_POINT ( 'NONE',  ( 111.2502832217621886, 1.308140751793696044, -1.308140751793640533 ) ) ;
#27326=CARTESIAN_POINT ( 'NONE',  ( 104.9999999999999432, -1.999999999999998668, -7.622424050173526697E-16 ) ) ;
#27335=DIRECTION ( 'NONE',  ( -1.000000000000000000, -1.665334536937736783E-16, -2.220446049250315546E-16 ) ) ;
#27338=ORIENTED_EDGE ( 'NONE', *, *, #25573, .F. ) ;
#27339=CARTESIAN_POINT ( 'NONE',  ( 114.1872167782375413, -1.849990392679411677, -0.7662911109076485650 ) ) ;
#27345=CARTESIAN_POINT ( 'NONE',  ( 110.6488248654049755, 2.000000000000001776, -0.8284271247459350507 ) ) ;
#27365=CYLINDRICAL_SURFACE ( 'NONE', #22752, 2.000000000000012879 ) ;
#27370=CARTESIAN_POINT ( 'NONE',  ( 110.4374999999997442, -2.500000000000024425, 1.035533905932809473 ) ) ;
#27384=ORIENTED_EDGE ( 'NONE', *, *, #14089, .T. ) ;
#27401=CARTESIAN_POINT ( 'NONE',  ( 114.2113248654050750, -1.999999999999890754, 0.000000000000000000 ) ) ;
#27409=CARTESIAN_POINT ( 'NONE',  ( 116.7502832217622171, -1.308140751793529510, 1.308140751793640533 ) ) ;
#27414=CARTESIAN_POINT ( 'NONE',  ( 0.000000000000000000, 0.000000000000000000, 0.000000000000000000 ) ) ;
#27428=CARTESIAN_POINT ( 'NONE',  ( 115.9999999999998153, 2.500000000000002220, 2.220446049250313081E-13 ) ) ;
#27436=CARTESIAN_POINT ( 'NONE',  ( 108.7502832217622881, -1.308140751793640533, 1.308140751793862577 ) ) ;
#27437=EDGE_LOOP ( 'NONE', ( #3572, #16566, #28510, #21991, #919, #1694, #26729, #18854, #21588, #24558, #3386, #19394, #28873, #29458, #25289, #23331, #8227, #28074, #9110, #1776, #9662, #8786, #9157, #22184, #11267, #23022, #14267, #6264, #13005, #19472, #2726, #19449, #19801, #6151, #26066, #16748 ) ) ;
#27455=ORIENTED_EDGE ( 'NONE', *, *, #24477, .F. ) ;
#27458=CARTESIAN_POINT ( 'NONE',  ( -1.110223024625164676E-16, 2.000000000000012879, 2.021286199229734960E-15 ) ) ;
#27460=CARTESIAN_POINT ( 'NONE',  ( 112.6252832217622597, 1.665334536937734811E-13, 1.849990392679745632 ) ) ;
#27472=CARTESIAN_POINT ( 'NONE',  ( 104.7401757384972427, 0.2428654671893633876, -1.837968757803231101 ) ) ;
#27479=CARTESIAN_POINT ( 'NONE',  ( 110.3122167782374419, -0.7662911109077388261, -1.849990392679411677 ) ) ;
#27481=CARTESIAN_POINT ( 'NONE',  ( 113.3122167782374277, -0.7662911109077388261, -1.849990392679231599 ) ) ;
#27485=CARTESIAN_POINT ( 'NONE',  ( 110.5863248654050750, 1.414213562373145550, -1.414213562373145550 ) ) ;
#27510=DIRECTION ( 'NONE',  ( 5.551115123125785167E-17, -1.000000000000000000, -8.881784197001256268E-16 ) ) ;
#27519=CARTESIAN_POINT ( 'NONE',  ( 105.1874999999998437, 1.035533905932749299, 2.500000000000265121 ) ) ;
#27528=VERTEX_POINT ( 'NONE', #1865 ) ;
#27536=CARTESIAN_POINT ( 'NONE',  ( 112.7886751345947403, -1.999999999999946265, 0.000000000000000000 ) ) ;
#27538=CARTESIAN_POINT ( 'NONE',  ( 110.6011751345947260, -0.8284271247461453269, 2.000000000000271783 ) ) ;
#27550=CARTESIAN_POINT ( 'NONE',  ( 114.3988248654049755, -0.8284271247461453269, -1.999999999999791278 ) ) ;
#27566=CARTESIAN_POINT ( 'NONE',  ( 119.2886751345947260, 1.999999999999946265, 1.110223024625156540E-13 ) ) ;
#27570=ORIENTED_EDGE ( 'NONE', *, *, #1506, .T. ) ;
#27575=CARTESIAN_POINT ( 'NONE',  ( 116.3124999999997158, -1.035533905932598975, 2.500000000000144773 ) ) ;
#27586=CARTESIAN_POINT ( 'NONE',  ( 115.1874999999998437, 1.035533905932719101, 2.500000000000265121 ) ) ;
#27588=CARTESIAN_POINT ( 'NONE',  ( 112.1877832217621886, 0.7662911109079189043, -1.849990392679291551 ) ) ;
#27592=CARTESIAN_POINT ( 'NONE',  ( 108.1247167782375556, -1.849990392679468076, 2.220446049250313081E-13 ) ) ;
#27610=DIRECTION ( 'NONE',  ( 2.220446049250313574E-16, 8.881784197001254296E-16, -1.000000000000000000 ) ) ;
#27613=DIRECTION ( 'NONE',  ( -1.000000000000000000, -1.665334536937736783E-16, -2.220446049250315546E-16 ) ) ;
#27618=CARTESIAN_POINT ( 'NONE',  ( 110.8752832217622029, -1.849990392679495832, 0.000000000000000000 ) ) ;
#27626=AXIS2_PLACEMENT_3D ( 'NONE', #17654, #4095, #11044 ) ;
#27634=CARTESIAN_POINT ( 'NONE',  ( 111.5622167782373566, 1.849990392679591977, -0.7662911109075283278 ) ) ;
#27636=CARTESIAN_POINT ( 'NONE',  ( 111.3747167782376692, -5.551115123125782702E-14, -1.849990392679523588 ) ) ;
#27654=CARTESIAN_POINT ( 'NONE',  ( 104.9999999999999716, -0.4876318259226519736, 1.939643060552054266 ) ) ;
#27657=CARTESIAN_POINT ( 'NONE',  ( 111.9136751345946692, -1.414213562373145550, -1.414213562373034527 ) ) ;
#27661=CARTESIAN_POINT ( 'NONE',  ( 108.9374999999997300, 2.500000000000115019, -1.035533905932508825 ) ) ;
#27674=CARTESIAN_POINT ( 'NONE',  ( 119.8747167782375982, 0.000000000000000000, 1.849990392679523588 ) ) ;
#27688=DIRECTION ( 'NONE',  ( -1.000000000000000000, -1.665334536937736783E-16, -2.220446049250315546E-16 ) ) ;
#27690=CARTESIAN_POINT ( 'NONE',  ( 118.1877832217622029, 0.7662911109078588412, -1.849990392679351725 ) ) ;
#27708=CARTESIAN_POINT ( 'NONE',  ( 116.1247167782375556, -1.849990392679468076, 1.110223024625156540E-13 ) ) ;
#27710=ADVANCED_FACE ( 'NONE', ( #5660 ), #24539, .T. ) ;
#27724=CYLINDRICAL_SURFACE ( 'NONE', #3226, 2.000000000000012879 ) ;
#27734=CARTESIAN_POINT ( 'NONE',  ( 116.3749999999998579, -1.767766952966209892, 1.767766952966542959 ) ) ;
#27742=CARTESIAN_POINT ( 'NONE',  ( 118.1874999999997158, 1.035533905932719101, 2.500000000000205169 ) ) ;
#27744=CARTESIAN_POINT ( 'NONE',  ( 107.3752832217621886, 1.849990392679523588, 0.000000000000000000 ) ) ;
#27757=( BOUNDED_CURVE ( )  B_SPLINE_CURVE ( 2, ( #5898, #3753, #6067, #29565, #15478, #25098, #17465, #3594, #4054, #13328, #15156 ),
 .UNSPECIFIED., .F., .T. ) 
 B_SPLINE_CURVE_WITH_KNOTS ( ( 3, 2, 2, 2, 2, 3 ),
 ( 0.9344201253893971160, 0.9411764705882352811, 0.9485294117647058432, 0.9558823529411765163, 0.9632352941176470784, 0.9705882352941176405 ),
 .UNSPECIFIED. ) 
 CURVE ( )  GEOMETRIC_REPRESENTATION_ITEM ( )  RATIONAL_B_SPLINE_CURVE ( ( 0.9886498549717824824, 0.9300557229131066750, 1.000000000000000000, 0.9238795325112867385, 1.000000000000000000, 0.9238795325112867385, 1.000000000000000000, 0.9238795325112867385, 1.000000000000000000, 0.9238795325112867385, 1.000000000000000000 ) ) 
 REPRESENTATION_ITEM ( '' )  );
#27788=CARTESIAN_POINT ( 'NONE',  ( 110.1247167782376124, -1.849990392679412565, 2.220446049250313081E-13 ) ) ;
#27790=CARTESIAN_POINT ( 'NONE',  ( 112.5622167782374703, 1.849990392679562001, -0.7662911109077087390 ) ) ;
#27793=CARTESIAN_POINT ( 'NONE',  ( 110.2738248654048903, -1.999999999999911626, -0.8284271247459952248 ) ) ;
#27808=CARTESIAN_POINT ( 'NONE',  ( 112.2261751345945555, 2.000000000000122125, -0.8284271247460553989 ) ) ;
#27812=EDGE_CURVE ( 'NONE', #7342, #15812, #7455, .T. ) ;
#27815=CARTESIAN_POINT ( 'NONE',  ( 108.5624999999997442, -2.499999999999934719, -1.035533905932568999 ) ) ;
#27819=SURFACE_STYLE_USAGE ( .BOTH. , #17463 ) ;
#27822=ORIENTED_EDGE ( 'NONE', *, *, #26900, .T. ) ;
#27829=CARTESIAN_POINT ( 'NONE',  ( 105.8124999999999574, 1.035533905932839449, -2.499999999999724221 ) ) ;
#27837=AXIS2_PLACEMENT_3D ( 'NONE', #2282, #17178, #5606 ) ;
#27843=CARTESIAN_POINT ( 'NONE',  ( 119.9999999999999574, -0.4876318259219858398, 1.939643060552387110 ) ) ;
#27847=CARTESIAN_POINT ( 'NONE',  ( 118.3752832217622029, 1.849990392679523588, 0.000000000000000000 ) ) ;
#27866=FACE_OUTER_BOUND ( 'NONE', #26028, .T. ) ;
#27867=CARTESIAN_POINT ( 'NONE',  ( 119.9999999999998721, -0.4876318259425804769, -1.939643060543838615 ) ) ;
#27868=CARTESIAN_POINT ( 'NONE',  ( 118.1247167782376408, -1.849990392679523588, 0.000000000000000000 ) ) ;
#27873=CARTESIAN_POINT ( 'NONE',  ( 113.5627832217622029, 0.7662911109078888172, 1.849990392679652151 ) ) ;
#27878=ORIENTED_EDGE ( 'NONE', *, *, #6608, .F. ) ;
#27882=CARTESIAN_POINT ( 'NONE',  ( 113.2886751345947118, 1.999999999999946265, 1.110223024625156540E-13 ) ) ;
#27890=CARTESIAN_POINT ( 'NONE',  ( 110.9999999999999147, 2.500000000000057732, 0.000000000000000000 ) ) ;
#27893=EDGE_CURVE ( 'NONE', #28223, #20037, #6426, .T. ) ;
#27898=CARTESIAN_POINT ( 'NONE',  ( 118.3124999999997726, -1.035533905932598975, 2.500000000000205169 ) ) ;
#27900=CARTESIAN_POINT ( 'NONE',  ( 105.8752832217621602, -1.849990392679412565, 2.220446049250313081E-13 ) ) ;
#27903=CARTESIAN_POINT ( 'NONE',  ( 107.6247167782376124, 1.849990392679523588, 0.000000000000000000 ) ) ;
#27905=CARTESIAN_POINT ( 'NONE',  ( 106.8363248654050750, 1.414213562373256572, 1.414213562373256572 ) ) ;
#27920=EDGE_CURVE ( 'NONE', #21920, #1067, #8386, .T. ) ;
#27924=CARTESIAN_POINT ( 'NONE',  ( 109.1252832217621744, -1.665334536937734811E-13, -1.849990392679523588 ) ) ;
#27938=CARTESIAN_POINT ( 'NONE',  ( 108.4372167782374419, 0.7662911109078588412, -1.849990392679231599 ) ) ;
#27944=CARTESIAN_POINT ( 'NONE',  ( 104.7401757384974417, 1.849990392679521589, 1.011113220803300925E-30 ) ) ;
#27953=CARTESIAN_POINT ( 'NONE',  ( 117.6011751345946266, -0.8284271247461453269, 2.000000000000212275 ) ) ;
#27954=CARTESIAN_POINT ( 'NONE',  ( 117.3988248654050892, -0.8284271247460250898, -1.999999999999851674 ) ) ;
#27963=CARTESIAN_POINT ( 'NONE',  ( 111.9999999999999716, 2.500000000000002220, 0.000000000000000000 ) ) ;
#27966=CARTESIAN_POINT ( 'NONE',  ( 115.0386751345947403, 1.110223024625156540E-13, -1.999999999999668709 ) ) ;
#27976=CARTESIAN_POINT ( 'NONE',  ( 105.4374999999998153, -2.499999999999994671, 1.035533905932929599 ) ) ;
#27995=ORIENTED_EDGE ( 'NONE', *, *, #9746, .F. ) ;
#27998=VECTOR ( 'NONE', #9893, 1000.000000000000000 ) ;
#28000=CARTESIAN_POINT ( 'NONE',  ( 118.7502832217622455, -1.308140751793529510, 1.308140751793640533 ) ) ;
#28006=CARTESIAN_POINT ( 'NONE',  ( 105.5238248654050750, 0.8284271247462654530, -1.999999999999851674 ) ) ;
#28017=CARTESIAN_POINT ( 'NONE',  ( 116.8747167782375556, 0.000000000000000000, 1.849990392679523588 ) ) ;
#28022=CARTESIAN_POINT ( 'NONE',  ( 114.0002832217621602, -1.308140751793585022, -1.308140751793640533 ) ) ;
#28044=CARTESIAN_POINT ( 'NONE',  ( 113.1249999999998295, 1.767766952966376426, 1.767766952966320915 ) ) ;
#28052=CARTESIAN_POINT ( 'NONE',  ( 114.8124999999998010, 1.035533905932749299, -2.499999999999844569 ) ) ;
#28054=CARTESIAN_POINT ( 'NONE',  ( 108.0002832217622597, -1.308140751793585022, -1.308140751793640533 ) ) ;
#28059=CARTESIAN_POINT ( 'NONE',  ( 105.4997167782376550, 1.308140751793668288, -1.308140751793640533 ) ) ;
#28073=CARTESIAN_POINT ( 'NONE',  ( 110.1249999999998437, 1.767766952966265404, 1.767766952966431937 ) ) ;
#28074=ORIENTED_EDGE ( 'NONE', *, *, #25322, .T. ) ;
#28079=CARTESIAN_POINT ( 'NONE',  ( 106.7502832217622597, -1.308140751793529510, 1.308140751793973600 ) ) ;
#28094=CARTESIAN_POINT ( 'NONE',  ( 109.9997167782376835, -1.308140751793612777, 1.308140751793640533 ) ) ;
#28096=EDGE_CURVE ( 'NONE', #27528, #13966, #6805, .T. ) ;
#28101=ORIENTED_EDGE ( 'NONE', *, *, #1011, .F. ) ;
#28120=VECTOR ( 'NONE', #27064, 1000.000000000000000 ) ;
#28123=CARTESIAN_POINT ( 'NONE',  ( 111.8124999999997584, 1.035533905932779275, -2.499999999999964473 ) ) ;
#28133=CARTESIAN_POINT ( 'NONE',  ( 106.1249999999999858, 1.767766952966320915, 1.767766952966431937 ) ) ;
#28150=CARTESIAN_POINT ( 'NONE',  ( 105.9372167782374135, -0.7662911109076184779, 1.849990392679652151 ) ) ;
#28152=CARTESIAN_POINT ( 'NONE',  ( 117.3752832217622029, 1.849990392679523588, 0.000000000000000000 ) ) ;
#28169=CARTESIAN_POINT ( 'NONE',  ( 119.6872167782376408, 1.849990392679562001, 0.7662911109079489913 ) ) ;
#28171=EDGE_CURVE ( 'NONE', #10146, #28423, #1351, .T. ) ;
#28175=CARTESIAN_POINT ( 'NONE',  ( 114.3127832217620465, 1.849990392679562001, -0.7662911109076485650 ) ) ;
#28185=DIRECTION ( 'NONE',  ( -1.000000000000000000, -1.665334536937736783E-16, -2.220446049250315546E-16 ) ) ;
#28190=CARTESIAN_POINT ( 'NONE',  ( 110.6249999999998437, -1.767766952966376426, -1.767766952966320915 ) ) ;
#28195=CARTESIAN_POINT ( 'NONE',  ( 115.6636751345946550, -1.414213562373090038, 1.414213562373145550 ) ) ;
#28202=CARTESIAN_POINT ( 'NONE',  ( 113.1249999999998295, 1.767766952966376426, 1.767766952966320915 ) ) ;
#28204=CARTESIAN_POINT ( 'NONE',  ( 105.3127832217621034, 1.849990392679562001, -0.7662911109076485650 ) ) ;
#28212=CARTESIAN_POINT ( 'NONE',  ( 107.1247167782375556, -1.849990392679301543, 2.220446049250313081E-13 ) ) ;
#28215=( BOUNDED_CURVE ( )  B_SPLINE_CURVE ( 2, ( #2750, #12469, #28685, #9834, #23812, #28843, #21809, #16634, #444 ),
 .UNSPECIFIED., .F., .T. ) 
 B_SPLINE_CURVE_WITH_KNOTS ( ( 3, 2, 2, 2, 3 ),
 ( 0.3823529411764705621, 0.3897058823529411242, 0.3970588235294117974, 0.4044117647058823595, 0.4117647058823529216 ),
 .UNSPECIFIED. ) 
 CURVE ( )  GEOMETRIC_REPRESENTATION_ITEM ( )  RATIONAL_B_SPLINE_CURVE ( ( 1.000000000000000000, 0.9238795325112867385, 1.000000000000000000, 0.9238795325112867385, 1.000000000000000000, 0.9238795325112867385, 1.000000000000000000, 0.9238795325112867385, 1.000000000000000000 ) ) 
 REPRESENTATION_ITEM ( '' )  );
#28216=ORIENTED_EDGE ( 'NONE', *, *, #1506, .F. ) ;
#28223=VERTEX_POINT ( 'NONE', #4353 ) ;
#28225=CARTESIAN_POINT ( 'NONE',  ( 110.1874999999997584, 1.035533905932779275, 2.500000000000205169 ) ) ;
#28229=CARTESIAN_POINT ( 'NONE',  ( 109.6636751345946976, -1.414213562373145550, 1.414213562373256572 ) ) ;
#28232=CARTESIAN_POINT ( 'NONE',  ( 108.4377832217621318, 1.849990392679532247, 0.7662911109080692285 ) ) ;
#28234=CARTESIAN_POINT ( 'NONE',  ( 119.5386751345946692, 2.775557561562891351E-14, 2.000000000000223821 ) ) ;
#28244=CYLINDRICAL_SURFACE ( 'NONE', #8178, 2.000000000000012879 ) ;
#28245=CARTESIAN_POINT ( 'NONE',  ( 116.6011751345946408, -0.8284271247461753029, 2.000000000000332179 ) ) ;
#28271=CARTESIAN_POINT ( 'NONE',  ( 109.2499999999999147, 0.000000000000000000, 2.499999999999946709 ) ) ;
#28282=CARTESIAN_POINT ( 'NONE',  ( 117.4372167782373566, 0.7662911109078888172, -1.849990392679411677 ) ) ;
#28287=CARTESIAN_POINT ( 'NONE',  ( 118.8749999999998295, 1.767766952966320915, -1.767766952966320915 ) ) ;
#28301=CARTESIAN_POINT ( 'NONE',  ( 104.9372167782373566, -0.7662911109077388261, 1.849990392679772278 ) ) ;
#28303=EDGE_CURVE ( 'NONE', #13966, #16234, #11911, .T. ) ;
#28304=CARTESIAN_POINT ( 'NONE',  ( 117.3127832217621318, 1.849990392679532247, -0.7662911109076485650 ) ) ;
#28308=DIRECTION ( 'NONE',  ( -5.551115123125785167E-17, 1.000000000000000000, 8.881784197001256268E-16 ) ) ;
#28321=CARTESIAN_POINT ( 'NONE',  ( 118.6872167782374703, 1.849990392679501827, 0.7662911109080090544 ) ) ;
#28323=VERTEX_POINT ( 'NONE', #4657 ) ;
#28338=DIRECTION ( 'NONE',  ( -1.000000000000000000, -1.665334536937736783E-16, -2.220446049250315546E-16 ) ) ;
#28344=CARTESIAN_POINT ( 'NONE',  ( 110.7499999999998010, 2.775557561562891351E-14, -2.499999999999946709 ) ) ;
#28354=CARTESIAN_POINT ( 'NONE',  ( 111.1874999999999858, 1.035533905932749299, 2.500000000000265121 ) ) ;
#28355=CARTESIAN_POINT ( 'NONE',  ( 112.1488248654050892, -1.999999999999941602, 0.8284271247463557142 ) ) ;
#28356=CARTESIAN_POINT ( 'NONE',  ( 106.4377832217622029, 1.849990392679562001, 0.7662911109078287542 ) ) ;
#28357=CARTESIAN_POINT ( 'NONE',  ( 112.8363248654051318, 1.414213562373201061, 1.414213562373256572 ) ) ;
#28371=CARTESIAN_POINT ( 'NONE',  ( 106.6249999999999289, -1.767766952966376426, -1.767766952966320915 ) ) ;
#28378=CARTESIAN_POINT ( 'NONE',  ( 107.7502832217622881, -1.308140751793585022, 1.308140751793751555 ) ) ;
#28411=ADVANCED_FACE ( 'NONE', ( #3396 ), #13837, .F. ) ;
#28420=CARTESIAN_POINT ( 'NONE',  ( 105.2499999999999147, -2.775557561562891351E-14, 2.499999999999946709 ) ) ;
#28421=CARTESIAN_POINT ( 'NONE',  ( 114.7886751345947403, -1.999999999999946265, 0.000000000000000000 ) ) ;
#28423=VERTEX_POINT ( 'NONE', #500 ) ;
#28429=CARTESIAN_POINT ( 'NONE',  ( 116.2497167782374845, -1.308140751793585022, -1.308140751793640533 ) ) ;
#28434=CARTESIAN_POINT ( 'NONE',  ( 119.4999999999999289, -2.499999999999919176, 0.000000000000000000 ) ) ;
#28450=CARTESIAN_POINT ( 'NONE',  ( 107.5622167782374561, 1.849990392679472073, -0.7662911109077686911 ) ) ;
#28453=CARTESIAN_POINT ( 'NONE',  ( 115.2502832217623592, 1.308140751793696044, -1.308140751793529510 ) ) ;
#28473=CARTESIAN_POINT ( 'NONE',  ( 112.5002832217623023, 1.308140751793696044, 1.308140751793640533 ) ) ;
#28474=EDGE_CURVE ( 'NONE', #1220, #13422, #14811, .T. ) ;
#28491=CARTESIAN_POINT ( 'NONE',  ( 111.0386751345947118, 5.551115123125782702E-14, -2.000000000000001776 ) ) ;
#28497=CARTESIAN_POINT ( 'NONE',  ( 111.7499999999998010, 0.000000000000000000, -2.499999999999946709 ) ) ;
#28502=CARTESIAN_POINT ( 'NONE',  ( 106.9761751345946266, -0.8284271247461453269, -1.999999999999791278 ) ) ;
#28503=CARTESIAN_POINT ( 'NONE',  ( 114.9999999999999716, 2.500000000000002220, 0.000000000000000000 ) ) ;
#28509=CARTESIAN_POINT ( 'NONE',  ( 106.3747167782374703, -5.551115123125782702E-14, -1.849990392679523588 ) ) ;
#28510=ORIENTED_EDGE ( 'NONE', *, *, #27230, .T. ) ;
#28518=CARTESIAN_POINT ( 'NONE',  ( 107.7499999999998579, 5.551115123125782702E-14, -2.499999999999946709 ) ) ;
#28520=CIRCLE ( 'NONE', #17788, 6.000000000000012434 ) ;
#28524=CARTESIAN_POINT ( 'NONE',  ( 107.1877832217621886, 0.7662911109078588412, -1.849990392679231599 ) ) ;
#28540=CARTESIAN_POINT ( 'NONE',  ( 116.5386751345946408, 1.110223024625156540E-13, 2.000000000000112799 ) ) ;
#28544=CARTESIAN_POINT ( 'NONE',  ( 110.1247167782376124, -1.849990392679412565, 2.220446049250313081E-13 ) ) ;
#28565=CARTESIAN_POINT ( 'NONE',  ( 107.4374999999997868, -2.499999999999964473, 1.035533905932989551 ) ) ;
#28568=AXIS2_PLACEMENT_3D ( 'NONE', #17386, #3209, #22437 ) ;
#28572=CARTESIAN_POINT ( 'NONE',  ( 107.7886751345947403, -1.999999999999835243, 1.110223024625156540E-13 ) ) ;
#28578=CARTESIAN_POINT ( 'NONE',  ( 119.4372167782374419, 0.7662911109078888172, -1.849990392679291551 ) ) ;
#28582=EDGE_CURVE ( 'NONE', #14144, #4583, #20321, .T. ) ;
#28584=CARTESIAN_POINT ( 'NONE',  ( 118.3124999999997726, -1.035533905932598975, 2.500000000000205169 ) ) ;
#28587=CARTESIAN_POINT ( 'NONE',  ( 115.3363248654051461, -1.414213562372979016, -1.414213562372812483 ) ) ;
#28593=CARTESIAN_POINT ( 'NONE',  ( 104.9997167782376692, -1.308140751793585022, 1.308140751793640533 ) ) ;
#28595=CARTESIAN_POINT ( 'NONE',  ( 113.9377832217623450, -1.849990392679441875, -0.7662911109076485650 ) ) ;
#28615=CARTESIAN_POINT ( 'NONE',  ( 119.2261751345946266, 2.000000000000001776, -0.8284271247459350507 ) ) ;
#28641=CARTESIAN_POINT ( 'NONE',  ( 109.2738248654049045, -1.999999999999941602, -0.8284271247458748766 ) ) ;
#28643=CARTESIAN_POINT ( 'NONE',  ( 111.1249999999999289, 1.767766952966320915, 1.767766952966431937 ) ) ;
#28650=CARTESIAN_POINT ( 'NONE',  ( 120.3752832217621460, 1.849990392679579099, 0.000000000000000000 ) ) ;
#28660=CARTESIAN_POINT ( 'NONE',  ( 106.9999999999999716, 2.500000000000030198, 0.000000000000000000 ) ) ;
#28668=CARTESIAN_POINT ( 'NONE',  ( 119.3124999999998437, -1.035533905932689347, 2.500000000000265121 ) ) ;
#28671=CARTESIAN_POINT ( 'NONE',  ( 113.7886751345947687, -1.999999999999918510, 0.000000000000000000 ) ) ;
#28685=CARTESIAN_POINT ( 'NONE',  ( 111.4136751345947260, 1.414213562373145550, 1.414213562373034527 ) ) ;
#28687=CARTESIAN_POINT ( 'NONE',  ( 109.6872167782374561, 1.849990392679562001, 0.7662911109080090544 ) ) ;
#28691=CARTESIAN_POINT ( 'NONE',  ( -1.110223024625164676E-16, 2.000000000000012879, 2.021286199229734960E-15 ) ) ;
#28696=ORIENTED_EDGE ( 'NONE', *, *, #19432, .F. ) ;
#28712=CARTESIAN_POINT ( 'NONE',  ( 108.9613248654050892, 1.110223024625156540E-13, 2.000000000000001776 ) ) ;
#28713=CARTESIAN_POINT ( 'NONE',  ( 107.1249999999998437, 1.767766952966265404, 1.767766952966320915 ) ) ;
#28719=CARTESIAN_POINT ( 'NONE',  ( 108.2886751345946834, 2.000000000000057288, 2.220446049250313081E-13 ) ) ;
#28724=CARTESIAN_POINT ( 'NONE',  ( 116.0622167782373566, -1.849990392679381701, 0.7662911109079489913 ) ) ;
#28730=CARTESIAN_POINT ( 'NONE',  ( 117.3124999999997300, -1.035533905932689347, 2.500000000000265121 ) ) ;
#28731=CARTESIAN_POINT ( 'NONE',  ( 5.000000000000018652, 6.000000000000081712, 1.170861610602048163E-13 ) ) ;
#28735=ORIENTED_EDGE ( 'NONE', *, *, #16971, .T. ) ;
#28747=CARTESIAN_POINT ( 'NONE',  ( 0.000000000000000000, 0.000000000000000000, 0.000000000000000000 ) ) ;
#28749=CARTESIAN_POINT ( 'NONE',  ( 114.6252832217623450, 0.000000000000000000, 1.849990392679523588 ) ) ;
#28779=CARTESIAN_POINT ( 'NONE',  ( 111.3988248654049613, -0.8284271247461153509, -1.999999999999791278 ) ) ;
#28783=( NAMED_UNIT ( * ) SI_UNIT ( $, .STERADIAN. ) SOLID_ANGLE_UNIT ( ) );
#28790=( BOUNDED_CURVE ( )  B_SPLINE_CURVE ( 2, ( #15741, #8795, #25050, #22771, #1715, #27953, #4917, #174, #19231 ),
 .UNSPECIFIED., .F., .F. ) 
 B_SPLINE_CURVE_WITH_KNOTS ( ( 3, 2, 2, 2, 3 ),
 ( 0.7352941176470588758, 0.7426470588235294379, 0.7500000000000000000, 0.7573529411764705621, 0.7647058823529411242 ),
 .UNSPECIFIED. ) 
 CURVE ( )  GEOMETRIC_REPRESENTATION_ITEM ( )  RATIONAL_B_SPLINE_CURVE ( ( 1.000000000000000000, 0.9238795325112867385, 1.000000000000000000, 0.9238795325112867385, 1.000000000000000000, 0.9238795325112867385, 1.000000000000000000, 0.9238795325112867385, 1.000000000000000000 ) ) 
 REPRESENTATION_ITEM ( '' )  );
#28797=CARTESIAN_POINT ( 'NONE',  ( 111.0624999999998295, 2.500000000000055067, 1.035533905932929599 ) ) ;
#28804=CARTESIAN_POINT ( 'NONE',  ( 119.5627832217620750, 0.7662911109078588412, 1.849990392679712103 ) ) ;
#28825=CARTESIAN_POINT ( 'NONE',  ( 120.9999999999997300, 2.500000000000113243, 3.330669073875469621E-13 ) ) ;
#28828=CARTESIAN_POINT ( 'NONE',  ( 0.000000000000000000, 0.000000000000000000, 0.000000000000000000 ) ) ;
#28838=CARTESIAN_POINT ( 'NONE',  ( 119.7499999999998721, 1.110223024625156540E-13, -2.499999999999946709 ) ) ;
#28843=CARTESIAN_POINT ( 'NONE',  ( 111.6011751345946692, -0.8284271247460852639, 2.000000000000212275 ) ) ;
#28849=B_SPLINE_CURVE_WITH_KNOTS ( 'NONE', 1,
 ( #12416, #21614 ),
 .UNSPECIFIED., .F., .F.,
 ( 2, 2 ),
 ( 0.000000000000000000, 0.9099963204919845339 ),
 .UNSPECIFIED. ) ;
#28852=DIRECTION ( 'NONE',  ( -1.000000000000000000, -1.665334536937736783E-16, -2.220446049250315546E-16 ) ) ;
#28855=EDGE_CURVE ( 'NONE', #10990, #15916, #21540, .T. ) ;
#28869=CARTESIAN_POINT ( 'NONE',  ( 105.9999999999998863, 2.500000000000002220, 1.110223024625156540E-13 ) ) ;
#28873=ORIENTED_EDGE ( 'NONE', *, *, #642, .T. ) ;
#28875=DIRECTION ( 'NONE',  ( -3.845925372767118265E-16, 1.000000000000000000, 8.881784197001258240E-16 ) ) ;
#28878=CARTESIAN_POINT ( 'NONE',  ( 119.2497167782374987, -1.308140751793557266, -1.308140751793640533 ) ) ;
#28884=CARTESIAN_POINT ( 'NONE',  ( 113.2499999999998437, 2.775557561562891351E-14, 2.500000000000168754 ) ) ;
#28909=ORIENTED_EDGE ( 'NONE', *, *, #5445, .T. ) ;
#28915=CARTESIAN_POINT ( 'NONE',  ( 114.6247167782376124, 1.849990392679523588, 0.000000000000000000 ) ) ;
#28921=CARTESIAN_POINT ( 'NONE',  ( 104.8283649806521396, 0.8716379956768015580, 1.698308124453599799 ) ) ;
#28933=MECHANICAL_DESIGN_GEOMETRIC_PRESENTATION_REPRESENTATION('',(#5393),#18219);
#28956=CARTESIAN_POINT ( 'NONE',  ( 104.3122167782373992, -0.7662911109076785410, -1.849990392679291551 ) ) ;
#28966=CARTESIAN_POINT ( 'NONE',  ( 114.0238248654048903, -0.8284271247461453269, 2.000000000000271783 ) ) ;
#28968=DIRECTION ( 'NONE',  ( 0.000000000000000000, -1.000000000000000000, -8.881784197001262184E-16 ) ) ;
#28976=CARTESIAN_POINT ( 'NONE',  ( 119.8749999999998863, 1.767766952966320915, -1.767766952966320915 ) ) ;
#28989=EDGE_CURVE ( 'NONE', #1067, #13876, #15829, .T. ) ;
#28997=CARTESIAN_POINT ( 'NONE',  ( 116.0863248654050608, -1.414213562373090038, 1.414213562373256572 ) ) ;
#29010=( BOUNDED_CURVE ( )  B_SPLINE_CURVE ( 2, ( #17872, #18735, #11687, #1546, #6160, #6458, #15577, #24890, #16448 ),
 .UNSPECIFIED., .F., .T. ) 
 B_SPLINE_CURVE_WITH_KNOTS ( ( 3, 2, 2, 2, 3 ),
 ( 0.5294117647058823595, 0.5367647058823529216, 0.5441176470588235947, 0.5514705882352941568, 0.5588235294117647189 ),
 .UNSPECIFIED. ) 
 CURVE ( )  GEOMETRIC_REPRESENTATION_ITEM ( )  RATIONAL_B_SPLINE_CURVE ( ( 1.000000000000000000, 0.9238795325112867385, 1.000000000000000000, 0.9238795325112867385, 1.000000000000000000, 0.9238795325112867385, 1.000000000000000000, 0.9238795325112867385, 1.000000000000000000 ) ) 
 REPRESENTATION_ITEM ( '' )  );
#29020=CARTESIAN_POINT ( 'NONE',  ( 107.6874999999997868, -1.035533905932659149, -2.499999999999724221 ) ) ;
#29033=CARTESIAN_POINT ( 'NONE',  ( 113.7497167782375698, 1.308140751793557266, 1.308140751793751555 ) ) ;
#29038=CARTESIAN_POINT ( 'NONE',  ( 112.8124999999998579, 1.035533905932779275, -2.499999999999904521 ) ) ;
#29040=DIRECTION ( 'NONE',  ( 5.551115123125785167E-17, -1.000000000000000000, -8.881784197001256268E-16 ) ) ;
#29061=EDGE_CURVE ( 'NONE', #22693, #4573, #10616, .T. ) ;
#29067=CARTESIAN_POINT ( 'NONE',  ( 114.7738248654050182, 2.000000000000061728, 0.8284271247462955401 ) ) ;
#29071=DIRECTION ( 'NONE',  ( -1.000000000000000000, -1.665334536937736783E-16, -2.220446049250315546E-16 ) ) ;
#29086=CARTESIAN_POINT ( 'NONE',  ( 118.0863248654050039, -1.414213562373034527, 1.414213562373256572 ) ) ;
#29098=DIRECTION ( 'NONE',  ( -1.000000000000000000, -1.665334536937736783E-16, -2.220446049250315546E-16 ) ) ;
#29105=CARTESIAN_POINT ( 'NONE',  ( 120.2502832217622739, 1.308140751793612777, -1.308140751793418488 ) ) ;
#29115=CARTESIAN_POINT ( 'NONE',  ( 104.6874999999998579, -1.035533905932689347, -2.499999999999724221 ) ) ;
#29119=ORIENTED_EDGE ( 'NONE', *, *, #20033, .F. ) ;
#29125=CARTESIAN_POINT ( 'NONE',  ( 120.6874999999997584, -1.035533905932719101, -2.499999999999844569 ) ) ;
#29137=FACE_OUTER_BOUND ( 'NONE', #27437, .T. ) ;
#29146=CARTESIAN_POINT ( 'NONE',  ( 115.8363248654051176, 1.414213562373117794, 1.414213562373034527 ) ) ;
#29155=ORIENTED_EDGE ( 'NONE', *, *, #14160, .F. ) ;
#29171=CARTESIAN_POINT ( 'NONE',  ( 108.5863248654051034, 1.414213562373173305, -1.414213562373145550 ) ) ;
#29172=CARTESIAN_POINT ( 'NONE',  ( 104.7401757384972996, -0.9317532982612999337, -1.616718326172621456 ) ) ;
#29175=CARTESIAN_POINT ( 'NONE',  ( 1.110223024625164183E-16, -2.000000000000012879, -1.776356839400262692E-15 ) ) ;
#29177=CARTESIAN_POINT ( 'NONE',  ( 112.4761751345946692, 0.8284271247462654530, 2.000000000000151879 ) ) ;
#29180=CARTESIAN_POINT ( 'NONE',  ( 112.1247167782376124, -1.849990392679579099, 1.110223024625156540E-13 ) ) ;
#29184=CARTESIAN_POINT ( 'NONE',  ( 114.3749999999998010, -1.767766952966154381, 1.767766952966653982 ) ) ;
#29214=CARTESIAN_POINT ( 'NONE',  ( 114.8363248654050324, 1.414213562373090038, 1.414213562373034527 ) ) ;
#29215=CARTESIAN_POINT ( 'NONE',  ( 111.6872167782374135, 1.849990392679562001, 0.7662911109079489913 ) ) ;
#29238=FILL_AREA_STYLE ('',( #30139 ) ) ;
#29250=CARTESIAN_POINT ( 'NONE',  ( 111.8363248654050039, 1.414213562373201061, 1.414213562373367594 ) ) ;
#29251=FACE_OUTER_BOUND ( 'NONE', #10843, .T. ) ;
#29256=CARTESIAN_POINT ( 'NONE',  ( 110.0386751345947971, 0.000000000000000000, -1.999999999999779732 ) ) ;
#29258=CARTESIAN_POINT ( 'NONE',  ( 119.3752832217622313, 1.849990392679523588, 0.000000000000000000 ) ) ;
#29262=ORIENTED_EDGE ( 'NONE', *, *, #10133, .F. ) ;
#29264=CYLINDRICAL_SURFACE ( 'NONE', #1835, 2.000000000000012879 ) ;
#29267=VERTEX_POINT ( 'NONE', #14169 ) ;
#29269=CARTESIAN_POINT ( 'NONE',  ( 105.3749999999999005, -1.767766952966320915, 1.767766952966431937 ) ) ;
#29278=CARTESIAN_POINT ( 'NONE',  ( 120.0624999999998721, 2.500000000000114575, 1.035533905932869425 ) ) ;
#29283=CARTESIAN_POINT ( 'NONE',  ( 105.9613248654051461, 5.551115123125782702E-14, 2.000000000000001776 ) ) ;
#29286=CYLINDRICAL_SURFACE ( 'NONE', #6770, 2.000000000000012879 ) ;
#29295=CARTESIAN_POINT ( 'NONE',  ( 111.3127832217622171, 1.849990392679501827, -0.7662911109077087390 ) ) ;
#29299=CARTESIAN_POINT ( 'NONE',  ( 109.8122167782375840, 0.7662911109078588412, 1.849990392679772278 ) ) ;
#29314=FILL_AREA_STYLE ('',( #24867 ) ) ;
#29322=CARTESIAN_POINT ( 'NONE',  ( 115.3752832217622881, 1.849990392679579099, 0.000000000000000000 ) ) ;
#29332=VERTEX_POINT ( 'NONE', #13550 ) ;
#29338=CARTESIAN_POINT ( 'NONE',  ( 114.4997167782375413, 1.308140751793696044, -1.308140751793640533 ) ) ;
#29344=CARTESIAN_POINT ( 'NONE',  ( 116.1874999999999005, 1.035533905932839227, 2.500000000000205169 ) ) ;
#29348=ADVANCED_FACE ( 'NONE', ( #18303 ), #23204, .F. ) ;
#29358=CARTESIAN_POINT ( 'NONE',  ( 104.1872167782373708, -1.849990392679351725, -0.7662911109074682647 ) ) ;
#29367=FACE_OUTER_BOUND ( 'NONE', #22502, .T. ) ;
#29369=CARTESIAN_POINT ( 'NONE',  ( 107.8749999999999858, 1.767766952966431937, -1.767766952966209892 ) ) ;
#29371=DIRECTION ( 'NONE',  ( 5.551115123125785167E-17, -1.000000000000000000, -8.881784197001256268E-16 ) ) ;
#29375=( BOUNDED_SURFACE ( )  B_SPLINE_SURFACE ( 1, 2, ( 
 ( #3188, #20102, #7954, #21806, #17824, #6112, #5491, #3046, #12464, #14896, #12612, #752, #10592, #17365, #26680, #21954, #888, #10139, #5643, #19507, #28838, #15047, #24393, #3337, #22106, #10437, #19790, #8096, #17513, #26825, #22254, #5789, #24538, #3488, #19943, #20396, #16140, #6404, #18578, #25285, #4257, #23179, #20555, #27898, #8731, #27742, #13677, #2123, #23018, #15525, #18118, #20715, #15839, #22865, #18421, #3795, #3939, #29906, #13525, #15985, #1803, #11526, #9182, #4103, #25445, #24846, #4409, #25138, #1964, #6260, #20867, #27287, #30063, #13834, #11051, #30218, #13225, #22565, #9033, #1655, #11368, #1495, #11208, #13369, #8886, #17974, #10907, #20262, #29608, #15681, #8569, #18273, #24989, #27586, #6564, #30371, #28503, #2858, #18729, #28052, #4568, #23771, #23485, #116, #9339, #21023, #7470, #25768, #12279, #16884, #21623, #555, #19170, #12131, #26203, #18881, #5154, #2423, #16442, #5006, #9644, #14146, #6872, #14569, #11837, #23917, #28202, #9945, #16737, #26061, #19321, #11988, #16295, #21173, #25615, #14438, #13994, #2704, #23333, #7179, #21475, #16591, #14289, #9791, #2276, #4713, #21319, #4861, #7329, #23630, #11680, #7024, #25913, #2565, #402, #261, #19036, #28354, #28643, #28797, #7759, #1424, #711, #18055, #24921, #12424, #3871, #26352, #29682, #27370, #8333, #10833, #25070, #15451, #17171, #24777, #1264, #5302, #3003, #21767, #11129, #7614, #15608, #14715, #3147, #6192, #20022, #3723, #13152, #17024, #22641, #24058, #26493, #5449, #20186, #10097, #15763, #13299, #19468, #1580, #12571, #8654, #4027, #17743, #29538, #13446, #22491, #21916, #8495, #10675, #29369, #27067, #6032, #17901, #27218, #10986, #20331, #22794, #1734, #11457, #16221, #25533, #29838, #14074, #9111, #23410, #23555, #9420, #18506, #9264, #11291, #7102, #1886, #4641, #2355, #16073, #18808, #14217, #28133, #11758, #6654, #30299, #20477, #27829, #18357, #2054, #22947, #18201, #18657, #27976, #20646, #16522, #25374, #27519, #21103, #25691, #13603, #32, #25844, #29992, #8968, #6496, #6950, #13759, #23106 ),
 ( #16368, #6797, #20801, #8816, #15919, #4791, #20949, #4496, #13919, #2493, #25220, #23262, #27674, #2203, #11608, #4188, #24276, #3082, #24137, #28578, #16814, #17103, #28878, #12505, #26580, #7259, #11918, #7546, #21844, #26284, #792, #19249, #26429, #14507, #14367, #19546, #12213, #14645, #23992, #14938, #17256, #16956, #7407, #21247, #2935, #188, #9571, #12352, #18965, #2785, #21703, #28282, #7695, #5233, #10176, #5385, #7842, #19401, #639, #12058, #4936, #5532, #16668, #25991, #23705, #2639, #21401, #334, #10022, #26136, #28429, #19104, #14792, #28724, #9727, #480, #5082, #23847, #21553, #9874, #8140, #20302, #10799, #17405, #8299, #29498, #19987, #8463, #3840, #6158, #22456, #17709, #10483, #19691, #5680, #12803, #20150, #22298, #29338, #17870, #10637, #27187, #22609, #27339, #13119, #29648, #15727, #10952, #3223, #1544, #29033, #15575, #15092, #15251, #7999, #8614, #27033, #18022, #13268, #5998, #15418, #12650, #21992, #3377, #24743, #926, #22144, #10325, #24582, #3684, #24430, #1390, #1229, #17557, #1087, #19833, #29180, #26874, #5836, #3530, #12961, #14036, #11253, #22908, #13569, #27634, #20763, #7069, #16335, #6913, #11418, #29951, #30261, #11721, #25656, #9380, #20443, #25035, #30109, #4607, #9073, #23374, #2009, #9226, #6613, #27479, #2320, #25332, #27788, #6764, #28094, #30413, #18466, #20604, #16185, #21064, #25492, #1850, #4457, #16035, #22759, #29802, #8780, #3990, #13412, #11568, #11097, #8931, #2168, #4307, #13883, #23223, #1700, #18616, #13726, #27938, #18167, #18774, #23068, #20913, #15883, #6456, #25182, #4148, #18321, #21117, #23865, #19270, #2805, #28450, #11776, #4952, #25552, #2509, #23428, #7118, #6967, #23279, #23720, #14387, #4658, #12231, #52, #2221, #7423, #349, #18674, #16831, #21569, #16386, #2373, #11625, #12079, #9441, #18824, #28150, #9280, #26152, #21417, #20969, #14240, #4811, #501, #5100, #9742, #14526, #16538, #9895, #25864, #23573, #28593, #28301, #11937, #4514, #13937, #21265, #30319, #204, #9590, #18979, #7281, #16685, #26007, #29358, #21865 ) ),
 .UNSPECIFIED., .F., .F., .T. ) 
 B_SPLINE_SURFACE_WITH_KNOTS ( ( 2, 2 ),
 ( 3, 2, 2, 2, 2, 2, 2, 2, 2, 2, 2, 2, 2, 2, 2, 2, 2, 2, 2, 2, 2, 2, 2, 2, 2, 2, 2, 2, 2, 2, 2, 2, 2, 2, 2, 2, 2, 2, 2, 2, 2, 2, 2, 2, 2, 2, 2, 2, 2, 2, 2, 2, 2, 2, 2, 2, 2, 2, 2, 2, 2, 2, 2, 2, 2, 2, 2, 2, 2, 2, 2, 2, 2, 2, 2, 2, 2, 2, 2, 2, 2, 2, 2, 2, 2, 2, 2, 2, 2, 2, 2, 2, 2, 2, 2, 2, 2, 2, 2, 2, 2, 2, 2, 2, 2, 2, 2, 2, 2, 2, 2, 2, 2, 2, 2, 2, 2, 2, 2, 2, 2, 2, 2, 2, 2, 2, 2, 2, 2, 2, 2, 2, 3 ),
 ( 0.000000000000000000, 1.000000000000000000 ),
 ( 0.000000000000000000, 0.007352941176470588133, 0.01470588235294117627, 0.02205882352941176613, 0.02941176470588235253, 0.03676470588235294240, 0.04411764705882353227, 0.05147058823529411520, 0.05882352941176470507, 0.06617647058823529493, 0.07352941176470588480, 0.08088235294117647467, 0.08823529411764706454, 0.09558823529411764053, 0.1029411764705882304, 0.1102941176470588203, 0.1176470588235294101, 0.1250000000000000000, 0.1323529411764705899, 0.1397058823529411797, 0.1470588235294117696, 0.1544117647058823595, 0.1617647058823529493, 0.1691176470588235392, 0.1764705882352941291, 0.1838235294117647189, 0.1911764705882352811, 0.1985294117647058709, 0.2058823529411764608, 0.2132352941176470507, 0.2205882352941176405, 0.2279411764705882304, 0.2352941176470588203, 0.2426470588235294101, 0.2500000000000000000, 0.2573529411764705621, 0.2647058823529411797, 0.2720588235294117418, 0.2794117647058823595, 0.2867647058823529216, 0.2941176470588235392, 0.3014705882352941013, 0.3088235294117647189, 0.3161764705882352811, 0.3235294117647058987, 0.3308823529411764608, 0.3382352941176470784, 0.3455882352941176405, 0.3529411764705882582, 0.3602941176470588203, 0.3676470588235294379, 0.3750000000000000000, 0.3823529411764705621, 0.3897058823529411797, 0.3970588235294117418, 0.4044117647058823595, 0.4117647058823529216, 0.4191176470588235392, 0.4264705882352941013, 0.4338235294117647189, 0.4411764705882352811, 0.4485294117647058987, 0.4558823529411764608, 0.4632352941176470784, 0.4705882352941176405, 0.4779411764705882582, 0.4852941176470588203, 0.4926470588235294379, 0.5000000000000000000, 0.5073529411764705621, 0.5147058823529411242, 0.5220588235294117974, 0.5294117647058823595, 0.5367647058823529216, 0.5441176470588234837, 0.5514705882352941568, 0.5588235294117647189, 0.5661764705882352811, 0.5735294117647058432, 0.5808823529411765163, 0.5882352941176470784, 0.5955882352941176405, 0.6029411764705882026, 0.6102941176470588758, 0.6176470588235294379, 0.6250000000000000000, 0.6323529411764705621, 0.6397058823529411242, 0.6470588235294117974, 0.6544117647058823595, 0.6617647058823529216, 0.6691176470588234837, 0.6764705882352941568, 0.6838235294117647189, 0.6911764705882352811, 0.6985294117647058432, 0.7058823529411765163, 0.7132352941176470784, 0.7205882352941176405, 0.7279411764705882026, 0.7352941176470588758, 0.7426470588235294379, 0.7500000000000000000, 0.7573529411764705621, 0.7647058823529411242, 0.7720588235294117974, 0.7794117647058823595, 0.7867647058823529216, 0.7941176470588234837, 0.8014705882352941568, 0.8088235294117647189, 0.8161764705882352811, 0.8235294117647058432, 0.8308823529411765163, 0.8382352941176470784, 0.8455882352941176405, 0.8529411764705882026, 0.8602941176470588758, 0.8676470588235294379, 0.8750000000000000000, 0.8823529411764705621, 0.8897058823529411242, 0.8970588235294117974, 0.9044117647058823595, 0.9117647058823529216, 0.9191176470588234837, 0.9264705882352941568, 0.9338235294117647189, 0.9411764705882352811, 0.9485294117647058432, 0.9558823529411765163, 0.9632352941176470784, 0.9705882352941176405 ),
 .UNSPECIFIED. ) 
 GEOMETRIC_REPRESENTATION_ITEM ( )  RATIONAL_B_SPLINE_SURFACE ( (
 ( 1.000000000000000000, 0.9238795325112867385, 1.000000000000000000, 0.9238795325112867385, 1.000000000000000000, 0.9238795325112867385, 1.000000000000000000, 0.9238795325112867385, 1.000000000000000000, 0.9238795325112867385, 1.000000000000000000, 0.9238795325112867385, 1.000000000000000000, 0.9238795325112867385, 1.000000000000000000, 0.9238795325112867385, 1.000000000000000000, 0.9238795325112867385, 1.000000000000000000, 0.9238795325112867385, 1.000000000000000000, 0.9238795325112867385, 1.000000000000000000, 0.9238795325112867385, 1.000000000000000000, 0.9238795325112867385, 1.000000000000000000, 0.9238795325112867385, 1.000000000000000000, 0.9238795325112867385, 1.000000000000000000, 0.9238795325112867385, 1.000000000000000000, 0.9238795325112867385, 1.000000000000000000, 0.9238795325112867385, 1.000000000000000000, 0.9238795325112867385, 1.000000000000000000, 0.9238795325112867385, 1.000000000000000000, 0.9238795325112867385, 1.000000000000000000, 0.9238795325112867385, 1.000000000000000000, 0.9238795325112867385, 1.000000000000000000, 0.9238795325112867385, 1.000000000000000000, 0.9238795325112867385, 1.000000000000000000, 0.9238795325112867385, 1.000000000000000000, 0.9238795325112867385, 1.000000000000000000, 0.9238795325112867385, 1.000000000000000000, 0.9238795325112867385, 1.000000000000000000, 0.9238795325112867385, 1.000000000000000000, 0.9238795325112867385, 1.000000000000000000, 0.9238795325112867385, 1.000000000000000000, 0.9238795325112867385, 1.000000000000000000, 0.9238795325112867385, 1.000000000000000000, 0.9238795325112867385, 1.000000000000000000, 0.9238795325112867385, 1.000000000000000000, 0.9238795325112867385, 1.000000000000000000, 0.9238795325112867385, 1.000000000000000000, 0.9238795325112867385, 1.000000000000000000, 0.9238795325112867385, 1.000000000000000000, 0.9238795325112867385, 1.000000000000000000, 0.9238795325112867385, 1.000000000000000000, 0.9238795325112867385, 1.000000000000000000, 0.9238795325112867385, 1.000000000000000000, 0.9238795325112867385, 1.000000000000000000, 0.9238795325112867385, 1.000000000000000000, 0.9238795325112867385, 1.000000000000000000, 0.9238795325112867385, 1.000000000000000000, 0.9238795325112867385, 1.000000000000000000, 0.9238795325112867385, 1.000000000000000000, 0.9238795325112867385, 1.000000000000000000, 0.9238795325112867385, 1.000000000000000000, 0.9238795325112867385, 1.000000000000000000, 0.9238795325112867385, 1.000000000000000000, 0.9238795325112867385, 1.000000000000000000, 0.9238795325112867385, 1.000000000000000000, 0.9238795325112867385, 1.000000000000000000, 0.9238795325112867385, 1.000000000000000000, 0.9238795325112867385, 1.000000000000000000, 0.9238795325112867385, 1.000000000000000000, 0.9238795325112867385, 1.000000000000000000, 0.9238795325112867385, 1.000000000000000000, 0.9238795325112867385, 1.000000000000000000, 0.9238795325112867385, 1.000000000000000000, 0.9238795325112867385, 1.000000000000000000, 0.9238795325112867385, 1.000000000000000000, 0.9238795325112867385, 1.000000000000000000, 0.9238795325112867385, 1.000000000000000000, 0.9238795325112867385, 1.000000000000000000, 0.9238795325112867385, 1.000000000000000000, 0.9238795325112867385, 1.000000000000000000, 0.9238795325112867385, 1.000000000000000000, 0.9238795325112867385, 1.000000000000000000, 0.9238795325112867385, 1.000000000000000000, 0.9238795325112867385, 1.000000000000000000, 0.9238795325112867385, 1.000000000000000000, 0.9238795325112867385, 1.000000000000000000, 0.9238795325112867385, 1.000000000000000000, 0.9238795325112867385, 1.000000000000000000, 0.9238795325112867385, 1.000000000000000000, 0.9238795325112867385, 1.000000000000000000, 0.9238795325112867385, 1.000000000000000000, 0.9238795325112867385, 1.000000000000000000, 0.9238795325112867385, 1.000000000000000000, 0.9238795325112867385, 1.000000000000000000, 0.9238795325112867385, 1.000000000000000000, 0.9238795325112867385, 1.000000000000000000, 0.9238795325112867385, 1.000000000000000000, 0.9238795325112867385, 1.000000000000000000, 0.9238795325112867385, 1.000000000000000000, 0.9238795325112867385, 1.000000000000000000, 0.9238795325112867385, 1.000000000000000000, 0.9238795325112867385, 1.000000000000000000, 0.9238795325112867385, 1.000000000000000000, 0.9238795325112867385, 1.000000000000000000, 0.9238795325112867385, 1.000000000000000000, 0.9238795325112867385, 1.000000000000000000, 0.9238795325112867385, 1.000000000000000000, 0.9238795325112867385, 1.000000000000000000, 0.9238795325112867385, 1.000000000000000000, 0.9238795325112867385, 1.000000000000000000, 0.9238795325112867385, 1.000000000000000000, 0.9238795325112867385, 1.000000000000000000, 0.9238795325112867385, 1.000000000000000000, 0.9238795325112867385, 1.000000000000000000, 0.9238795325112867385, 1.000000000000000000, 0.9238795325112867385, 1.000000000000000000, 0.9238795325112867385, 1.000000000000000000, 0.9238795325112867385, 1.000000000000000000, 0.9238795325112867385, 1.000000000000000000, 0.9238795325112867385, 1.000000000000000000, 0.9238795325112867385, 1.000000000000000000, 0.9238795325112867385, 1.000000000000000000, 0.9238795325112867385, 1.000000000000000000, 0.9238795325112867385, 1.000000000000000000, 0.9238795325112867385, 1.000000000000000000, 0.9238795325112867385, 1.000000000000000000, 0.9238795325112867385, 1.000000000000000000, 0.9238795325112867385, 1.000000000000000000, 0.9238795325112867385, 1.000000000000000000, 0.9238795325112867385, 1.000000000000000000, 0.9238795325112867385, 1.000000000000000000, 0.9238795325112867385, 1.000000000000000000, 0.9238795325112867385, 1.000000000000000000, 0.9238795325112867385, 1.000000000000000000, 0.9238795325112867385, 1.000000000000000000, 0.9238795325112867385, 1.000000000000000000, 0.9238795325112867385, 1.000000000000000000, 0.9238795325112867385, 1.000000000000000000, 0.9238795325112867385, 1.000000000000000000, 0.9238795325112867385, 1.000000000000000000, 0.9238795325112867385, 1.000000000000000000),
 ( 1.000000000000000000, 0.9238795325112867385, 1.000000000000000000, 0.9238795325112867385, 1.000000000000000000, 0.9238795325112867385, 1.000000000000000000, 0.9238795325112867385, 1.000000000000000000, 0.9238795325112867385, 1.000000000000000000, 0.9238795325112867385, 1.000000000000000000, 0.9238795325112867385, 1.000000000000000000, 0.9238795325112867385, 1.000000000000000000, 0.9238795325112867385, 1.000000000000000000, 0.9238795325112867385, 1.000000000000000000, 0.9238795325112867385, 1.000000000000000000, 0.9238795325112867385, 1.000000000000000000, 0.9238795325112867385, 1.000000000000000000, 0.9238795325112867385, 1.000000000000000000, 0.9238795325112867385, 1.000000000000000000, 0.9238795325112867385, 1.000000000000000000, 0.9238795325112867385, 1.000000000000000000, 0.9238795325112867385, 1.000000000000000000, 0.9238795325112867385, 1.000000000000000000, 0.9238795325112867385, 1.000000000000000000, 0.9238795325112867385, 1.000000000000000000, 0.9238795325112867385, 1.000000000000000000, 0.9238795325112867385, 1.000000000000000000, 0.9238795325112867385, 1.000000000000000000, 0.9238795325112867385, 1.000000000000000000, 0.9238795325112867385, 1.000000000000000000, 0.9238795325112867385, 1.000000000000000000, 0.9238795325112867385, 1.000000000000000000, 0.9238795325112867385, 1.000000000000000000, 0.9238795325112867385, 1.000000000000000000, 0.9238795325112867385, 1.000000000000000000, 0.9238795325112867385, 1.000000000000000000, 0.9238795325112867385, 1.000000000000000000, 0.9238795325112867385, 1.000000000000000000, 0.9238795325112867385, 1.000000000000000000, 0.9238795325112867385, 1.000000000000000000, 0.9238795325112867385, 1.000000000000000000, 0.9238795325112867385, 1.000000000000000000, 0.9238795325112867385, 1.000000000000000000, 0.9238795325112867385, 1.000000000000000000, 0.9238795325112867385, 1.000000000000000000, 0.9238795325112867385, 1.000000000000000000, 0.9238795325112867385, 1.000000000000000000, 0.9238795325112867385, 1.000000000000000000, 0.9238795325112867385, 1.000000000000000000, 0.9238795325112867385, 1.000000000000000000, 0.9238795325112867385, 1.000000000000000000, 0.9238795325112867385, 1.000000000000000000, 0.9238795325112867385, 1.000000000000000000, 0.9238795325112867385, 1.000000000000000000, 0.9238795325112867385, 1.000000000000000000, 0.9238795325112867385, 1.000000000000000000, 0.9238795325112867385, 1.000000000000000000, 0.9238795325112867385, 1.000000000000000000, 0.9238795325112867385, 1.000000000000000000, 0.9238795325112867385, 1.000000000000000000, 0.9238795325112867385, 1.000000000000000000, 0.9238795325112867385, 1.000000000000000000, 0.9238795325112867385, 1.000000000000000000, 0.9238795325112867385, 1.000000000000000000, 0.9238795325112867385, 1.000000000000000000, 0.9238795325112867385, 1.000000000000000000, 0.9238795325112867385, 1.000000000000000000, 0.9238795325112867385, 1.000000000000000000, 0.9238795325112867385, 1.000000000000000000, 0.9238795325112867385, 1.000000000000000000, 0.9238795325112867385, 1.000000000000000000, 0.9238795325112867385, 1.000000000000000000, 0.9238795325112867385, 1.000000000000000000, 0.9238795325112867385, 1.000000000000000000, 0.9238795325112867385, 1.000000000000000000, 0.9238795325112867385, 1.000000000000000000, 0.9238795325112867385, 1.000000000000000000, 0.9238795325112867385, 1.000000000000000000, 0.9238795325112867385, 1.000000000000000000, 0.9238795325112867385, 1.000000000000000000, 0.9238795325112867385, 1.000000000000000000, 0.9238795325112867385, 1.000000000000000000, 0.9238795325112867385, 1.000000000000000000, 0.9238795325112867385, 1.000000000000000000, 0.9238795325112867385, 1.000000000000000000, 0.9238795325112867385, 1.000000000000000000, 0.9238795325112867385, 1.000000000000000000, 0.9238795325112867385, 1.000000000000000000, 0.9238795325112867385, 1.000000000000000000, 0.9238795325112867385, 1.000000000000000000, 0.9238795325112867385, 1.000000000000000000, 0.9238795325112867385, 1.000000000000000000, 0.9238795325112867385, 1.000000000000000000, 0.9238795325112867385, 1.000000000000000000, 0.9238795325112867385, 1.000000000000000000, 0.9238795325112867385, 1.000000000000000000, 0.9238795325112867385, 1.000000000000000000, 0.9238795325112867385, 1.000000000000000000, 0.9238795325112867385, 1.000000000000000000, 0.9238795325112867385, 1.000000000000000000, 0.9238795325112867385, 1.000000000000000000, 0.9238795325112867385, 1.000000000000000000, 0.9238795325112867385, 1.000000000000000000, 0.9238795325112867385, 1.000000000000000000, 0.9238795325112867385, 1.000000000000000000, 0.9238795325112867385, 1.000000000000000000, 0.9238795325112867385, 1.000000000000000000, 0.9238795325112867385, 1.000000000000000000, 0.9238795325112867385, 1.000000000000000000, 0.9238795325112867385, 1.000000000000000000, 0.9238795325112867385, 1.000000000000000000, 0.9238795325112867385, 1.000000000000000000, 0.9238795325112867385, 1.000000000000000000, 0.9238795325112867385, 1.000000000000000000, 0.9238795325112867385, 1.000000000000000000, 0.9238795325112867385, 1.000000000000000000, 0.9238795325112867385, 1.000000000000000000, 0.9238795325112867385, 1.000000000000000000, 0.9238795325112867385, 1.000000000000000000, 0.9238795325112867385, 1.000000000000000000, 0.9238795325112867385, 1.000000000000000000, 0.9238795325112867385, 1.000000000000000000, 0.9238795325112867385, 1.000000000000000000, 0.9238795325112867385, 1.000000000000000000, 0.9238795325112867385, 1.000000000000000000, 0.9238795325112867385, 1.000000000000000000, 0.9238795325112867385, 1.000000000000000000, 0.9238795325112867385, 1.000000000000000000, 0.9238795325112867385, 1.000000000000000000, 0.9238795325112867385, 1.000000000000000000, 0.9238795325112867385, 1.000000000000000000, 0.9238795325112867385, 1.000000000000000000, 0.9238795325112867385, 1.000000000000000000, 0.9238795325112867385, 1.000000000000000000, 0.9238795325112867385, 1.000000000000000000, 0.9238795325112867385, 1.000000000000000000) ) ) 
 REPRESENTATION_ITEM ( '' )  SURFACE ( )  );
#29405=CARTESIAN_POINT ( 'NONE',  ( 114.3363248654051176, -1.414213562373256572, -1.414213562372923505 ) ) ;
#29408=CARTESIAN_POINT ( 'NONE',  ( 120.5622167782374419, 1.849990392679652151, -0.7662911109075283278 ) ) ;
#29415=CARTESIAN_POINT ( 'NONE',  ( 118.6877832217621460, -0.7662911109076785410, 1.849990392679712103 ) ) ;
#29420=AXIS2_PLACEMENT_3D ( 'NONE', #12591, #865, #28968 ) ;
#29431=CARTESIAN_POINT ( 'NONE',  ( 119.2113248654050466, -1.999999999999946265, 2.220446049250313081E-13 ) ) ;
#29433=CARTESIAN_POINT ( 'NONE',  ( 117.4374999999997584, -2.499999999999844569, 1.035533905932929599 ) ) ;
#29446=CARTESIAN_POINT ( 'NONE',  ( 110.9377832217620323, -1.849990392679411677, -0.7662911109076485650 ) ) ;
#29451=CARTESIAN_POINT ( 'NONE',  ( 108.3747167782376124, -1.665334536937734811E-13, -1.849990392679523588 ) ) ;
#29458=ORIENTED_EDGE ( 'NONE', *, *, #8341, .T. ) ;
#29461=( BOUNDED_CURVE ( )  B_SPLINE_CURVE ( 2, ( #15771, #16227, #4192, #30153, #22954, #1892, #11298, #7268, #28434, #5239, #21108, #21253, #16820, #9578, #2361, #7413, #14224, #26436, #28287, #2940, #14653, #14800, #5086, #11765, #2645, #2792, #39, #28584, #26141, #23997, #7551, #10029, #9880, #23852, #11923, #25849, #7700, #12357, #21707, #645, #17109, #19405, #14512, #28730, #21407, #12219, #18971, #9425, #16528, #16673, #19256, #12064, #14373, #21558, #338, #16961, #486, #5391, #4797, #23561, #4943, #29344, #15422, #27038, #12967, #8145, #931, #10180, #17262, #3231, #10642, #12809, #19838, #1234, #1094, #19992, #13122, #17875, #3536, #20156, #27192, #24283, #10805, #10331, #21851, #17715, #8306, #26881, #3383, #6004, #29184, #5538, #796, #24750, #19696, #17410, #26584, #7849, #3690, #22303, #19551, #15098, #17563, #24142, #22460, #22151, #8004, #5688, #28884, #1396, #29504, #26724, #24434, #8468, #6167, #29038, #21996, #12656, #14943, #10489, #3085, #5842, #15257, #12511, #24587, #7092, #22, #6640, #27963, #18797, #9249, #28123, #14208, #25835, #11746, #6940, #30136, #8955, #16062, #2037, #9409, #18642, #16509, #30289, #4785, #11906, #16658, #2346, #18954, #25981, #182, #4925, #21239, #18347, #23546, #4330, #4484, #6786, #25360, #23250, #16209, #20633, #2486, #9098, #25520, #13749, #23094, #9562, #21091, #29976, #11596, #2189, #28271, #7250, #22936, #1875, #20788, #27661, #16359, #11279, #11443, #13908, #18495, #27815, #20938, #25680, #4628, #14061, #23400, #26706, #5519, #26569, #628, #19239, #19535, #914, #14928, #29020, #9714, #14356, #10012, #28565, #21692, #17244, #2630, #2776, #28713, #12203, #23695, #19389, #26128, #7984, #9865, #24263, #7828, #12050, #7685, #3213, #21392, #14501, #23841, #10163, #17094, #12636, #28869, #21981, #21835, #5372, #21544, #7400, #19678, #10312, #17391, #324, #19095, #23982, #28420, #5074, #26421, #2923, #7534, #16807, #12340, #470, #14780, #16945, #26274, #783, #5224 ),
 .UNSPECIFIED., .F., .T. ) 
 B_SPLINE_CURVE_WITH_KNOTS ( ( 3, 2, 2, 2, 2, 2, 2, 2, 2, 2, 2, 2, 2, 2, 2, 2, 2, 2, 2, 2, 2, 2, 2, 2, 2, 2, 2, 2, 2, 2, 2, 2, 2, 2, 2, 2, 2, 2, 2, 2, 2, 2, 2, 2, 2, 2, 2, 2, 2, 2, 2, 2, 2, 2, 2, 2, 2, 2, 2, 2, 2, 2, 2, 2, 2, 2, 2, 2, 2, 2, 2, 2, 2, 2, 2, 2, 2, 2, 2, 2, 2, 2, 2, 2, 2, 2, 2, 2, 2, 2, 2, 2, 2, 2, 2, 2, 2, 2, 2, 2, 2, 2, 2, 2, 2, 2, 2, 2, 2, 2, 2, 2, 2, 2, 2, 2, 2, 2, 2, 2, 2, 2, 2, 2, 3 ),
 ( 0.05882352941176714062, 0.06617647058823770967, 0.07352941176470828566, 0.08088235294117884777, 0.08823529411764942376, 0.09558823529411997200, 0.1029411764705905480, 0.1102941176470611240, 0.1176470588235316861, 0.1250000000000022482, 0.1323529411764728381, 0.1397058823529434002, 0.1470588235294139623, 0.1544117647058845244, 0.1617647058823551143, 0.1691176470588256764, 0.1764705882352962663, 0.1838235294117668006, 0.1911764705882373350, 0.1985294117647079526, 0.2058823529411784869, 0.2132352941176490768, 0.2205882352941196389, 0.2279411764705902288, 0.2352941176470607632, 0.2426470588235313530, 0.2500000000000018874, 0.2573529411764724495, 0.2647058823529430671, 0.2720588235294135737, 0.2794117647058841913, 0.2867647058823546979, 0.2941176470588253711, 0.3014705882352958777, 0.3088235294117664953, 0.3161764705882370019, 0.3235294117647076195, 0.3308823529411781816, 0.3382352941176487993, 0.3455882352941193059, 0.3529411764705899235, 0.3602941176470604301, 0.3676470588235310477, 0.3750000000000015543, 0.3823529411764721719, 0.3897058823529427340, 0.3970588235294132962, 0.4044117647058838583, 0.4117647058823544204, 0.4191176470588250380, 0.4264705882352955446, 0.4338235294117661622, 0.4411764705882366688, 0.4485294117647072865, 0.4558823529411778486, 0.4632352941176484662, 0.4705882352941189728, 0.4779411764705895904, 0.4852941176470600970, 0.4926470588235307146, 0.5000000000000012212, 0.5073529411764717834, 0.5147058823529422344, 0.5220588235294129076, 0.5294117647058835807, 0.5367647058823540318, 0.5441176470588245939, 0.5514705882352952671, 0.5588235294117658292, 0.5661764705882363913, 0.5735294117647068424, 0.5808823529411775155, 0.5882352941176480776, 0.5955882352941186397, 0.6029411764705892018, 0.6102941176470598750, 0.6176470588235304371, 0.6250000000000008882, 0.6323529411764714503, 0.6397058823529420124, 0.6470588235294126855, 0.6544117647058831366, 0.6617647058823536987, 0.6691176470588242609, 0.6764705882352949340, 0.6838235294117654961, 0.6911764705882359472, 0.6985294117647066203, 0.7058823529411772935, 0.7132352941176478556, 0.7205882352941183067, 0.7279411764705888688, 0.7352941176470595419, 0.7426470588235301040, 0.7500000000000005551, 0.7573529411764711172, 0.7647058823529416793, 0.7720588235294123525, 0.7794117647058829146, 0.7867647058823533657, 0.7941176470588239278, 0.8014705882352946009, 0.8088235294117651630, 0.8161764705882356141, 0.8235294117647061762, 0.8308823529411768494, 0.8382352941176474115, 0.8455882352941180846, 0.8529411764705885357, 0.8602941176470592088, 0.8676470588235297710, 0.8750000000000003331, 0.8823529411764707842, 0.8897058823529413463, 0.8970588235294120194, 0.9044117647058825815, 0.9117647058823530326, 0.9191176470588235947, 0.9264705882352942679, 0.9338235294117648300, 0.9411764705882352811, 0.9485294117647058432, 0.9558823529411765163, 0.9632352941176470784, 0.9705882352941176405 ),
 .UNSPECIFIED. ) 
 CURVE ( )  GEOMETRIC_REPRESENTATION_ITEM ( )  RATIONAL_B_SPLINE_CURVE ( ( 0.9999999999999747979, 0.9238795325113119405, 1.000000000000000000, 0.9238795325112867385, 1.000000000000000000, 0.9238795325112867385, 1.000000000000000000, 0.9238795325112867385, 1.000000000000000000, 0.9238795325112867385, 1.000000000000000000, 0.9238795325112867385, 1.000000000000000000, 0.9238795325112867385, 1.000000000000000000, 0.9238795325112867385, 1.000000000000000000, 0.9238795325112867385, 1.000000000000000000, 0.9238795325112867385, 1.000000000000000000, 0.9238795325112867385, 1.000000000000000000, 0.9238795325112867385, 1.000000000000000000, 0.9238795325112867385, 1.000000000000000000, 0.9238795325112867385, 1.000000000000000000, 0.9238795325112867385, 1.000000000000000000, 0.9238795325112867385, 1.000000000000000000, 0.9238795325112867385, 1.000000000000000000, 0.9238795325112867385, 1.000000000000000000, 0.9238795325112867385, 1.000000000000000000, 0.9238795325112867385, 1.000000000000000000, 0.9238795325112867385, 1.000000000000000000, 0.9238795325112867385, 1.000000000000000000, 0.9238795325112867385, 1.000000000000000000, 0.9238795325112867385, 1.000000000000000000, 0.9238795325112867385, 1.000000000000000000, 0.9238795325112867385, 1.000000000000000000, 0.9238795325112867385, 1.000000000000000000, 0.9238795325112867385, 1.000000000000000000, 0.9238795325112867385, 1.000000000000000000, 0.9238795325112867385, 1.000000000000000000, 0.9238795325112867385, 1.000000000000000000, 0.9238795325112867385, 1.000000000000000000, 0.9238795325112867385, 1.000000000000000000, 0.9238795325112867385, 1.000000000000000000, 0.9238795325112867385, 1.000000000000000000, 0.9238795325112867385, 1.000000000000000000, 0.9238795325112867385, 1.000000000000000000, 0.9238795325112867385, 1.000000000000000000, 0.9238795325112867385, 1.000000000000000000, 0.9238795325112867385, 1.000000000000000000, 0.9238795325112867385, 1.000000000000000000, 0.9238795325112867385, 1.000000000000000000, 0.9238795325112867385, 1.000000000000000000, 0.9238795325112867385, 1.000000000000000000, 0.9238795325112867385, 1.000000000000000000, 0.9238795325112867385, 1.000000000000000000, 0.9238795325112867385, 1.000000000000000000, 0.9238795325112867385, 1.000000000000000000, 0.9238795325112867385, 1.000000000000000000, 0.9238795325112867385, 1.000000000000000000, 0.9238795325112867385, 1.000000000000000000, 0.9238795325112867385, 1.000000000000000000, 0.9238795325112867385, 1.000000000000000000, 0.9238795325112867385, 1.000000000000000000, 0.9238795325112867385, 1.000000000000000000, 0.9238795325112867385, 1.000000000000000000, 0.9238795325112867385, 1.000000000000000000, 0.9238795325112867385, 1.000000000000000000, 0.9238795325112867385, 1.000000000000000000, 0.9238795325112867385, 1.000000000000000000, 0.9238795325112867385, 1.000000000000000000, 0.9238795325112867385, 1.000000000000000000, 0.9238795325112867385, 1.000000000000000000, 0.9238795325112867385, 1.000000000000000000, 0.9238795325112867385, 1.000000000000000000, 0.9238795325112867385, 1.000000000000000000, 0.9238795325112867385, 1.000000000000000000, 0.9238795325112867385, 1.000000000000000000, 0.9238795325112867385, 1.000000000000000000, 0.9238795325112867385, 1.000000000000000000, 0.9238795325112867385, 1.000000000000000000, 0.9238795325112867385, 1.000000000000000000, 0.9238795325112867385, 1.000000000000000000, 0.9238795325112867385, 1.000000000000000000, 0.9238795325112867385, 1.000000000000000000, 0.9238795325112867385, 1.000000000000000000, 0.9238795325112867385, 1.000000000000000000, 0.9238795325112867385, 1.000000000000000000, 0.9238795325112867385, 1.000000000000000000, 0.9238795325112867385, 1.000000000000000000, 0.9238795325112867385, 1.000000000000000000, 0.9238795325112867385, 1.000000000000000000, 0.9238795325112867385, 1.000000000000000000, 0.9238795325112867385, 1.000000000000000000, 0.9238795325112867385, 1.000000000000000000, 0.9238795325112867385, 1.000000000000000000, 0.9238795325112867385, 1.000000000000000000, 0.9238795325112867385, 1.000000000000000000, 0.9238795325112867385, 1.000000000000000000, 0.9238795325112867385, 1.000000000000000000, 0.9238795325112867385, 1.000000000000000000, 0.9238795325112867385, 1.000000000000000000, 0.9238795325112867385, 1.000000000000000000, 0.9238795325112867385, 1.000000000000000000, 0.9238795325112867385, 1.000000000000000000, 0.9238795325112867385, 1.000000000000000000, 0.9238795325112867385, 1.000000000000000000, 0.9238795325112867385, 1.000000000000000000, 0.9238795325112867385, 1.000000000000000000, 0.9238795325112867385, 1.000000000000000000, 0.9238795325112867385, 1.000000000000000000, 0.9238795325112867385, 1.000000000000000000, 0.9238795325112867385, 1.000000000000000000, 0.9238795325112867385, 1.000000000000000000, 0.9238795325112867385, 1.000000000000000000, 0.9238795325112867385, 1.000000000000000000, 0.9238795325112867385, 1.000000000000000000, 0.9238795325112867385, 1.000000000000000000, 0.9238795325112867385, 1.000000000000000000, 0.9238795325112867385, 1.000000000000000000, 0.9238795325112867385, 1.000000000000000000, 0.9238795325112867385, 1.000000000000000000, 0.9238795325112867385, 1.000000000000000000, 0.9238795325112867385, 1.000000000000000000, 0.9238795325112867385, 1.000000000000000000, 0.9238795325112867385, 1.000000000000000000, 0.9238795325112867385, 1.000000000000000000, 0.9238795325112867385, 1.000000000000000000, 0.9238795325112867385, 1.000000000000000000, 0.9238795325112867385, 1.000000000000000000, 0.9238795325112867385, 1.000000000000000000, 0.9238795325112867385, 1.000000000000000000, 0.9238795325112867385, 1.000000000000000000, 0.9238795325112867385, 1.000000000000000000 ) ) 
 REPRESENTATION_ITEM ( '' )  );
#29463=ORIENTED_EDGE ( 'NONE', *, *, #28171, .T. ) ;
#29470=AXIS2_PLACEMENT_3D ( 'NONE', #12526, #21568, #10196 ) ;
#29471=EDGE_LOOP ( 'NONE', ( #26624, #165, #5763, #4255 ) ) ;
#29479=CARTESIAN_POINT ( 'NONE',  ( 113.8127832217621034, -1.849990392679441875, 0.7662911109079489913 ) ) ;
#29483=CARTESIAN_POINT ( 'NONE',  ( 119.3988248654050039, -0.8284271247460852639, -1.999999999999791278 ) ) ;
#29498=CARTESIAN_POINT ( 'NONE',  ( 115.3122167782374845, -0.7662911109077388261, -1.849990392679291551 ) ) ;
#29504=CARTESIAN_POINT ( 'NONE',  ( 113.1249999999998295, 1.767766952966376426, 1.767766952966320915 ) ) ;
#29510=VERTEX_POINT ( 'NONE', #21646 ) ;
#29517=LINE ( 'NONE', #22006, #19226 ) ;
#29522=( BOUNDED_CURVE ( )  B_SPLINE_CURVE ( 2, ( #29431, #15188, #22552, #1485, #26666, #1168, #10576, #1330, #10423 ),
 .UNSPECIFIED., .F., .F. ) 
 B_SPLINE_CURVE_WITH_KNOTS ( ( 3, 2, 2, 2, 3 ),
 ( 0.08823529411764706454, 0.09558823529411764053, 0.1029411764705882304, 0.1102941176470588203, 0.1176470588235294101 ),
 .UNSPECIFIED. ) 
 CURVE ( )  GEOMETRIC_REPRESENTATION_ITEM ( )  RATIONAL_B_SPLINE_CURVE ( ( 1.000000000000000000, 0.9238795325112867385, 1.000000000000000000, 0.9238795325112867385, 1.000000000000000000, 0.9238795325112867385, 1.000000000000000000, 0.9238795325112867385, 1.000000000000000000 ) ) 
 REPRESENTATION_ITEM ( '' )  );
#29538=CARTESIAN_POINT ( 'NONE',  ( 108.2499999999998863, 5.551115123125782702E-14, 2.499999999999946709 ) ) ;
#29559=CARTESIAN_POINT ( 'NONE',  ( 110.4136751345947260, 1.414213562373117794, 1.414213562373034527 ) ) ;
#29565=CARTESIAN_POINT ( 'NONE',  ( 104.5622167782374561, 1.849990392679501827, -0.7662911109076485650 ) ) ;
#29570=EDGE_CURVE ( 'NONE', #16234, #26967, #3470, .T. ) ;
#29578=ORIENTED_EDGE ( 'NONE', *, *, #27893, .F. ) ;
#29582=CARTESIAN_POINT ( 'NONE',  ( 116.9377832217621460, -1.849990392679441875, -0.7662911109077087390 ) ) ;
#29583=FACE_OUTER_BOUND ( 'NONE', #14377, .T. ) ;
#29599=CARTESIAN_POINT ( 'NONE',  ( 117.0624999999998579, 2.500000000000234479, 1.035533905932989551 ) ) ;
#29602=FACE_OUTER_BOUND ( 'NONE', #3775, .T. ) ;
#29606=EDGE_LOOP ( 'NONE', ( #23963, #23704 ) ) ;
#29608=CARTESIAN_POINT ( 'NONE',  ( 115.4999999999998153, -2.499999999999891198, 0.000000000000000000 ) ) ;
#29609=CARTESIAN_POINT ( 'NONE',  ( 108.9377832217621886, -1.849990392679411677, -0.7662911109076485650 ) ) ;
#29631=EDGE_CURVE ( 'NONE', #29267, #12068, #29522, .T. ) ;
#29633=CARTESIAN_POINT ( 'NONE',  ( 113.0627832217621886, -0.7662911109076184779, -1.849990392679291551 ) ) ;
#29647=ORIENTED_EDGE ( 'NONE', *, *, #28303, .F. ) ;
#29648=CARTESIAN_POINT ( 'NONE',  ( 114.0622167782374845, -1.849990392679501827, 0.7662911109078287542 ) ) ;
#29652=( BOUNDED_CURVE ( )  B_SPLINE_CURVE ( 2, ( #23628, #401, #21915, #28502, #2856, #2561, #11985, #26058, #9943 ),
 .UNSPECIFIED., .F., .T. ) 
 B_SPLINE_CURVE_WITH_KNOTS ( ( 3, 2, 2, 2, 3 ),
 ( 0.1176470588235294379, 0.1250000000000000000, 0.1323529411764705621, 0.1397058823529411242, 0.1470588235294117974 ),
 .UNSPECIFIED. ) 
 CURVE ( )  GEOMETRIC_REPRESENTATION_ITEM ( )  RATIONAL_B_SPLINE_CURVE ( ( 1.000000000000000000, 0.9238795325112867385, 1.000000000000000000, 0.9238795325112867385, 1.000000000000000000, 0.9238795325112867385, 1.000000000000000000, 0.9238795325112867385, 1.000000000000000000 ) ) 
 REPRESENTATION_ITEM ( '' )  );
#29659=ORIENTED_EDGE ( 'NONE', *, *, #2900, .T. ) ;
#29682=CARTESIAN_POINT ( 'NONE',  ( 110.4999999999999432, -2.499999999999891198, 3.330669073875469621E-13 ) ) ;
#29684=FACE_OUTER_BOUND ( 'NONE', #12438, .T. ) ;
#29688=EDGE_CURVE ( 'NONE', #6944, #15581, #16519, .T. ) ;
#29690=VECTOR ( 'NONE', #18391, 1000.000000000000114 ) ;
#29700=VERTEX_POINT ( 'NONE', #684 ) ;
#29702=CARTESIAN_POINT ( 'NONE',  ( 105.2886751345946550, 2.000000000000057288, 0.000000000000000000 ) ) ;
#29705=CARTESIAN_POINT ( 'NONE',  ( 121.2502832217622171, 1.308140751793640533, -1.308140751793418488 ) ) ;
#29721=CARTESIAN_POINT ( 'NONE',  ( 116.3752832217622597, 1.849990392679523588, 0.000000000000000000 ) ) ;
#29737=DIRECTION ( 'NONE',  ( -1.000000000000000000, -1.665334536937736783E-16, -2.220446049250315546E-16 ) ) ;
#29744=CARTESIAN_POINT ( 'NONE',  ( 116.1874999999999005, 1.035533905932839449, 2.500000000000205169 ) ) ;
#29747=CARTESIAN_POINT ( 'NONE',  ( 106.0238248654050182, -0.8284271247461453269, 2.000000000000332179 ) ) ;
#29754=CARTESIAN_POINT ( 'NONE',  ( 112.3752832217621176, 1.849990392679551343, 0.000000000000000000 ) ) ;
#29758=CARTESIAN_POINT ( 'NONE',  ( 109.4997167782374845, 1.308140751793696044, -1.308140751793640533 ) ) ;
#29782=CARTESIAN_POINT ( 'NONE',  ( 1.110223024625164183E-16, -2.000000000000012879, -1.776356839400262692E-15 ) ) ;
#29800=VERTEX_POINT ( 'NONE', #12254 ) ;
#29802=CARTESIAN_POINT ( 'NONE',  ( 109.3122167782373566, -0.7662911109077388261, -1.849990392679351725 ) ) ;
#29808=ORIENTED_EDGE ( 'NONE', *, *, #18463, .F. ) ;
#29810=CARTESIAN_POINT ( 'NONE',  ( 105.8511751345945981, -1.999999999999911626, -0.8284271247459350507 ) ) ;
#29831=CYLINDRICAL_SURFACE ( 'NONE', #13582, 2.000000000000012879 ) ;
#29836=( BOUNDED_CURVE ( )  B_SPLINE_CURVE ( 2, ( #16734, #7468, #5002, #14437, #5152, #12278, #19318, #28641, #7612 ),
 .UNSPECIFIED., .F., .T. ) 
 B_SPLINE_CURVE_WITH_KNOTS ( ( 3, 2, 2, 2, 3 ),
 ( 0.6470588235294117974, 0.6544117647058823595, 0.6617647058823529216, 0.6691176470588234837, 0.6764705882352941568 ),
 .UNSPECIFIED. ) 
 CURVE ( )  GEOMETRIC_REPRESENTATION_ITEM ( )  RATIONAL_B_SPLINE_CURVE ( ( 1.000000000000000000, 0.9238795325112867385, 1.000000000000000000, 0.9238795325112867385, 1.000000000000000000, 0.9238795325112867385, 1.000000000000000000, 0.9238795325112867385, 1.000000000000000000 ) ) 
 REPRESENTATION_ITEM ( '' )  );
#29838=CARTESIAN_POINT ( 'NONE',  ( 107.1249999999998437, 1.767766952966265404, 1.767766952966320915 ) ) ;
#29854=CARTESIAN_POINT ( 'NONE',  ( 113.1636751345946692, 1.414213562373145550, -1.414213562372812483 ) ) ;
#29866=CARTESIAN_POINT ( 'NONE',  ( 104.8953215971908293, -1.758631583619322480, -0.8464305698015709423 ) ) ;
#29877=CARTESIAN_POINT ( 'NONE',  ( 118.8127832217620465, -1.849990392679381701, 0.7662911109078287542 ) ) ;
#29895=CARTESIAN_POINT ( 'NONE',  ( 115.3124999999998863, -1.035533905932659149, 2.500000000000205169 ) ) ;
#29906=CARTESIAN_POINT ( 'NONE',  ( 117.4374999999997584, -2.499999999999844569, 1.035533905932929599 ) ) ;
#29907=CARTESIAN_POINT ( 'NONE',  ( 109.6252832217622739, -2.775557561562891351E-14, 1.849990392679523588 ) ) ;
#29910=EDGE_LOOP ( 'NONE', ( #13968, #2066, #24659 ) ) ;
#29912=CARTESIAN_POINT ( 'NONE',  ( 108.2497167782376266, -1.308140751793585022, -1.308140751793640533 ) ) ;
#29934=CARTESIAN_POINT ( 'NONE',  ( 111.1877832217622029, 0.7662911109078588412, -1.849990392679411677 ) ) ;
#29950=ORIENTED_EDGE ( 'NONE', *, *, #7956, .F. ) ;
#29951=CARTESIAN_POINT ( 'NONE',  ( 111.1872167782375698, -1.849990392679472073, -0.7662911109075283278 ) ) ;
#29952=CARTESIAN_POINT ( 'NONE',  ( 118.7113248654050750, 1.999999999999946265, 1.110223024625156540E-13 ) ) ;
#29953=CARTESIAN_POINT ( 'NONE',  ( 111.6247167782376408, 1.849990392679523588, 0.000000000000000000 ) ) ;
#29961=VECTOR ( 'NONE', #15594, 1000.000000000000000 ) ;
#29976=CARTESIAN_POINT ( 'NONE',  ( 109.4374999999998863, -2.499999999999934719, 1.035533905932929599 ) ) ;
#29978=CARTESIAN_POINT ( 'NONE',  ( 106.6011751345947118, -0.8284271247462053900, 2.000000000000271783 ) ) ;
#29992=CARTESIAN_POINT ( 'NONE',  ( 104.8124999999997868, 1.035533905932779275, -2.499999999999904521 ) ) ;
#30007=CARTESIAN_POINT ( 'NONE',  ( 105.2261751345946408, 2.000000000000062172, -0.8284271247459947807 ) ) ;
#30011=CARTESIAN_POINT ( 'NONE',  ( 120.6252832217622881, 2.775557561562891351E-14, 1.849990392679523588 ) ) ;
#30031=CARTESIAN_POINT ( 'NONE',  ( 116.6247167782376692, 1.849990392679523588, 0.000000000000000000 ) ) ;
#30050=EDGE_CURVE ( 'NONE', #20271, #20037, #2266, .T. ) ;
#30054=CARTESIAN_POINT ( 'NONE',  ( 116.8749999999998863, 1.767766952966320915, -1.767766952966320915 ) ) ;
#30060=CARTESIAN_POINT ( 'NONE',  ( 107.2113248654050608, -1.999999999999946265, 0.000000000000000000 ) ) ;
#30063=CARTESIAN_POINT ( 'NONE',  ( 116.4999999999999574, -2.499999999999891198, 0.000000000000000000 ) ) ;
#30065=CARTESIAN_POINT ( 'NONE',  ( 107.4377832217621744, 1.849990392679562001, 0.7662911109080692285 ) ) ;
#30069=CARTESIAN_POINT ( 'NONE',  ( 107.7497167782375982, 1.308140751793668288, 1.308140751793640533 ) ) ;
#30072=CARTESIAN_POINT ( 'NONE',  ( 106.7113248654050324, 2.000000000000001776, 1.110223024625156540E-13 ) ) ;
#30074=EDGE_CURVE ( 'NONE', #12110, #19914, #28520, .T. ) ;
#30076=ORIENTED_EDGE ( 'NONE', *, *, #17139, .F. ) ;
#30081=VERTEX_POINT ( 'NONE', #30284 ) ;
#30086=CARTESIAN_POINT ( 'NONE',  ( 107.7886751345947403, -1.999999999999835243, 1.110223024625156540E-13 ) ) ;
#30087=EDGE_LOOP ( 'NONE', ( #15024, #18420, #10962, #10253 ) ) ;
#30091=CARTESIAN_POINT ( 'NONE',  ( 109.7261751345946408, -1.999999999999941602, 0.8284271247463557142 ) ) ;
#30094=CARTESIAN_POINT ( 'NONE',  ( 110.1877832217620750, 0.7662911109078588412, -1.849990392679411677 ) ) ;
#30108=VERTEX_POINT ( 'NONE', #6783 ) ;
#30109=CARTESIAN_POINT ( 'NONE',  ( 110.7497167782376550, 1.308140751793640533, 1.308140751793640533 ) ) ;
#30111=CARTESIAN_POINT ( 'NONE',  ( 111.5622167782373566, 1.849990392679591977, -0.7662911109075283278 ) ) ;
#30136=CARTESIAN_POINT ( 'NONE',  ( 111.4999999999998863, -2.499999999999946709, 1.110223024625156540E-13 ) ) ;
#30139=FILL_AREA_STYLE_COLOUR ( '', #9767 ) ;
#30153=CARTESIAN_POINT ( 'NONE',  ( 119.8124999999998721, 1.035533905932839227, -2.499999999999844569 ) ) ;
#30154=( BOUNDED_CURVE ( )  B_SPLINE_CURVE ( 2, ( #26968, #8400, #5774, #3621, #3468, #19635, #7938, #26123, #10421 ),
 .UNSPECIFIED., .F., .F. ) 
 B_SPLINE_CURVE_WITH_KNOTS ( ( 3, 2, 2, 2, 3 ),
 ( 0.6470588235294116863, 0.6544117647058823595, 0.6617647058823529216, 0.6691176470588235947, 0.6764705882352941568 ),
 .UNSPECIFIED. ) 
 CURVE ( )  GEOMETRIC_REPRESENTATION_ITEM ( )  RATIONAL_B_SPLINE_CURVE ( ( 1.000000000000000000, 0.9238795325112867385, 1.000000000000000000, 0.9238795325112867385, 1.000000000000000000, 0.9238795325112867385, 1.000000000000000000, 0.9238795325112867385, 1.000000000000000000 ) ) 
 REPRESENTATION_ITEM ( '' )  );
#30167=CARTESIAN_POINT ( 'NONE',  ( 119.0002832217622455, -1.308140751793585022, -1.308140751793529510 ) ) ;
#30175=CARTESIAN_POINT ( 'NONE',  ( 116.7113248654051318, 2.000000000000057288, 0.000000000000000000 ) ) ;
#30184=CARTESIAN_POINT ( 'NONE',  ( 118.6247167782376408, 1.849990392679468076, 0.000000000000000000 ) ) ;
#30189=CARTESIAN_POINT ( 'NONE',  ( 115.1877832217620892, 0.7662911109078588412, -1.849990392679231599 ) ) ;
#30210=CARTESIAN_POINT ( 'NONE',  ( 113.2499999999998437, 2.775557561562891351E-14, 2.500000000000168754 ) ) ;
#30218=CARTESIAN_POINT ( 'NONE',  ( 116.3124999999997158, -1.035533905932598975, 2.500000000000144773 ) ) ;
#30220=CARTESIAN_POINT ( 'NONE',  ( 107.9377832217621886, -1.849990392679472073, -0.7662911109075283278 ) ) ;
#30240=CARTESIAN_POINT ( 'NONE',  ( 111.2261751345945981, 2.000000000000061728, -0.8284271247459952248 ) ) ;
#30244=CARTESIAN_POINT ( 'NONE',  ( 112.3127832217622455, 1.849990392679411677, -0.7662911109077087390 ) ) ;
#30260=ORIENTED_EDGE ( 'NONE', *, *, #13890, .T. ) ;
#30261=CARTESIAN_POINT ( 'NONE',  ( 111.1247167782376124, -1.849990392679579099, 1.110223024625156540E-13 ) ) ;
#30265=EDGE_CURVE ( 'NONE', #3730, #24742, #30154, .T. ) ;
#30266=CARTESIAN_POINT ( 'NONE',  ( 110.3363248654051318, -1.414213562373201061, -1.414213562373034527 ) ) ;
#30272=ORIENTED_EDGE ( 'NONE', *, *, #28171, .F. ) ;
#30284=CARTESIAN_POINT ( 'NONE',  ( 104.7401757384974417, 1.849990392679521589, 1.011113220803300925E-30 ) ) ;
#30289=CARTESIAN_POINT ( 'NONE',  ( 111.0624999999998295, 2.500000000000054623, 1.035533905932929599 ) ) ;
#30299=CARTESIAN_POINT ( 'NONE',  ( 105.9374999999997584, 2.500000000000144773, -1.035533905932568777 ) ) ;
#30319=CARTESIAN_POINT ( 'NONE',  ( 104.6247167782375271, 1.849990392679523588, 0.000000000000000000 ) ) ;
#30321=CARTESIAN_POINT ( 'NONE',  ( 117.5627832217621460, 0.7662911109078588412, 1.849990392679772278 ) ) ;
#30338=DIRECTION ( 'NONE',  ( 5.551115123125785167E-17, -1.000000000000000000, -8.881784197001256268E-16 ) ) ;
#30340=CARTESIAN_POINT ( 'NONE',  ( 117.8122167782374135, 0.7662911109077388261, 1.849990392679832230 ) ) ;
#30345=CARTESIAN_POINT ( 'NONE',  ( 113.2502832217622455, 1.308140751793612777, -1.308140751793640533 ) ) ;
#30347=VERTEX_POINT ( 'NONE', #25431 ) ;
#30352=ORIENTED_EDGE ( 'NONE', *, *, #30265, .F. ) ;
#30361=CARTESIAN_POINT ( 'NONE',  ( 111.4374999999997300, -2.499999999999904521, 1.035533905932869425 ) ) ;
#30364=CARTESIAN_POINT ( 'NONE',  ( 0.000000000000000000, 0.000000000000000000, 0.000000000000000000 ) ) ;
#30371=CARTESIAN_POINT ( 'NONE',  ( 115.0624999999998153, 2.499999999999994671, 1.035533905932929599 ) ) ;
#30373=CARTESIAN_POINT ( 'NONE',  ( 107.5002832217622881, 1.308140751793585022, 1.308140751793751555 ) ) ;
#30378=CARTESIAN_POINT ( 'NONE',  ( 106.6872167782374277, 1.849990392679562001, 0.7662911109079489913 ) ) ;
#30392=CARTESIAN_POINT ( 'NONE',  ( 107.6249999999998721, -1.767766952966376426, -1.767766952966320915 ) ) ;
#30398=CARTESIAN_POINT ( 'NONE',  ( 107.6252832217623308, -2.775557561562891351E-14, 1.849990392679523588 ) ) ;
#30402=EDGE_CURVE ( 'NONE', #4728, #20271, #13509, .T. ) ;
#30412=VERTEX_POINT ( 'NONE', #22549 ) ;
#30413=CARTESIAN_POINT ( 'NONE',  ( 109.9372167782373424, -0.7662911109076785410, 1.849990392679712103 ) ) ;
ENDSEC;
END-ISO-10303-21;
